ISO-10303-21;
HEADER;
FILE_DESCRIPTION (('STEP AP214'),
    '1' );
FILE_NAME ('spur gear_iso_ISO - Spur gear 2M 30T 20PA 10FW ---S30B10H150L6.0S1.step',
    '2026-09-30T13:58:28',
    ( '' ),
    ( '' ),
    'SwSTEP 2.0',
    'SolidWorks 2026',
    '' );
FILE_SCHEMA (( 'AUTOMOTIVE_DESIGN' ));
ENDSEC;

DATA;
#5=EDGE_CURVE ( 'NONE', #21395, #6732, #6706, .T. ) ;
#8=PLANE ( 'NONE',  #10324 ) ;
#10=DIRECTION ( 'NONE',  ( 0.000000000000000000, -0.8660254037844328234, -0.5000000000000101030 ) ) ;
#15=ORIENTED_EDGE ( 'NONE', *, *, #3774, .T. ) ;
#16=LINE ( 'NONE', #18466, #6212 ) ;
#23=CIRCLE ( 'NONE', #12352, 32.00000000000000000 ) ;
#24=CYLINDRICAL_SURFACE ( 'NONE', #8070, 11.99999999999999822 ) ;
#26=ORIENTED_EDGE ( 'NONE', *, *, #547, .T. ) ;
#27=DIRECTION ( 'NONE',  ( 0.000000000000000000, -0.2079116908177664202, 0.9781476007338040235 ) ) ;
#28=ORIENTED_EDGE ( 'NONE', *, *, #6517, .T. ) ;
#29=EDGE_CURVE ( 'NONE', #3387, #1233, #12896, .T. ) ;
#31=EDGE_CURVE ( 'NONE', #17610, #10261, #11843, .T. ) ;
#35=DIRECTION ( 'NONE',  ( 0.000000000000000000, 0.000000000000000000, 1.000000000000000000 ) ) ;
#37=FACE_OUTER_BOUND ( 'NONE', #13774, .T. ) ;
#44=EDGE_LOOP ( 'NONE', ( #15562, #858, #14802, #18530 ) ) ;
#50=CARTESIAN_POINT ( 'NONE',  ( 10.00000000000000000, -19.07277123396528395, -19.80970465344768172 ) ) ;
#51=ORIENTED_EDGE ( 'NONE', *, *, #17728, .T. ) ;
#54=FACE_OUTER_BOUND ( 'NONE', #7670, .T. ) ;
#61=DIRECTION ( 'NONE',  ( 0.000000000000000000, -0.5877852522924797984, 0.8090169943749425663 ) ) ;
#62=DIRECTION ( 'NONE',  ( 1.000000000000000000, 0.000000000000000000, -0.000000000000000000 ) ) ;
#69=ORIENTED_EDGE ( 'NONE', *, *, #9047, .F. ) ;
#74=AXIS2_PLACEMENT_3D ( 'NONE', #17668, #2628, #2518 ) ;
#80=DIRECTION ( 'NONE',  ( 0.000000000000000000, 0.000000000000000000, 1.000000000000000000 ) ) ;
#82=DIRECTION ( 'NONE',  ( -1.000000000000000000, -0.000000000000000000, -0.000000000000000000 ) ) ;
#98=ORIENTED_EDGE ( 'NONE', *, *, #11209, .F. ) ;
#99=CIRCLE ( 'NONE', #20908, 27.49900000000000233 ) ;
#100=ORIENTED_EDGE ( 'NONE', *, *, #14180, .F. ) ;
#102=ORIENTED_EDGE ( 'NONE', *, *, #14178, .T. ) ;
#104=CIRCLE ( 'NONE', #9604, 12.00000000000000000 ) ;
#105=EDGE_LOOP ( 'NONE', ( #14807, #14622, #2671, #8655 ) ) ;
#116=DIRECTION ( 'NONE',  ( -1.000000000000000000, 0.000000000000000000, 0.000000000000000000 ) ) ;
#117=CIRCLE ( 'NONE', #19528, 32.00000000000000000 ) ;
#118=EDGE_CURVE ( 'NONE', #7770, #17965, #10413, .T. ) ;
#119=EDGE_LOOP ( 'NONE', ( #6288, #20757, #6100, #17161 ) ) ;
#121=ORIENTED_EDGE ( 'NONE', *, *, #11165, .T. ) ;
#123=AXIS2_PLACEMENT_3D ( 'NONE', #20145, #6454, #4998 ) ;
#126=ORIENTED_EDGE ( 'NONE', *, *, #4189, .T. ) ;
#127=ORIENTED_EDGE ( 'NONE', *, *, #547, .F. ) ;
#129=FACE_OUTER_BOUND ( 'NONE', #11446, .T. ) ;
#130=VECTOR ( 'NONE', #16734, 1000.000000000000000 ) ;
#142=VERTEX_POINT ( 'NONE', #1713 ) ;
#144=EDGE_CURVE ( 'NONE', #2079, #18856, #6208, .T. ) ;
#147=VECTOR ( 'NONE', #20842, 1000.000000000000000 ) ;
#158=ORIENTED_EDGE ( 'NONE', *, *, #20800, .T. ) ;
#163=VECTOR ( 'NONE', #1366, 1000.000000000000000 ) ;
#175=ADVANCED_FACE ( 'NONE', ( #54 ), #18832, .T. ) ;
#177=DIRECTION ( 'NONE',  ( -1.000000000000000000, -0.000000000000000000, -0.000000000000000000 ) ) ;
#179=DIRECTION ( 'NONE',  ( -1.000000000000000000, -0.000000000000000000, -0.000000000000000000 ) ) ;
#186=ORIENTED_EDGE ( 'NONE', *, *, #21572, .F. ) ;
#188=AXIS2_PLACEMENT_3D ( 'NONE', #7103, #5656, #15592 ) ;
#201=DIRECTION ( 'NONE',  ( -1.000000000000000000, 0.000000000000000000, 0.000000000000000000 ) ) ;
#206=CARTESIAN_POINT ( 'NONE',  ( 10.00000000000000000, 0.000000000000000000, 0.000000000000000000 ) ) ;
#207=EDGE_CURVE ( 'NONE', #13474, #6639, #1819, .T. ) ;
#221=ORIENTED_EDGE ( 'NONE', *, *, #20358, .T. ) ;
#223=ORIENTED_EDGE ( 'NONE', *, *, #9452, .F. ) ;
#225=DIRECTION ( 'NONE',  ( 0.000000000000000000, 0.000000000000000000, -1.000000000000000000 ) ) ;
#226=CARTESIAN_POINT ( 'NONE',  ( 10.00000000000000000, 0.000000000000000000, 0.000000000000000000 ) ) ;
#227=CARTESIAN_POINT ( 'NONE',  ( 10.00000000000000000, -27.26034713664092379, 4.817140289263571518 ) ) ;
#229=CARTESIAN_POINT ( 'NONE',  ( 10.00000000000000000, 25.48117629651189375, 10.33947075754270095 ) ) ;
#230=DIRECTION ( 'NONE',  ( 0.000000000000000000, 0.5877852522924741363, -0.8090169943749466741 ) ) ;
#231=CIRCLE ( 'NONE', #6580, 12.00000000000000000 ) ;
#233=CIRCLE ( 'NONE', #1637, 32.00000000000000000 ) ;
#234=VECTOR ( 'NONE', #13783, 1000.000000000000000 ) ;
#235=DIRECTION ( 'NONE',  ( -1.000000000000000000, 0.000000000000000000, 0.000000000000000000 ) ) ;
#240=ORIENTED_EDGE ( 'NONE', *, *, #6283, .F. ) ;
#241=DIRECTION ( 'NONE',  ( 0.000000000000000000, 0.000000000000000000, 1.000000000000000000 ) ) ;
#242=ORIENTED_EDGE ( 'NONE', *, *, #31, .T. ) ;
#243=AXIS2_PLACEMENT_3D ( 'NONE', #14900, #16894, #21541 ) ;
#253=ORIENTED_EDGE ( 'NONE', *, *, #21351, .F. ) ;
#254=EDGE_CURVE ( 'NONE', #9160, #4990, #3798, .T. ) ;
#255=CIRCLE ( 'NONE', #10121, 11.99999999999999822 ) ;
#261=DIRECTION ( 'NONE',  ( -1.000000000000000000, -0.000000000000000000, -0.000000000000000000 ) ) ;
#262=EDGE_LOOP ( 'NONE', ( #26, #4295, #8253, #16006 ) ) ;
#263=ORIENTED_EDGE ( 'NONE', *, *, #7411, .F. ) ;
#264=DIRECTION ( 'NONE',  ( -1.000000000000000000, -0.000000000000000000, -0.000000000000000000 ) ) ;
#266=ORIENTED_EDGE ( 'NONE', *, *, #14983, .F. ) ;
#285=LINE ( 'NONE', #7031, #6929 ) ;
#289=VERTEX_POINT ( 'NONE', #1331 ) ;
#296=ORIENTED_EDGE ( 'NONE', *, *, #20800, .F. ) ;
#317=VECTOR ( 'NONE', #1446, 1000.000000000000000 ) ;
#324=AXIS2_PLACEMENT_3D ( 'NONE', #2500, #12657, #2719 ) ;
#327=ORIENTED_EDGE ( 'NONE', *, *, #5685, .T. ) ;
#337=ORIENTED_EDGE ( 'NONE', *, *, #5445, .T. ) ;
#338=CARTESIAN_POINT ( 'NONE',  ( 0.000000000000000000, -13.56333590713994575, -28.98337314858449076 ) ) ;
#344=CARTESIAN_POINT ( 'NONE',  ( 0.000000000000000000, 12.46320060045762013, -29.47318494484016327 ) ) ;
#346=DIRECTION ( 'NONE',  ( 1.000000000000000000, -0.000000000000000000, -0.000000000000000000 ) ) ;
#353=DIRECTION ( 'NONE',  ( -1.000000000000000000, 0.000000000000000000, -0.000000000000000000 ) ) ;
#354=ORIENTED_EDGE ( 'NONE', *, *, #19846, .T. ) ;
#358=CIRCLE ( 'NONE', #2121, 27.49900000000000944 ) ;
#359=CIRCLE ( 'NONE', #4230, 27.49900000000000233 ) ;
#361=CARTESIAN_POINT ( 'NONE',  ( 10.00000000000000000, -27.26034713664092379, -7.182859710736426706 ) ) ;
#363=DIRECTION ( 'NONE',  ( 0.000000000000000000, 0.000000000000000000, 1.000000000000000000 ) ) ;
#377=ORIENTED_EDGE ( 'NONE', *, *, #8030, .T. ) ;
#391=ORIENTED_EDGE ( 'NONE', *, *, #16340, .T. ) ;
#394=CARTESIAN_POINT ( 'NONE',  ( 10.00000000000000000, 28.15804365424197186, -1.358152127006073684 ) ) ;
#402=DIRECTION ( 'NONE',  ( 0.000000000000000000, -0.8660254037844328234, -0.5000000000000101030 ) ) ;
#404=DIRECTION ( 'NONE',  ( -1.000000000000000000, -0.000000000000000000, 0.000000000000000000 ) ) ;
#407=DIRECTION ( 'NONE',  ( 1.000000000000000000, 0.000000000000000000, 0.000000000000000000 ) ) ;
#423=EDGE_CURVE ( 'NONE', #1592, #10683, #10658, .T. ) ;
#424=ORIENTED_EDGE ( 'NONE', *, *, #5191, .T. ) ;
#428=VERTEX_POINT ( 'NONE', #21651 ) ;
#432=CARTESIAN_POINT ( 'NONE',  ( 5.000000000000000000, -30.24235385705231849, -10.45944707835137777 ) ) ;
#448=VECTOR ( 'NONE', #10833, 1000.000000000000000 ) ;
#451=DIRECTION ( 'NONE',  ( 0.000000000000000000, 0.2079116908177599532, -0.9781476007338055778 ) ) ;
#462=DIRECTION ( 'NONE',  ( 0.000000000000000000, 0.000000000000000000, 1.000000000000000000 ) ) ;
#468=CARTESIAN_POINT ( 'NONE',  ( 0.000000000000000000, 0.000000000000000000, 0.000000000000000000 ) ) ;
#483=CARTESIAN_POINT ( 'NONE',  ( 0.000000000000000000, 0.000000000000000000, 0.000000000000000000 ) ) ;
#489=DIRECTION ( 'NONE',  ( -1.000000000000000000, 0.000000000000000000, 0.000000000000000000 ) ) ;
#501=ORIENTED_EDGE ( 'NONE', *, *, #10543, .F. ) ;
#514=DIRECTION ( 'NONE',  ( 0.000000000000000000, -0.9945218953682744001, 0.1045284632676437286 ) ) ;
#525=CIRCLE ( 'NONE', #18926, 32.00000000000000000 ) ;
#531=ORIENTED_EDGE ( 'NONE', *, *, #20947, .F. ) ;
#532=DIRECTION ( 'NONE',  ( 0.000000000000000000, 0.000000000000000000, -1.000000000000000000 ) ) ;
#546=AXIS2_PLACEMENT_3D ( 'NONE', #10508, #2124, #572 ) ;
#547=EDGE_CURVE ( 'NONE', #16474, #10634, #16910, .T. ) ;
#557=FACE_OUTER_BOUND ( 'NONE', #3741, .T. ) ;
#560=CIRCLE ( 'NONE', #1979, 32.00000000000000000 ) ;
#563=AXIS2_PLACEMENT_3D ( 'NONE', #8857, #15596, #14375 ) ;
#569=VERTEX_POINT ( 'NONE', #15459 ) ;
#572=DIRECTION ( 'NONE',  ( 0.000000000000000000, 0.000000000000000000, 1.000000000000000000 ) ) ;
#582=ORIENTED_EDGE ( 'NONE', *, *, #10536, .F. ) ;
#586=ORIENTED_EDGE ( 'NONE', *, *, #3118, .T. ) ;
#588=EDGE_CURVE ( 'NONE', #8553, #4990, #15267, .T. ) ;
#592=FACE_OUTER_BOUND ( 'NONE', #14290, .T. ) ;
#594=ORIENTED_EDGE ( 'NONE', *, *, #1930, .F. ) ;
#597=EDGE_CURVE ( 'NONE', #6613, #715, #14016, .T. ) ;
#598=DIRECTION ( 'NONE',  ( 0.000000000000000000, -0.5877852522924632561, -0.8090169943749545567 ) ) ;
#611=DIRECTION ( 'NONE',  ( 0.000000000000000000, 0.000000000000000000, 1.000000000000000000 ) ) ;
#619=CARTESIAN_POINT ( 'NONE',  ( 0.000000000000000000, -27.07404830566974141, 4.815694066514342175 ) ) ;
#628=VERTEX_POINT ( 'NONE', #13806 ) ;
#632=DIRECTION ( 'NONE',  ( 0.000000000000000000, -0.8660254037844327124, -0.5000000000000103251 ) ) ;
#633=CIRCLE ( 'NONE', #5574, 11.99999999999999645 ) ;
#648=DIRECTION ( 'NONE',  ( 0.000000000000000000, 0.000000000000000000, 1.000000000000000000 ) ) ;
#652=DIRECTION ( 'NONE',  ( -1.000000000000000000, 0.000000000000000000, 0.000000000000000000 ) ) ;
#663=AXIS2_PLACEMENT_3D ( 'NONE', #18207, #3060, #9786 ) ;
#666=AXIS2_PLACEMENT_3D ( 'NONE', #6861, #10168, #5524 ) ;
#667=VERTEX_POINT ( 'NONE', #18888 ) ;
#671=ADVANCED_FACE ( 'NONE', ( #17558 ), #2098, .T. ) ;
#680=DIRECTION ( 'NONE',  ( 0.000000000000000000, -0.4067366430757888285, -0.9135454576426059736 ) ) ;
#681=CYLINDRICAL_SURFACE ( 'NONE', #11395, 11.99999999999999822 ) ;
#682=CARTESIAN_POINT ( 'NONE',  ( 10.00000000000000000, 0.000000000000000000, 0.000000000000000000 ) ) ;
#685=FACE_OUTER_BOUND ( 'NONE', #14334, .T. ) ;
#688=DIRECTION ( 'NONE',  ( -1.000000000000000000, 0.000000000000000000, -0.000000000000000000 ) ) ;
#689=ORIENTED_EDGE ( 'NONE', *, *, #10298, .T. ) ;
#692=CYLINDRICAL_SURFACE ( 'NONE', #12976, 27.49900000000000233 ) ;
#696=ADVANCED_FACE ( 'NONE', ( #2956 ), #11142, .T. ) ;
#698=DIRECTION ( 'NONE',  ( 0.000000000000000000, 0.9945218953682737340, -0.1045284632676503622 ) ) ;
#703=ORIENTED_EDGE ( 'NONE', *, *, #1678, .T. ) ;
#705=DIRECTION ( 'NONE',  ( -1.000000000000000000, 0.000000000000000000, -0.000000000000000000 ) ) ;
#706=DIRECTION ( 'NONE',  ( -1.000000000000000000, 0.000000000000000000, -0.000000000000000000 ) ) ;
#715=VERTEX_POINT ( 'NONE', #17891 ) ;
#716=EDGE_CURVE ( 'NONE', #7135, #13798, #8224, .T. ) ;
#719=ADVANCED_FACE ( 'NONE', ( #7822 ), #1191, .T. ) ;
#723=FACE_OUTER_BOUND ( 'NONE', #4694, .T. ) ;
#731=LINE ( 'NONE', #12221, #17426 ) ;
#736=CYLINDRICAL_SURFACE ( 'NONE', #5140, 27.49900000000000233 ) ;
#747=FACE_OUTER_BOUND ( 'NONE', #17905, .T. ) ;
#759=CARTESIAN_POINT ( 'NONE',  ( 0.000000000000000000, -12.94633825542284100, 24.26081875733330051 ) ) ;
#771=VERTEX_POINT ( 'NONE', #861 ) ;
#778=CARTESIAN_POINT ( 'NONE',  ( 10.00000000000000000, 19.07277123396568896, -19.80970465344728737 ) ) ;
#781=AXIS2_PLACEMENT_3D ( 'NONE', #11638, #6451, #15157 ) ;
#784=DIRECTION ( 'NONE',  ( -1.000000000000000000, 0.000000000000000000, -0.000000000000000000 ) ) ;
#789=ORIENTED_EDGE ( 'NONE', *, *, #14633, .F. ) ;
#793=ADVANCED_FACE ( 'NONE', ( #7721 ), #12574, .T. ) ;
#796=ORIENTED_EDGE ( 'NONE', *, *, #7154, .F. ) ;
#801=LINE ( 'NONE', #17290, #19926 ) ;
#806=DIRECTION ( 'NONE',  ( -1.000000000000000000, 0.000000000000000000, 0.000000000000000000 ) ) ;
#808=EDGE_CURVE ( 'NONE', #1381, #2463, #1520, .T. ) ;
#810=ADVANCED_FACE ( 'NONE', ( #19317 ), #6296, .T. ) ;
#811=EDGE_CURVE ( 'NONE', #9001, #20936, #12797, .T. ) ;
#817=CARTESIAN_POINT ( 'NONE',  ( 0.000000000000000000, 27.82509854686817263, -4.525913221810857756 ) ) ;
#818=ORIENTED_EDGE ( 'NONE', *, *, #17741, .T. ) ;
#819=VECTOR ( 'NONE', #6483, 1000.000000000000000 ) ;
#830=EDGE_LOOP ( 'NONE', ( #3498, #14260, #1454, #15635 ) ) ;
#834=CARTESIAN_POINT ( 'NONE',  ( 0.000000000000000000, 23.57863763525741874, -15.45211464167639548 ) ) ;
#839=VERTEX_POINT ( 'NONE', #13118 ) ;
#842=EDGE_CURVE ( 'NONE', #7508, #15448, #1880, .T. ) ;
#844=DIRECTION ( 'NONE',  ( 0.000000000000000000, -6.938893903907229167E-15, 1.000000000000000000 ) ) ;
#850=EDGE_LOOP ( 'NONE', ( #11771, #11484, #2762, #12556 ) ) ;
#855=LINE ( 'NONE', #7604, #2634 ) ;
#858=ORIENTED_EDGE ( 'NONE', *, *, #16652, .F. ) ;
#861=CARTESIAN_POINT ( 'NONE',  ( 0.000000000000000000, -26.69209308833503513, -6.612652082459592684 ) ) ;
#865=DIRECTION ( 'NONE',  ( -1.000000000000000000, 0.000000000000000000, -0.000000000000000000 ) ) ;
#873=ORIENTED_EDGE ( 'NONE', *, *, #17135, .F. ) ;
#874=VERTEX_POINT ( 'NONE', #18333 ) ;
#878=AXIS2_PLACEMENT_3D ( 'NONE', #17750, #6154, #9440 ) ;
#880=VECTOR ( 'NONE', #10189, 1000.000000000000000 ) ;
#882=EDGE_LOOP ( 'NONE', ( #18404, #3005, #16371, #10437 ) ) ;
#888=FACE_OUTER_BOUND ( 'NONE', #15311, .T. ) ;
#897=VECTOR ( 'NONE', #19140, 1000.000000000000000 ) ;
#899=DIRECTION ( 'NONE',  ( -1.000000000000000000, 0.000000000000000000, 0.000000000000000000 ) ) ;
#900=DIRECTION ( 'NONE',  ( -1.000000000000000000, -0.000000000000000000, -0.000000000000000000 ) ) ;
#907=ORIENTED_EDGE ( 'NONE', *, *, #5195, .T. ) ;
#910=VERTEX_POINT ( 'NONE', #18216 ) ;
#912=AXIS2_PLACEMENT_3D ( 'NONE', #10757, #14292, #5583 ) ;
#922=DIRECTION ( 'NONE',  ( -1.000000000000000000, -0.000000000000000000, 0.000000000000000000 ) ) ;
#924=CARTESIAN_POINT ( 'NONE',  ( 5.000000000000000888, 30.61448696004452685, 9.314139153634330981 ) ) ;
#933=FILL_AREA_STYLE_COLOUR ( '', #3570 ) ;
#934=ORIENTED_EDGE ( 'NONE', *, *, #20775, .T. ) ;
#939=EDGE_CURVE ( 'NONE', #6341, #4965, #11356, .T. ) ;
#941=LINE ( 'NONE', #10997, #17560 ) ;
#944=EDGE_CURVE ( 'NONE', #4641, #10985, #19860, .T. ) ;
#951=AXIS2_PLACEMENT_3D ( 'NONE', #5313, #20121, #17241 ) ;
#954=CYLINDRICAL_SURFACE ( 'NONE', #13043, 32.00000000000000000 ) ;
#959=EDGE_LOOP ( 'NONE', ( #4249, #5076, #17336, #20807 ) ) ;
#962=AXIS2_PLACEMENT_3D ( 'NONE', #13792, #17107, #1971 ) ;
#970=CARTESIAN_POINT ( 'NONE',  ( 0.000000000000000000, -12.46320060045702860, -29.47318494484041196 ) ) ;
#973=EDGE_CURVE ( 'NONE', #839, #20292, #8403, .T. ) ;
#974=FACE_OUTER_BOUND ( 'NONE', #9117, .T. ) ;
#987=CIRCLE ( 'NONE', #16158, 32.00000000000000000 ) ;
#991=EDGE_CURVE ( 'NONE', #1185, #8085, #10864, .T. ) ;
#994=VECTOR ( 'NONE', #16575, 1000.000000000000000 ) ;
#996=ORIENTED_EDGE ( 'NONE', *, *, #14739, .T. ) ;
#1008=DIRECTION ( 'NONE',  ( 0.000000000000000000, 0.000000000000000000, 1.000000000000000000 ) ) ;
#1009=LINE ( 'NONE', #7756, #11856 ) ;
#1024=VERTEX_POINT ( 'NONE', #10668 ) ;
#1025=AXIS2_PLACEMENT_3D ( 'NONE', #11902, #6831, #15939 ) ;
#1028=AXIS2_PLACEMENT_3D ( 'NONE', #2510, #17878, #9236 ) ;
#1031=CIRCLE ( 'NONE', #19373, 27.49900000000000588 ) ;
#1039=CARTESIAN_POINT ( 'NONE',  ( 10.00000000000000000, -19.85071254963763465, -20.01672328094552356 ) ) ;
#1041=VERTEX_POINT ( 'NONE', #7374 ) ;
#1047=AXIS2_PLACEMENT_3D ( 'NONE', #19279, #18850, #611 ) ;
#1050=CARTESIAN_POINT ( 'NONE',  ( -10.00000000000000000, 0.000000000000000000, 0.000000000000000000 ) ) ;
#1056=VERTEX_POINT ( 'NONE', #6946 ) ;
#1063=CIRCLE ( 'NONE', #11989, 32.00000000000000000 ) ;
#1064=CARTESIAN_POINT ( 'NONE',  ( 0.000000000000000000, 0.000000000000000000, 0.000000000000000000 ) ) ;
#1067=DIRECTION ( 'NONE',  ( -1.000000000000000000, 0.000000000000000000, 0.000000000000000000 ) ) ;
#1068=DIRECTION ( 'NONE',  ( -1.000000000000000000, 0.000000000000000000, 0.000000000000000000 ) ) ;
#1069=ADVANCED_FACE ( 'NONE', ( #13669 ), #5707, .T. ) ;
#1070=ORIENTED_EDGE ( 'NONE', *, *, #10900, .F. ) ;
#1073=CARTESIAN_POINT ( 'NONE',  ( 0.000000000000000000, 0.000000000000000000, 0.000000000000000000 ) ) ;
#1082=CARTESIAN_POINT ( 'NONE',  ( 10.00000000000000000, 7.409634587003466777, -27.19958299168149907 ) ) ;
#1084=DIRECTION ( 'NONE',  ( 1.000000000000000000, 0.000000000000000000, 0.000000000000000000 ) ) ;
#1088=CARTESIAN_POINT ( 'NONE',  ( 10.00000000000000000, 0.000000000000000000, 0.000000000000000000 ) ) ;
#1091=CARTESIAN_POINT ( 'NONE',  ( 0.000000000000000000, 0.000000000000000000, 0.000000000000000000 ) ) ;
#1104=CARTESIAN_POINT ( 'NONE',  ( 10.00000000000000000, 1.959304526718168571, -27.42911093658673138 ) ) ;
#1107=CARTESIAN_POINT ( 'NONE',  ( -140.0000507999999968, 0.000000000000000000, 3.000000000000000444 ) ) ;
#1108=EDGE_CURVE ( 'NONE', #16260, #21189, #633, .T. ) ;
#1110=DIRECTION ( 'NONE',  ( -1.000000000000000000, 0.000000000000000000, 0.000000000000000000 ) ) ;
#1111=CARTESIAN_POINT ( 'NONE',  ( 10.00000000000000000, 12.94633825542301153, -24.26081875733320814 ) ) ;
#1121=AXIS2_PLACEMENT_3D ( 'NONE', #5058, #82, #8485 ) ;
#1123=DIRECTION ( 'NONE',  ( -1.000000000000000000, 0.000000000000000000, -0.000000000000000000 ) ) ;
#1126=DIRECTION ( 'NONE',  ( 0.000000000000000000, 0.5877852522924688072, 0.8090169943749505599 ) ) ;
#1131=ORIENTED_EDGE ( 'NONE', *, *, #11671, .T. ) ;
#1144=CARTESIAN_POINT ( 'NONE',  ( 10.00000000000000000, -23.57863763525709189, -15.45211464167688753 ) ) ;
#1151=DIRECTION ( 'NONE',  ( -1.000000000000000000, -0.000000000000000000, -0.000000000000000000 ) ) ;
#1159=ORIENTED_EDGE ( 'NONE', *, *, #13532, .T. ) ;
#1160=ORIENTED_EDGE ( 'NONE', *, *, #10270, .F. ) ;
#1169=DIRECTION ( 'NONE',  ( -1.000000000000000000, 0.000000000000000000, 0.000000000000000000 ) ) ;
#1170=DIRECTION ( 'NONE',  ( 0.000000000000000000, 0.000000000000000000, 1.000000000000000000 ) ) ;
#1183=DIRECTION ( 'NONE',  ( -1.000000000000000000, 0.000000000000000000, 0.000000000000000000 ) ) ;
#1185=VERTEX_POINT ( 'NONE', #2712 ) ;
#1186=CARTESIAN_POINT ( 'NONE',  ( 10.00000000000000000, -31.88200538760791503, -2.745493118647322817 ) ) ;
#1189=CIRCLE ( 'NONE', #9291, 11.99999999999999822 ) ;
#1191=CYLINDRICAL_SURFACE ( 'NONE', #9624, 32.00000000000000000 ) ;
#1197=DIRECTION ( 'NONE',  ( -1.000000000000000000, 0.000000000000000000, 0.000000000000000000 ) ) ;
#1198=EDGE_CURVE ( 'NONE', #16573, #10108, #16519, .T. ) ;
#1199=CARTESIAN_POINT ( 'NONE',  ( 0.000000000000000000, -27.40684453873977944, 16.51862198942000148 ) ) ;
#1200=DIRECTION ( 'NONE',  ( -1.000000000000000000, 0.000000000000000000, -0.000000000000000000 ) ) ;
#1203=CARTESIAN_POINT ( 'NONE',  ( 0.000000000000000000, 12.94633825542266869, 24.26081875733338933 ) ) ;
#1206=CIRCLE ( 'NONE', #19555, 27.49900000000000233 ) ;
#1208=ORIENTED_EDGE ( 'NONE', *, *, #14309, .T. ) ;
#1217=EDGE_CURVE ( 'NONE', #17002, #15753, #18642, .T. ) ;
#1220=CIRCLE ( 'NONE', #19573, 5.000000000000000000 ) ;
#1223=DIRECTION ( 'NONE',  ( -1.000000000000000000, -0.000000000000000000, -0.000000000000000000 ) ) ;
#1229=CARTESIAN_POINT ( 'NONE',  ( 0.000000000000000000, 0.000000000000000000, 0.000000000000000000 ) ) ;
#1232=AXIS2_PLACEMENT_3D ( 'NONE', #16450, #15113, #10025 ) ;
#1233=VERTEX_POINT ( 'NONE', #4596 ) ;
#1234=ORIENTED_EDGE ( 'NONE', *, *, #1888, .F. ) ;
#1236=EDGE_CURVE ( 'NONE', #7793, #21395, #2397, .T. ) ;
#1241=ORIENTED_EDGE ( 'NONE', *, *, #19219, .F. ) ;
#1254=FILL_AREA_STYLE_COLOUR ( '', #5512 ) ;
#1255=CARTESIAN_POINT ( 'NONE',  ( 0.000000000000000000, -14.53731623274945406, 23.34226719384900761 ) ) ;
#1259=CARTESIAN_POINT ( 'NONE',  ( 10.00000000000000000, 0.000000000000000000, 0.000000000000000000 ) ) ;
#1261=ORIENTED_EDGE ( 'NONE', *, *, #13381, .F. ) ;
#1266=AXIS2_PLACEMENT_3D ( 'NONE', #5002, #14839, #18487 ) ;
#1269=AXIS2_PLACEMENT_3D ( 'NONE', #17599, #10842, #5154 ) ;
#1279=ORIENTED_EDGE ( 'NONE', *, *, #11236, .T. ) ;
#1282=EDGE_LOOP ( 'NONE', ( #2209, #5838, #5505, #21179 ) ) ;
#1285=LINE ( 'NONE', #6711, #21381 ) ;
#1288=DIRECTION ( 'NONE',  ( 1.000000000000000000, -0.000000000000000000, -0.000000000000000000 ) ) ;
#1290=CIRCLE ( 'NONE', #19275, 11.99999999999999822 ) ;
#1295=VERTEX_POINT ( 'NONE', #21599 ) ;
#1296=DIRECTION ( 'NONE',  ( 0.000000000000000000, -0.5877852522924632561, -0.8090169943749546677 ) ) ;
#1298=CARTESIAN_POINT ( 'NONE',  ( 0.000000000000000000, -19.29292659243987984, -25.53004080487782090 ) ) ;
#1299=DIRECTION ( 'NONE',  ( 0.000000000000000000, -0.2079116908177468248, -0.9781476007338083534 ) ) ;
#1309=CARTESIAN_POINT ( 'NONE',  ( 5.000000000000000000, 23.37352460145283928, 21.85585385440887762 ) ) ;
#1310=DIRECTION ( 'NONE',  ( -1.000000000000000000, 0.000000000000000000, 0.000000000000000000 ) ) ;
#1322=EDGE_CURVE ( 'NONE', #10634, #19849, #13193, .T. ) ;
#1326=ADVANCED_FACE ( 'NONE', ( #8022, #19830 ), #14964, .F. ) ;
#1330=EDGE_LOOP ( 'NONE', ( #5862, #4662, #6873, #13438 ) ) ;
#1331=CARTESIAN_POINT ( 'NONE',  ( 10.00000000000000000, -24.17932380791732427, 20.96092317126996818 ) ) ;
#1333=AXIS2_PLACEMENT_3D ( 'NONE', #11197, #4347, #12847 ) ;
#1342=VECTOR ( 'NONE', #9120, 1000.000000000000000 ) ;
#1348=ORIENTED_EDGE ( 'NONE', *, *, #11032, .T. ) ;
#1350=VERTEX_POINT ( 'NONE', #18511 ) ;
#1357=CARTESIAN_POINT ( 'NONE',  ( 10.00000000000000000, 0.000000000000000000, 0.000000000000000000 ) ) ;
#1366=DIRECTION ( 'NONE',  ( -1.000000000000000000, 0.000000000000000000, 0.000000000000000000 ) ) ;
#1369=EDGE_CURVE ( 'NONE', #20559, #15579, #20168, .T. ) ;
#1373=EDGE_CURVE ( 'NONE', #11931, #9160, #4118, .T. ) ;
#1376=CIRCLE ( 'NONE', #324, 11.99999999999999822 ) ;
#1377=CARTESIAN_POINT ( 'NONE',  ( 10.00000000000000000, 13.56333590714055326, -28.98337314858420299 ) ) ;
#1378=CIRCLE ( 'NONE', #9127, 11.99999999999999822 ) ;
#1381=VERTEX_POINT ( 'NONE', #6915 ) ;
#1391=ORIENTED_EDGE ( 'NONE', *, *, #11842, .F. ) ;
#1397=DIRECTION ( 'NONE',  ( 0.000000000000000000, 0.7431448254773908024, 0.6691306063588620123 ) ) ;
#1399=LINE ( 'NONE', #13197, #15906 ) ;
#1402=AXIS2_PLACEMENT_3D ( 'NONE', #12323, #20831, #10446 ) ;
#1410=ORIENTED_EDGE ( 'NONE', *, *, #9707, .F. ) ;
#1414=ORIENTED_EDGE ( 'NONE', *, *, #18533, .T. ) ;
#1415=LINE ( 'NONE', #9458, #15187 ) ;
#1417=ORIENTED_EDGE ( 'NONE', *, *, #2720, .F. ) ;
#1420=ORIENTED_EDGE ( 'NONE', *, *, #15564, .F. ) ;
#1421=CARTESIAN_POINT ( 'NONE',  ( 10.00000000000000000, 19.85071254963803611, -20.01672328094512565 ) ) ;
#1426=DIRECTION ( 'NONE',  ( -1.000000000000000000, 0.000000000000000000, 0.000000000000000000 ) ) ;
#1428=EDGE_CURVE ( 'NONE', #18773, #7709, #15405, .T. ) ;
#1433=VERTEX_POINT ( 'NONE', #15288 ) ;
#1445=DIRECTION ( 'NONE',  ( -1.000000000000000000, 0.000000000000000000, 0.000000000000000000 ) ) ;
#1446=DIRECTION ( 'NONE',  ( -1.000000000000000000, 0.000000000000000000, 0.000000000000000000 ) ) ;
#1452=ORIENTED_EDGE ( 'NONE', *, *, #9538, .T. ) ;
#1454=ORIENTED_EDGE ( 'NONE', *, *, #18800, .F. ) ;
#1456=DIRECTION ( 'NONE',  ( 0.000000000000000000, -0.7431448254773999063, 0.6691306063588517983 ) ) ;
#1459=CARTESIAN_POINT ( 'NONE',  ( 10.00000000000000000, 0.000000000000000000, 0.000000000000000000 ) ) ;
#1467=CARTESIAN_POINT ( 'NONE',  ( 10.00000000000000000, 27.82509854686817263, -4.525913221810857756 ) ) ;
#1487=DIRECTION ( 'NONE',  ( -1.000000000000000000, 0.000000000000000000, 0.000000000000000000 ) ) ;
#1496=EDGE_CURVE ( 'NONE', #10884, #20540, #3691, .T. ) ;
#1498=FACE_OUTER_BOUND ( 'NONE', #4002, .T. ) ;
#1504=ORIENTED_EDGE ( 'NONE', *, *, #4914, .T. ) ;
#1506=DIRECTION ( 'NONE',  ( -1.000000000000000000, 0.000000000000000000, 0.000000000000000000 ) ) ;
#1513=CARTESIAN_POINT ( 'NONE',  ( 150.0000507999999968, 0.000000000000000000, 0.000000000000000000 ) ) ;
#1518=CARTESIAN_POINT ( 'NONE',  ( 10.00000000000000000, 9.992993448021589842, 26.36019881529889020 ) ) ;
#1519=AXIS2_PLACEMENT_3D ( 'NONE', #7177, #17128, #1988 ) ;
#1520=CIRCLE ( 'NONE', #12458, 11.99999999999999822 ) ;
#1528=EDGE_CURVE ( 'NONE', #18417, #16782, #7448, .T. ) ;
#1538=AXIS2_PLACEMENT_3D ( 'NONE', #3716, #11687, #17203 ) ;
#1543=VERTEX_POINT ( 'NONE', #16167 ) ;
#1550=DIRECTION ( 'NONE',  ( -1.000000000000000000, 0.000000000000000000, -0.000000000000000000 ) ) ;
#1552=AXIS2_PLACEMENT_3D ( 'NONE', #2014, #5226, #1800 ) ;
#1564=ORIENTED_EDGE ( 'NONE', *, *, #5961, .F. ) ;
#1566=AXIS2_PLACEMENT_3D ( 'NONE', #9885, #1487, #21390 ) ;
#1571=CARTESIAN_POINT ( 'NONE',  ( 10.00000000000000000, 0.000000000000000000, 0.000000000000000000 ) ) ;
#1572=DIRECTION ( 'NONE',  ( -1.000000000000000000, -0.000000000000000000, 0.000000000000000000 ) ) ;
#1574=SURFACE_STYLE_USAGE ( .BOTH. , #14727 ) ;
#1576=CARTESIAN_POINT ( 'NONE',  ( 10.00000000000000000, -12.90282758292962662, -25.06465718894790484 ) ) ;
#1579=AXIS2_PLACEMENT_3D ( 'NONE', #10140, #8382, #3081 ) ;
#1588=CARTESIAN_POINT ( 'NONE',  ( 10.00000000000000000, -9.366510754379408610, 25.85466064925422458 ) ) ;
#1592=VERTEX_POINT ( 'NONE', #12737 ) ;
#1595=FACE_OUTER_BOUND ( 'NONE', #6372, .T. ) ;
#1599=ORIENTED_EDGE ( 'NONE', *, *, #19434, .T. ) ;
#1601=AXIS2_PLACEMENT_3D ( 'NONE', #15817, #20790, #462 ) ;
#1611=DIRECTION ( 'NONE',  ( -1.000000000000000000, 0.000000000000000000, 0.000000000000000000 ) ) ;
#1613=CIRCLE ( 'NONE', #5156, 32.00000000000000000 ) ;
#1614=AXIS2_PLACEMENT_3D ( 'NONE', #13529, #489, #20279 ) ;
#1616=AXIS2_PLACEMENT_3D ( 'NONE', #16141, #2777, #9387 ) ;
#1619=ADVANCED_FACE ( 'NONE', ( #2570 ), #2356, .T. ) ;
#1632=DIRECTION ( 'NONE',  ( -1.000000000000000000, 0.000000000000000000, -0.000000000000000000 ) ) ;
#1636=DIRECTION ( 'NONE',  ( 0.000000000000000000, 0.000000000000000000, 1.000000000000000000 ) ) ;
#1637=AXIS2_PLACEMENT_3D ( 'NONE', #4015, #2357, #4458 ) ;
#1639=CIRCLE ( 'NONE', #4406, 27.49900000000000233 ) ;
#1642=EDGE_CURVE ( 'NONE', #11604, #21750, #15801, .T. ) ;
#1645=DIRECTION ( 'NONE',  ( -1.000000000000000000, -0.000000000000000000, 0.000000000000000000 ) ) ;
#1649=EDGE_CURVE ( 'NONE', #8568, #7280, #14510, .T. ) ;
#1652=AXIS2_PLACEMENT_3D ( 'NONE', #682, #5658, #1008 ) ;
#1658=EDGE_LOOP ( 'NONE', ( #13864, #6422, #15295, #16148 ) ) ;
#1660=DIRECTION ( 'NONE',  ( -1.000000000000000000, 0.000000000000000000, 0.000000000000000000 ) ) ;
#1663=DIRECTION ( 'NONE',  ( -1.000000000000000000, -0.000000000000000000, 0.000000000000000000 ) ) ;
#1668=CARTESIAN_POINT ( 'NONE',  ( 10.00000000000000000, -31.88200538760795766, 2.745493118646876951 ) ) ;
#1676=AXIS2_PLACEMENT_3D ( 'NONE', #9689, #2860, #6415 ) ;
#1678=EDGE_CURVE ( 'NONE', #628, #13720, #3106, .T. ) ;
#1686=VERTEX_POINT ( 'NONE', #13283 ) ;
#1691=DIRECTION ( 'NONE',  ( 0.000000000000000000, 0.000000000000000000, 1.000000000000000000 ) ) ;
#1696=AXIS2_PLACEMENT_3D ( 'NONE', #20737, #12431, #3607 ) ;
#1697=ORIENTED_EDGE ( 'NONE', *, *, #15237, .T. ) ;
#1698=VECTOR ( 'NONE', #8210, 1000.000000000000000 ) ;
#1701=DIRECTION ( 'NONE',  ( 0.000000000000000000, 0.000000000000000000, 1.000000000000000000 ) ) ;
#1702=ORIENTED_EDGE ( 'NONE', *, *, #7980, .T. ) ;
#1713=CARTESIAN_POINT ( 'NONE',  ( 10.00000000000000000, -23.37352460145267941, -21.85585385440903394 ) ) ;
#1715=ORIENTED_EDGE ( 'NONE', *, *, #11220, .T. ) ;
#1720=CARTESIAN_POINT ( 'NONE',  ( 0.000000000000000000, 1.959304526718168571, -27.42911093658673138 ) ) ;
#1722=EDGE_CURVE ( 'NONE', #16061, #7775, #7193, .T. ) ;
#1724=DIRECTION ( 'NONE',  ( -1.000000000000000000, 0.000000000000000000, -0.000000000000000000 ) ) ;
#1726=CARTESIAN_POINT ( 'NONE',  ( 0.000000000000000000, 0.000000000000000000, 0.000000000000000000 ) ) ;
#1729=EDGE_LOOP ( 'NONE', ( #5221, #16291, #20410, #6226 ) ) ;
#1730=DIRECTION ( 'NONE',  ( 1.000000000000000000, 0.000000000000000000, 0.000000000000000000 ) ) ;
#1731=FACE_OUTER_BOUND ( 'NONE', #3040, .T. ) ;
#1734=ORIENTED_EDGE ( 'NONE', *, *, #16924, .F. ) ;
#1737=CARTESIAN_POINT ( 'NONE',  ( 0.000000000000000000, -7.240962358591358061, -31.16999300804322104 ) ) ;
#1740=CARTESIAN_POINT ( 'NONE',  ( 0.000000000000000000, 0.000000000000000000, 0.000000000000000000 ) ) ;
#1746=AXIS2_PLACEMENT_3D ( 'NONE', #8270, #2756, #9478 ) ;
#1760=VECTOR ( 'NONE', #17870, 1000.000000000000000 ) ;
#1761=EDGE_LOOP ( 'NONE', ( #16780, #17714, #19772, #15246 ) ) ;
#1770=DIRECTION ( 'NONE',  ( 0.000000000000000000, 0.9510565162951544194, -0.3090169943749448422 ) ) ;
#1773=CARTESIAN_POINT ( 'NONE',  ( 10.00000000000000000, -21.69483248597433089, 16.89761061231773454 ) ) ;
#1779=ORIENTED_EDGE ( 'NONE', *, *, #21178, .T. ) ;
#1787=AXIS2_PLACEMENT_3D ( 'NONE', #19020, #15689, #3549 ) ;
#1798=CARTESIAN_POINT ( 'NONE',  ( 10.00000000000000000, -24.73395913766471921, 12.01774797440568854 ) ) ;
#1800=DIRECTION ( 'NONE',  ( 0.000000000000000000, 0.2079116908177532363, 0.9781476007338069101 ) ) ;
#1805=CARTESIAN_POINT ( 'NONE',  ( 10.00000000000000000, -1.592605004252595213, -28.14575649959895998 ) ) ;
#1814=ORIENTED_EDGE ( 'NONE', *, *, #10137, .T. ) ;
#1815=ORIENTED_EDGE ( 'NONE', *, *, #6236, .F. ) ;
#1819=LINE ( 'NONE', #16843, #13837 ) ;
#1823=DIRECTION ( 'NONE',  ( -1.000000000000000000, 0.000000000000000000, 0.000000000000000000 ) ) ;
#1824=DIRECTION ( 'NONE',  ( -1.000000000000000000, 0.000000000000000000, 0.000000000000000000 ) ) ;
#1835=FACE_OUTER_BOUND ( 'NONE', #9879, .T. ) ;
#1839=ORIENTED_EDGE ( 'NONE', *, *, #9862, .T. ) ;
#1842=DIRECTION ( 'NONE',  ( -1.000000000000000000, -0.000000000000000000, -0.000000000000000000 ) ) ;
#1849=FACE_OUTER_BOUND ( 'NONE', #12378, .T. ) ;
#1852=DIRECTION ( 'NONE',  ( -1.000000000000000000, -0.000000000000000000, -0.000000000000000000 ) ) ;
#1859=ORIENTED_EDGE ( 'NONE', *, *, #18834, .T. ) ;
#1860=DIRECTION ( 'NONE',  ( -1.000000000000000000, 0.000000000000000000, 0.000000000000000000 ) ) ;
#1868=CARTESIAN_POINT ( 'NONE',  ( 10.00000000000000000, 0.000000000000000000, -1.000000000000000000 ) ) ;
#1880=CIRCLE ( 'NONE', #1121, 32.00000000000000000 ) ;
#1882=VECTOR ( 'NONE', #9616, 1000.000000000000000 ) ;
#1886=EDGE_CURVE ( 'NONE', #11372, #569, #8748, .T. ) ;
#1888=EDGE_CURVE ( 'NONE', #7717, #19310, #987, .T. ) ;
#1892=EDGE_CURVE ( 'NONE', #2943, #17734, #12277, .T. ) ;
#1893=AXIS2_PLACEMENT_3D ( 'NONE', #12875, #19624, #5709 ) ;
#1900=AXIS2_PLACEMENT_3D ( 'NONE', #21169, #14639, #11548 ) ;
#1905=ORIENTED_EDGE ( 'NONE', *, *, #5553, .T. ) ;
#1911=DIRECTION ( 'NONE',  ( 1.000000000000000000, 0.000000000000000000, 0.000000000000000000 ) ) ;
#1912=EDGE_LOOP ( 'NONE', ( #19167, #17868, #13333, #2266 ) ) ;
#1913=AXIS2_PLACEMENT_3D ( 'NONE', #483, #4010, #17614 ) ;
#1915=ORIENTED_EDGE ( 'NONE', *, *, #5042, .T. ) ;
#1922=CIRCLE ( 'NONE', #11450, 11.99999999999999645 ) ;
#1927=CARTESIAN_POINT ( 'NONE',  ( 10.00000000000000000, -17.70753755129051754, 21.03896658273966480 ) ) ;
#1929=DIRECTION ( 'NONE',  ( -1.000000000000000000, 0.000000000000000000, 0.000000000000000000 ) ) ;
#1930=EDGE_CURVE ( 'NONE', #17767, #10255, #6654, .T. ) ;
#1931=AXIS2_PLACEMENT_3D ( 'NONE', #20709, #15847, #598 ) ;
#1934=VECTOR ( 'NONE', #7608, 1000.000000000000000 ) ;
#1935=DIRECTION ( 'NONE',  ( -1.000000000000000000, -0.000000000000000000, 0.000000000000000000 ) ) ;
#1936=FACE_OUTER_BOUND ( 'NONE', #262, .T. ) ;
#1938=ADVANCED_FACE ( 'NONE', ( #10190 ), #18597, .T. ) ;
#1941=ORIENTED_EDGE ( 'NONE', *, *, #9162, .F. ) ;
#1960=DIRECTION ( 'NONE',  ( -1.000000000000000000, 0.000000000000000000, -0.000000000000000000 ) ) ;
#1970=CARTESIAN_POINT ( 'NONE',  ( 10.00000000000000000, -27.40684453873977589, 16.51862198942000148 ) ) ;
#1971=DIRECTION ( 'NONE',  ( 0.000000000000000000, -0.9945218953682744001, 0.1045284632676436454 ) ) ;
#1978=CIRCLE ( 'NONE', #5863, 12.00000000000000178 ) ;
#1979=AXIS2_PLACEMENT_3D ( 'NONE', #11772, #13537, #16855 ) ;
#1982=CIRCLE ( 'NONE', #17160, 32.00000000000000000 ) ;
#1988=DIRECTION ( 'NONE',  ( 0.000000000000000000, 0.2079116908177599532, -0.9781476007338055778 ) ) ;
#1995=ORIENTED_EDGE ( 'NONE', *, *, #15830, .F. ) ;
#2001=DIRECTION ( 'NONE',  ( 1.000000000000000000, 0.000000000000000000, 0.000000000000000000 ) ) ;
#2004=DIRECTION ( 'NONE',  ( -1.000000000000000000, -0.000000000000000000, -0.000000000000000000 ) ) ;
#2006=AXIS2_PLACEMENT_3D ( 'NONE', #17180, #3907, #20710 ) ;
#2014=CARTESIAN_POINT ( 'NONE',  ( 0.000000000000000000, 0.000000000000000000, 0.000000000000000000 ) ) ;
#2015=DIRECTION ( 'NONE',  ( 0.000000000000000000, 0.7431448254773953543, -0.6691306063588570163 ) ) ;
#2016=DIRECTION ( 'NONE',  ( 0.000000000000000000, 0.000000000000000000, 1.000000000000000000 ) ) ;
#2021=AXIS2_PLACEMENT_3D ( 'NONE', #17760, #12442, #11235 ) ;
#2023=CARTESIAN_POINT ( 'NONE',  ( 10.00000000000000000, 12.90282758293013643, -25.06465718894764194 ) ) ;
#2024=DIRECTION ( 'NONE',  ( 0.000000000000000000, 0.000000000000000000, 1.000000000000000000 ) ) ;
#2027=VERTEX_POINT ( 'NONE', #14046 ) ;
#2035=AXIS2_PLACEMENT_3D ( 'NONE', #12161, #2004, #20784 ) ;
#2047=ADVANCED_FACE ( 'NONE', ( #888 ), #2446, .T. ) ;
#2056=LINE ( 'NONE', #7133, #12676 ) ;
#2064=ORIENTED_EDGE ( 'NONE', *, *, #19637, .T. ) ;
#2069=DIRECTION ( 'NONE',  ( -1.000000000000000000, 0.000000000000000000, -0.000000000000000000 ) ) ;
#2073=ADVANCED_FACE ( 'NONE', ( #7522 ), #681, .T. ) ;
#2076=CARTESIAN_POINT ( 'NONE',  ( 10.00000000000000000, 0.000000000000000000, 0.000000000000000000 ) ) ;
#2079=VERTEX_POINT ( 'NONE', #12598 ) ;
#2080=VECTOR ( 'NONE', #688, 1000.000000000000000 ) ;
#2088=CIRCLE ( 'NONE', #16550, 11.99999999999999822 ) ;
#2096=DIRECTION ( 'NONE',  ( 0.000000000000000000, 0.000000000000000000, -1.000000000000000000 ) ) ;
#2098=CYLINDRICAL_SURFACE ( 'NONE', #11036, 5.000000000000000000 ) ;
#2106=AXIS2_PLACEMENT_3D ( 'NONE', #12009, #10242, #8695 ) ;
#2118=ADVANCED_FACE ( 'NONE', ( #16681 ), #4428, .T. ) ;
#2121=AXIS2_PLACEMENT_3D ( 'NONE', #6254, #9422, #19715 ) ;
#2124=DIRECTION ( 'NONE',  ( -1.000000000000000000, -0.000000000000000000, 0.000000000000000000 ) ) ;
#2131=CYLINDRICAL_SURFACE ( 'NONE', #7345, 11.99999999999999645 ) ;
#2137=ORIENTED_EDGE ( 'NONE', *, *, #6250, .T. ) ;
#2138=EDGE_CURVE ( 'NONE', #14005, #6732, #14412, .T. ) ;
#2140=LINE ( 'NONE', #5675, #17098 ) ;
#2142=DIRECTION ( 'NONE',  ( 1.000000000000000000, -0.000000000000000000, -0.000000000000000000 ) ) ;
#2163=ORIENTED_EDGE ( 'NONE', *, *, #11784, .F. ) ;
#2164=ADVANCED_FACE ( 'NONE', ( #2775 ), #9596, .T. ) ;
#2165=DIRECTION ( 'NONE',  ( -1.000000000000000000, 0.000000000000000000, 0.000000000000000000 ) ) ;
#2186=EDGE_LOOP ( 'NONE', ( #8307, #13055, #12438, #12358 ) ) ;
#2198=DIRECTION ( 'NONE',  ( 0.000000000000000000, 0.9945218953682736229, -0.1045284632676503761 ) ) ;
#2200=EDGE_CURVE ( 'NONE', #17790, #1295, #9739, .T. ) ;
#2202=ADVANCED_FACE ( 'NONE', ( #21553 ), #6432, .T. ) ;
#2205=AXIS2_PLACEMENT_3D ( 'NONE', #11819, #16463, #15230 ) ;
#2208=EDGE_CURVE ( 'NONE', #4047, #20991, #7057, .T. ) ;
#2209=ORIENTED_EDGE ( 'NONE', *, *, #4224, .T. ) ;
#2213=ORIENTED_EDGE ( 'NONE', *, *, #16340, .F. ) ;
#2216=DIRECTION ( 'NONE',  ( 1.000000000000000000, -0.000000000000000000, -0.000000000000000000 ) ) ;
#2225=DIRECTION ( 'NONE',  ( -1.000000000000000000, 0.000000000000000000, 0.000000000000000000 ) ) ;
#2228=AXIS2_PLACEMENT_3D ( 'NONE', #7935, #14457, #21300 ) ;
#2229=ORIENTED_EDGE ( 'NONE', *, *, #18915, .T. ) ;
#2232=DIRECTION ( 'NONE',  ( -1.000000000000000000, -0.000000000000000000, -0.000000000000000000 ) ) ;
#2234=ORIENTED_EDGE ( 'NONE', *, *, #12389, .T. ) ;
#2236=EDGE_LOOP ( 'NONE', ( #12449, #5599, #19523, #18390 ) ) ;
#2239=DIRECTION ( 'NONE',  ( 0.000000000000000000, 0.000000000000000000, 1.000000000000000000 ) ) ;
#2242=CYLINDRICAL_SURFACE ( 'NONE', #8619, 11.99999999999999822 ) ;
#2266=ORIENTED_EDGE ( 'NONE', *, *, #6042, .T. ) ;
#2289=ADVANCED_FACE ( 'NONE', ( #7377 ), #15436, .T. ) ;
#2293=VECTOR ( 'NONE', #18270, 1000.000000000000000 ) ;
#2294=VERTEX_POINT ( 'NONE', #13879 ) ;
#2295=ORIENTED_EDGE ( 'NONE', *, *, #12743, .T. ) ;
#2297=CARTESIAN_POINT ( 'NONE',  ( 10.00000000000000000, 0.000000000000000000, 0.000000000000000000 ) ) ;
#2303=AXIS2_PLACEMENT_3D ( 'NONE', #21284, #11006, #632 ) ;
#2305=CYLINDRICAL_SURFACE ( 'NONE', #2561, 11.99999999999999822 ) ;
#2308=FACE_OUTER_BOUND ( 'NONE', #119, .T. ) ;
#2326=CARTESIAN_POINT ( 'NONE',  ( -10.00000000000000000, 0.000000000000000000, 0.000000000000000000 ) ) ;
#2330=CARTESIAN_POINT ( 'NONE',  ( 0.000000000000000000, 3.786343810537937227, -27.23708136986048700 ) ) ;
#2353=ORIENTED_EDGE ( 'NONE', *, *, #20965, .T. ) ;
#2356=CYLINDRICAL_SURFACE ( 'NONE', #9447, 27.49900000000000233 ) ;
#2357=DIRECTION ( 'NONE',  ( -1.000000000000000000, -0.000000000000000000, -0.000000000000000000 ) ) ;
#2361=DIRECTION ( 'NONE',  ( 0.000000000000000000, -0.9510565162951566398, 0.3090169943749382364 ) ) ;
#2382=EDGE_CURVE ( 'NONE', #1056, #17052, #1376, .T. ) ;
#2392=CARTESIAN_POINT ( 'NONE',  ( 10.00000000000000000, -22.77465461094683974, 15.41136296218079238 ) ) ;
#2394=AXIS2_PLACEMENT_3D ( 'NONE', #7779, #10972, #7344 ) ;
#2395=CARTESIAN_POINT ( 'NONE',  ( 10.00000000000000888, 0.000000000000000000, 3.000000000000000444 ) ) ;
#2396=AXIS2_PLACEMENT_3D ( 'NONE', #2023, #20482, #7216 ) ;
#2397=CIRCLE ( 'NONE', #8059, 32.00000000000000000 ) ;
#2398=CIRCLE ( 'NONE', #16522, 27.49900000000000233 ) ;
#2403=CARTESIAN_POINT ( 'NONE',  ( 0.000000000000000000, 0.000000000000000000, 0.000000000000000000 ) ) ;
#2408=DIRECTION ( 'NONE',  ( -1.000000000000000000, -0.000000000000000000, -0.000000000000000000 ) ) ;
#2409=ORIENTED_EDGE ( 'NONE', *, *, #21341, .F. ) ;
#2412=CARTESIAN_POINT ( 'NONE',  ( 0.000000000000000000, 7.619321854369562885, 26.42235673590693423 ) ) ;
#2416=VECTOR ( 'NONE', #16143, 1000.000000000000000 ) ;
#2420=DIRECTION ( 'NONE',  ( 0.000000000000000000, 0.000000000000000000, 1.000000000000000000 ) ) ;
#2424=FACE_OUTER_BOUND ( 'NONE', #8917, .T. ) ;
#2425=EDGE_CURVE ( 'NONE', #18297, #8691, #14429, .T. ) ;
#2429=CIRCLE ( 'NONE', #5624, 27.49900000000000233 ) ;
#2430=ORIENTED_EDGE ( 'NONE', *, *, #4064, .F. ) ;
#2433=ORIENTED_EDGE ( 'NONE', *, *, #1496, .F. ) ;
#2434=VERTEX_POINT ( 'NONE', #12989 ) ;
#2441=LINE ( 'NONE', #7421, #20982 ) ;
#2443=AXIS2_PLACEMENT_3D ( 'NONE', #20912, #5787, #17617 ) ;
#2444=EDGE_CURVE ( 'NONE', #18200, #4811, #2088, .T. ) ;
#2446=CYLINDRICAL_SURFACE ( 'NONE', #6108, 32.00000000000000000 ) ;
#2447=CIRCLE ( 'NONE', #15502, 11.99999999999999645 ) ;
#2452=FACE_OUTER_BOUND ( 'NONE', #12977, .T. ) ;
#2453=VERTEX_POINT ( 'NONE', #11327 ) ;
#2454=DIRECTION ( 'NONE',  ( 0.000000000000000000, 0.000000000000000000, 1.000000000000000000 ) ) ;
#2457=EDGE_CURVE ( 'NONE', #10255, #11426, #2604, .T. ) ;
#2463=VERTEX_POINT ( 'NONE', #15971 ) ;
#2464=EDGE_CURVE ( 'NONE', #18297, #2871, #12762, .T. ) ;
#2467=ORIENTED_EDGE ( 'NONE', *, *, #15247, .F. ) ;
#2478=CIRCLE ( 'NONE', #21187, 11.99999999999999822 ) ;
#2491=ORIENTED_EDGE ( 'NONE', *, *, #10543, .T. ) ;
#2500=CARTESIAN_POINT ( 'NONE',  ( 0.000000000000000000, 21.98203405400955290, 17.64965094506551324 ) ) ;
#2510=CARTESIAN_POINT ( 'NONE',  ( 0.000000000000000000, 0.000000000000000000, 0.000000000000000000 ) ) ;
#2511=ORIENTED_EDGE ( 'NONE', *, *, #3520, .F. ) ;
#2515=ORIENTED_EDGE ( 'NONE', *, *, #20681, .T. ) ;
#2516=DIRECTION ( 'NONE',  ( -1.000000000000000000, -0.000000000000000000, -0.000000000000000000 ) ) ;
#2518=DIRECTION ( 'NONE',  ( 0.000000000000000000, 0.000000000000000000, 1.000000000000000000 ) ) ;
#2524=CARTESIAN_POINT ( 'NONE',  ( 10.00000000000000000, -28.15804365424196121, -1.358152127006266197 ) ) ;
#2529=ORIENTED_EDGE ( 'NONE', *, *, #12233, .F. ) ;
#2531=ORIENTED_EDGE ( 'NONE', *, *, #3784, .F. ) ;
#2536=VERTEX_POINT ( 'NONE', #13533 ) ;
#2537=DIRECTION ( 'NONE',  ( -1.000000000000000000, -0.000000000000000000, -0.000000000000000000 ) ) ;
#2550=EDGE_CURVE ( 'NONE', #19310, #7770, #10222, .T. ) ;
#2551=ADVANCED_FACE ( 'NONE', ( #11560 ), #20066, .T. ) ;
#2552=DIRECTION ( 'NONE',  ( -1.000000000000000000, -0.000000000000000000, 0.000000000000000000 ) ) ;
#2561=AXIS2_PLACEMENT_3D ( 'NONE', #17012, #19004, #8609 ) ;
#2564=FACE_OUTER_BOUND ( 'NONE', #13460, .T. ) ;
#2566=EDGE_CURVE ( 'NONE', #20563, #13049, #1399, .T. ) ;
#2570=FACE_OUTER_BOUND ( 'NONE', #14308, .T. ) ;
#2573=AXIS2_PLACEMENT_3D ( 'NONE', #18937, #7338, #15508 ) ;
#2574=CARTESIAN_POINT ( 'NONE',  ( -140.0000507999999968, 0.000000000000000000, -5.000000000000000000 ) ) ;
#2577=CARTESIAN_POINT ( 'NONE',  ( 0.000000000000000000, 19.29292659244040564, -25.53004080487742300 ) ) ;
#2579=DIRECTION ( 'NONE',  ( -1.000000000000000000, -0.000000000000000000, -0.000000000000000000 ) ) ;
#2595=DIRECTION ( 'NONE',  ( 0.000000000000000000, -0.8660254037844328234, -0.5000000000000101030 ) ) ;
#2604=LINE ( 'NONE', #9226, #17915 ) ;
#2628=DIRECTION ( 'NONE',  ( -1.000000000000000000, -0.000000000000000000, -0.000000000000000000 ) ) ;
#2631=CARTESIAN_POINT ( 'NONE',  ( 10.00000000000000000, -19.07277123396555041, 19.80970465344741882 ) ) ;
#2632=CIRCLE ( 'NONE', #1579, 11.99999999999999822 ) ;
#2634=VECTOR ( 'NONE', #14339, 1000.000000000000000 ) ;
#2644=CIRCLE ( 'NONE', #15001, 12.00000000000000000 ) ;
#2648=DIRECTION ( 'NONE',  ( -1.000000000000000000, 0.000000000000000000, -0.000000000000000000 ) ) ;
#2655=DIRECTION ( 'NONE',  ( -1.000000000000000000, -0.000000000000000000, -0.000000000000000000 ) ) ;
#2663=AXIS2_PLACEMENT_3D ( 'NONE', #5561, #261, #17169 ) ;
#2666=CARTESIAN_POINT ( 'NONE',  ( 0.000000000000000000, 30.61448696004452685, 9.314139153634330981 ) ) ;
#2671=ORIENTED_EDGE ( 'NONE', *, *, #14760, .T. ) ;
#2675=CIRCLE ( 'NONE', #14318, 11.99999999999999822 ) ;
#2677=CARTESIAN_POINT ( 'NONE',  ( 10.00000000000000000, -14.53731623274912366, -23.34226719384920656 ) ) ;
#2681=DIRECTION ( 'NONE',  ( 0.000000000000000000, 0.000000000000000000, 1.000000000000000000 ) ) ;
#2683=CIRCLE ( 'NONE', #21337, 11.99999999999999822 ) ;
#2692=ORIENTED_EDGE ( 'NONE', *, *, #7676, .F. ) ;
#2699=CARTESIAN_POINT ( 'NONE',  ( 0.000000000000000000, 23.37352460145283928, 21.85585385440887762 ) ) ;
#2711=CARTESIAN_POINT ( 'NONE',  ( 10.00000000000000000, -25.17124263951000529, -12.69364185792245081 ) ) ;
#2712=CARTESIAN_POINT ( 'NONE',  ( 10.00000000000000000, 31.75612719289746266, -3.943144139962236228 ) ) ;
#2714=VECTOR ( 'NONE', #16423, 1000.000000000000000 ) ;
#2717=DIRECTION ( 'NONE',  ( -1.000000000000000000, 0.000000000000000000, 0.000000000000000000 ) ) ;
#2719=DIRECTION ( 'NONE',  ( 0.000000000000000000, 0.000000000000000000, -1.000000000000000000 ) ) ;
#2720=EDGE_CURVE ( 'NONE', #21761, #8420, #5256, .T. ) ;
#2724=EDGE_LOOP ( 'NONE', ( #20486, #7003, #4348, #21102 ) ) ;
#2741=EDGE_CURVE ( 'NONE', #19412, #16260, #18841, .T. ) ;
#2742=VERTEX_POINT ( 'NONE', #8673 ) ;
#2749=AXIS2_PLACEMENT_3D ( 'NONE', #16510, #15060, #21692 ) ;
#2750=LINE ( 'NONE', #2631, #4837 ) ;
#2756=DIRECTION ( 'NONE',  ( 1.000000000000000000, 0.000000000000000000, 0.000000000000000000 ) ) ;
#2760=ORIENTED_EDGE ( 'NONE', *, *, #7713, .T. ) ;
#2762=ORIENTED_EDGE ( 'NONE', *, *, #2720, .T. ) ;
#2765=AXIS2_PLACEMENT_3D ( 'NONE', #7765, #2552, #20803 ) ;
#2770=FACE_OUTER_BOUND ( 'NONE', #850, .T. ) ;
#2771=EDGE_LOOP ( 'NONE', ( #19821, #15, #5275, #8334 ) ) ;
#2774=CARTESIAN_POINT ( 'NONE',  ( 10.00000000000000000, 27.26034713664097353, -7.182859710736244629 ) ) ;
#2775=FACE_OUTER_BOUND ( 'NONE', #1912, .T. ) ;
#2777=DIRECTION ( 'NONE',  ( 1.000000000000000000, 0.000000000000000000, 0.000000000000000000 ) ) ;
#2779=DIRECTION ( 'NONE',  ( 0.000000000000000000, 0.000000000000000000, 1.000000000000000000 ) ) ;
#2780=AXIS2_PLACEMENT_3D ( 'NONE', #15669, #6854, #3747 ) ;
#2781=AXIS2_PLACEMENT_3D ( 'NONE', #2403, #10587, #15773 ) ;
#2793=ORIENTED_EDGE ( 'NONE', *, *, #16804, .F. ) ;
#2799=CIRCLE ( 'NONE', #663, 11.99999999999999645 ) ;
#2801=DIRECTION ( 'NONE',  ( -1.000000000000000000, -0.000000000000000000, -0.000000000000000000 ) ) ;
#2805=CARTESIAN_POINT ( 'NONE',  ( 10.00000000000000000, 0.000000000000000000, 0.000000000000000000 ) ) ;
#2807=CYLINDRICAL_SURFACE ( 'NONE', #6872, 11.99999999999999645 ) ;
#2809=CARTESIAN_POINT ( 'NONE',  ( 10.00000000000000000, -24.73395913766471921, 12.01774797440568854 ) ) ;
#2812=CARTESIAN_POINT ( 'NONE',  ( 10.00000000000000000, 0.000000000000000000, 0.000000000000000000 ) ) ;
#2831=DIRECTION ( 'NONE',  ( -1.000000000000000000, -0.000000000000000000, 0.000000000000000000 ) ) ;
#2833=ADVANCED_FACE ( 'NONE', ( #9303 ), #7454, .T. ) ;
#2837=EDGE_LOOP ( 'NONE', ( #17354, #17175, #16867, #1234 ) ) ;
#2838=CARTESIAN_POINT ( 'NONE',  ( 10.00000000000000000, 9.992993448021589842, 26.36019881529889020 ) ) ;
#2843=EDGE_CURVE ( 'NONE', #4620, #2079, #7886, .T. ) ;
#2850=VERTEX_POINT ( 'NONE', #19269 ) ;
#2853=CYLINDRICAL_SURFACE ( 'NONE', #19735, 11.99999999999999822 ) ;
#2855=CARTESIAN_POINT ( 'NONE',  ( 0.000000000000000000, 0.000000000000000000, 0.000000000000000000 ) ) ;
#2859=CARTESIAN_POINT ( 'NONE',  ( 10.00000000000000000, 19.29292659244040564, -25.53004080487741945 ) ) ;
#2860=DIRECTION ( 'NONE',  ( -1.000000000000000000, 0.000000000000000000, -0.000000000000000000 ) ) ;
#2867=EDGE_CURVE ( 'NONE', #18968, #8553, #17487, .T. ) ;
#2870=CARTESIAN_POINT ( 'NONE',  ( 10.00000000000000000, -27.26034713664092379, -7.182859710736426706 ) ) ;
#2871=VERTEX_POINT ( 'NONE', #12632 ) ;
#2873=CARTESIAN_POINT ( 'NONE',  ( 0.000000000000000000, 7.409634587003093742, 27.19958299168160565 ) ) ;
#2894=ORIENTED_EDGE ( 'NONE', *, *, #10989, .F. ) ;
#2901=AXIS2_PLACEMENT_3D ( 'NONE', #1459, #10290, #17036 ) ;
#2902=DIRECTION ( 'NONE',  ( -1.000000000000000000, 0.000000000000000000, 0.000000000000000000 ) ) ;
#2915=DIRECTION ( 'NONE',  ( -1.000000000000000000, 0.000000000000000000, 0.000000000000000000 ) ) ;
#2916=ORIENTED_EDGE ( 'NONE', *, *, #13411, .F. ) ;
#2921=ORIENTED_EDGE ( 'NONE', *, *, #6673, .F. ) ;
#2922=DIRECTION ( 'NONE',  ( 0.000000000000000000, 0.000000000000000000, 1.000000000000000000 ) ) ;
#2925=ORIENTED_EDGE ( 'NONE', *, *, #12063, .T. ) ;
#2930=LINE ( 'NONE', #9549, #21668 ) ;
#2931=DIRECTION ( 'NONE',  ( -1.000000000000000000, -0.000000000000000000, -0.000000000000000000 ) ) ;
#2937=CIRCLE ( 'NONE', #15277, 27.49900000000000233 ) ;
#2943=VERTEX_POINT ( 'NONE', #2809 ) ;
#2955=LINE ( 'NONE', #9680, #13238 ) ;
#2956=FACE_OUTER_BOUND ( 'NONE', #20735, .T. ) ;
#2966=CARTESIAN_POINT ( 'NONE',  ( 0.000000000000000000, 14.53731623274961571, -23.34226719384889748 ) ) ;
#2990=EDGE_CURVE ( 'NONE', #11426, #6341, #6194, .T. ) ;
#2994=CIRCLE ( 'NONE', #21335, 32.00000000000000000 ) ;
#3000=CYLINDRICAL_SURFACE ( 'NONE', #4260, 12.00000000000000000 ) ;
#3001=ORIENTED_EDGE ( 'NONE', *, *, #2200, .F. ) ;
#3005=ORIENTED_EDGE ( 'NONE', *, *, #17010, .F. ) ;
#3006=AXIS2_PLACEMENT_3D ( 'NONE', #15101, #10243, #11794 ) ;
#3009=ORIENTED_EDGE ( 'NONE', *, *, #842, .F. ) ;
#3013=EDGE_CURVE ( 'NONE', #15171, #3628, #2675, .T. ) ;
#3020=DIRECTION ( 'NONE',  ( -1.000000000000000000, 0.000000000000000000, 0.000000000000000000 ) ) ;
#3039=ORIENTED_EDGE ( 'NONE', *, *, #16740, .F. ) ;
#3040=EDGE_LOOP ( 'NONE', ( #15423, #1417, #15958, #16737 ) ) ;
#3043=EDGE_LOOP ( 'NONE', ( #18237, #16756, #16895, #13114 ) ) ;
#3049=CARTESIAN_POINT ( 'NONE',  ( 0.000000000000000000, 0.000000000000000000, 0.000000000000000000 ) ) ;
#3055=FACE_OUTER_BOUND ( 'NONE', #11175, .T. ) ;
#3060=DIRECTION ( 'NONE',  ( -1.000000000000000000, 0.000000000000000000, 0.000000000000000000 ) ) ;
#3070=FACE_OUTER_BOUND ( 'NONE', #2236, .T. ) ;
#3074=DIRECTION ( 'NONE',  ( -1.000000000000000000, -0.000000000000000000, 0.000000000000000000 ) ) ;
#3076=LINE ( 'NONE', #16561, #8043 ) ;
#3081=DIRECTION ( 'NONE',  ( 0.000000000000000000, 0.7431448254773954654, -0.6691306063588569053 ) ) ;
#3089=EDGE_CURVE ( 'NONE', #10281, #7717, #13288, .T. ) ;
#3092=AXIS2_PLACEMENT_3D ( 'NONE', #19431, #12690, #2198 ) ;
#3096=FACE_BOUND ( 'NONE', #14025, .T. ) ;
#3100=CARTESIAN_POINT ( 'NONE',  ( 10.00000000000000000, 1.592605004252791279, 28.14575649959894932 ) ) ;
#3106=CIRCLE ( 'NONE', #11585, 11.99999999999999822 ) ;
#3110=EDGE_CURVE ( 'NONE', #21233, #12524, #11845, .T. ) ;
#3113=ADVANCED_FACE ( 'NONE', ( #17370 ), #15263, .T. ) ;
#3116=ORIENTED_EDGE ( 'NONE', *, *, #1649, .T. ) ;
#3117=DIRECTION ( 'NONE',  ( -1.000000000000000000, 0.000000000000000000, -0.000000000000000000 ) ) ;
#3118=EDGE_CURVE ( 'NONE', #4988, #11544, #9714, .T. ) ;
#3120=LINE ( 'NONE', #432, #2293 ) ;
#3122=VECTOR ( 'NONE', #2648, 1000.000000000000000 ) ;
#3123=FACE_OUTER_BOUND ( 'NONE', #9898, .T. ) ;
#3127=AXIS2_PLACEMENT_3D ( 'NONE', #6540, #19786, #11378 ) ;
#3134=EDGE_CURVE ( 'NONE', #16531, #5051, #6535, .T. ) ;
#3142=AXIS2_PLACEMENT_3D ( 'NONE', #9155, #3868, #5966 ) ;
#3144=ORIENTED_EDGE ( 'NONE', *, *, #8827, .T. ) ;
#3148=ORIENTED_EDGE ( 'NONE', *, *, #17662, .F. ) ;
#3153=CARTESIAN_POINT ( 'NONE',  ( 0.000000000000000000, 0.000000000000000000, 0.000000000000000000 ) ) ;
#3168=EDGE_CURVE ( 'NONE', #14063, #16061, #15497, .T. ) ;
#3171=EDGE_LOOP ( 'NONE', ( #8883, #4615, #2916, #1414 ) ) ;
#3172=CYLINDRICAL_SURFACE ( 'NONE', #7394, 11.99999999999999822 ) ;
#3180=VECTOR ( 'NONE', #18844, 1000.000000000000000 ) ;
#3183=CARTESIAN_POINT ( 'NONE',  ( 10.00000000000000000, 27.26034713664087406, 7.182859710736605230 ) ) ;
#3189=DIRECTION ( 'NONE',  ( 1.000000000000000000, 0.000000000000000000, -0.000000000000000000 ) ) ;
#3190=CARTESIAN_POINT ( 'NONE',  ( 10.00000000000000000, -21.69483248597433089, 16.89761061231773454 ) ) ;
#3193=ORIENTED_EDGE ( 'NONE', *, *, #20460, .T. ) ;
#3197=EDGE_LOOP ( 'NONE', ( #5402, #15087, #15019, #15960 ) ) ;
#3198=CARTESIAN_POINT ( 'NONE',  ( 10.00000000000000000, 9.366510754379572035, -25.85466064925416774 ) ) ;
#3199=EDGE_LOOP ( 'NONE', ( #12894, #19274, #1452, #20814 ) ) ;
#3219=ORIENTED_EDGE ( 'NONE', *, *, #6093, .F. ) ;
#3223=LINE ( 'NONE', #15670, #21691 ) ;
#3224=CARTESIAN_POINT ( 'NONE',  ( 5.000000000000000000, 30.24235385705238244, 10.45944707835118237 ) ) ;
#3231=DIRECTION ( 'NONE',  ( 0.000000000000000000, -0.5877852522924631451, -0.8090169943749545567 ) ) ;
#3236=ORIENTED_EDGE ( 'NONE', *, *, #16937, .F. ) ;
#3237=ADVANCED_FACE ( 'NONE', ( #12280 ), #21227, .T. ) ;
#3242=LINE ( 'NONE', #21695, #11124 ) ;
#3243=EDGE_LOOP ( 'NONE', ( #3144, #8652, #14945, #7704 ) ) ;
#3258=CARTESIAN_POINT ( 'NONE',  ( 0.000000000000000000, -3.786343810537759147, 27.23708136986050832 ) ) ;
#3264=CARTESIAN_POINT ( 'NONE',  ( 10.00000000000000000, -21.98203405400942856, -17.64965094506566246 ) ) ;
#3273=CARTESIAN_POINT ( 'NONE',  ( 0.000000000000000000, 0.000000000000000000, 0.000000000000000000 ) ) ;
#3276=CIRCLE ( 'NONE', #13141, 32.00000000000000000 ) ;
#3279=ORIENTED_EDGE ( 'NONE', *, *, #20460, .F. ) ;
#3283=VERTEX_POINT ( 'NONE', #14258 ) ;
#3284=LINE ( 'NONE', #1309, #9849 ) ;
#3286=CARTESIAN_POINT ( 'NONE',  ( 10.00000000000000000, 25.48117629651203941, -10.33947075754235989 ) ) ;
#3289=ADVANCED_FACE ( 'NONE', ( #4432 ), #14490, .T. ) ;
#3292=AXIS2_PLACEMENT_3D ( 'NONE', #21415, #16111, #12682 ) ;
#3299=CARTESIAN_POINT ( 'NONE',  ( 10.00000000000000000, -6.063030049134860100, -31.42037024962131397 ) ) ;
#3302=CARTESIAN_POINT ( 'NONE',  ( 5.000000000000000888, 28.00896854772013000, -15.47571261340895887 ) ) ;
#3303=ORIENTED_EDGE ( 'NONE', *, *, #19060, .F. ) ;
#3304=DIRECTION ( 'NONE',  ( 0.000000000000000000, -0.4067366430758070917, 0.9135454576425978690 ) ) ;
#3315=DIRECTION ( 'NONE',  ( 0.000000000000000000, 0.2079116908177532919, 0.9781476007338070211 ) ) ;
#3319=ORIENTED_EDGE ( 'NONE', *, *, #7155, .T. ) ;
#3329=ORIENTED_EDGE ( 'NONE', *, *, #9020, .T. ) ;
#3332=CARTESIAN_POINT ( 'NONE',  ( 10.00000000000000000, 23.57863763525741874, -15.45211464167639548 ) ) ;
#3334=EDGE_CURVE ( 'NONE', #6248, #18295, #19351, .T. ) ;
#3345=VECTOR ( 'NONE', #18229, 1000.000000000000000 ) ;
#3354=ORIENTED_EDGE ( 'NONE', *, *, #9862, .F. ) ;
#3356=EDGE_LOOP ( 'NONE', ( #14008, #18777, #18066, #17907 ) ) ;
#3366=CIRCLE ( 'NONE', #10408, 27.49900000000000588 ) ;
#3367=DIRECTION ( 'NONE',  ( -1.000000000000000000, 0.000000000000000000, 0.000000000000000000 ) ) ;
#3368=CARTESIAN_POINT ( 'NONE',  ( 0.000000000000000000, 0.000000000000000000, 0.000000000000000000 ) ) ;
#3372=CARTESIAN_POINT ( 'NONE',  ( 5.000000000000000888, 7.240962358591573889, 31.16999300804317130 ) ) ;
#3374=EDGE_LOOP ( 'NONE', ( #8969, #10841, #7132, #19223, #12207, #12919, #20490, #3421, #2793, #6559, #6553, #20813, #11033, #69, #10042, #2692, #3039, #15723, #15870, #18021, #6426, #4324, #6587, #266, #3745, #1261, #7596, #15067, #4578, #1410, #13434, #2511, #17413, #5644, #21082, #16794, #18903, #6060, #1391, #19828, #17230, #20859, #15015, #13319, #17120, #4446, #14159, #2430, #10280, #16279, #11122, #13524, #5559, #6472, #19722, #1160, #13205, #10003, #21548, #10058, #3594, #5403, #14502, #11179, #1941, #15392, #17303, #2529, #5193, #5236, #11106, #9376, #20906, #9254, #1815, #5324, #11722, #17087, #5885, #14492, #19873, #17446, #13870, #17770, #4353, #3009, #14165, #8364, #4855, #13484, #14296, #9483, #582, #6312, #11857, #186, #13485, #12726, #9145, #15041, #296, #2467, #11132, #11068, #5102, #5625, #3001, #13030, #18015, #12537, #15363, #5164, #4334, #12638, #18939, #15842, #11091, #8196, #12231, #3879, #2531, #8498, #13919, #7541, #12816 ) ) ;
#3375=CARTESIAN_POINT ( 'NONE',  ( 0.000000000000000000, -22.77465461094663368, -15.41136296218110147 ) ) ;
#3378=EDGE_LOOP ( 'NONE', ( #7901, #14842, #51, #18970 ) ) ;
#3380=CIRCLE ( 'NONE', #5157, 27.49900000000000233 ) ;
#3383=AXIS2_PLACEMENT_3D ( 'NONE', #12489, #19033, #3889 ) ;
#3385=DIRECTION ( 'NONE',  ( 0.000000000000000000, -0.2079116908177468248, -0.9781476007338083534 ) ) ;
#3386=CARTESIAN_POINT ( 'NONE',  ( 10.00000000000000000, 0.000000000000000000, 0.000000000000000000 ) ) ;
#3387=VERTEX_POINT ( 'NONE', #15922 ) ;
#3399=DIRECTION ( 'NONE',  ( 0.000000000000000000, 0.5877852522924741363, -0.8090169943749466741 ) ) ;
#3409=EDGE_CURVE ( 'NONE', #16206, #4982, #19893, .T. ) ;
#3410=CARTESIAN_POINT ( 'NONE',  ( 5.000000000000000000, -27.40684453873977944, 16.51862198942000148 ) ) ;
#3414=VECTOR ( 'NONE', #6743, 1000.000000000000000 ) ;
#3417=VECTOR ( 'NONE', #19348, 1000.000000000000000 ) ;
#3421=ORIENTED_EDGE ( 'NONE', *, *, #16613, .F. ) ;
#3428=FACE_OUTER_BOUND ( 'NONE', #17603, .T. ) ;
#3429=AXIS2_PLACEMENT_3D ( 'NONE', #2838, #19303, #20958 ) ;
#3438=EDGE_LOOP ( 'NONE', ( #12551, #6391, #3602, #14766 ) ) ;
#3439=EDGE_CURVE ( 'NONE', #3621, #16306, #6434, .T. ) ;
#3440=VERTEX_POINT ( 'NONE', #20123 ) ;
#3454=DIRECTION ( 'NONE',  ( -1.000000000000000000, -0.000000000000000000, -0.000000000000000000 ) ) ;
#3456=CARTESIAN_POINT ( 'NONE',  ( 0.000000000000000000, 28.15804365424197186, -1.358152127006073684 ) ) ;
#3458=CYLINDRICAL_SURFACE ( 'NONE', #7724, 32.00000000000000000 ) ;
#3492=ORIENTED_EDGE ( 'NONE', *, *, #12062, .T. ) ;
#3494=DIRECTION ( 'NONE',  ( 0.000000000000000000, 0.000000000000000000, -1.000000000000000000 ) ) ;
#3495=ORIENTED_EDGE ( 'NONE', *, *, #21273, .T. ) ;
#3496=CARTESIAN_POINT ( 'NONE',  ( 10.00000000000000000, 0.000000000000000000, 0.000000000000000000 ) ) ;
#3497=DIRECTION ( 'NONE',  ( 0.000000000000000000, 0.000000000000000000, -1.000000000000000000 ) ) ;
#3498=ORIENTED_EDGE ( 'NONE', *, *, #6387, .F. ) ;
#3501=ORIENTED_EDGE ( 'NONE', *, *, #16648, .T. ) ;
#3515=CARTESIAN_POINT ( 'NONE',  ( 0.000000000000000000, 0.000000000000000000, 0.000000000000000000 ) ) ;
#3517=DIRECTION ( 'NONE',  ( 1.000000000000000000, 0.000000000000000000, 0.000000000000000000 ) ) ;
#3519=ADVANCED_FACE ( 'NONE', ( #9715 ), #14816, .T. ) ;
#3520=EDGE_CURVE ( 'NONE', #15608, #6772, #14354, .T. ) ;
#3521=CARTESIAN_POINT ( 'NONE',  ( 0.000000000000000000, 0.000000000000000000, 0.000000000000000000 ) ) ;
#3540=DIRECTION ( 'NONE',  ( -1.000000000000000000, -0.000000000000000000, -0.000000000000000000 ) ) ;
#3541=VECTOR ( 'NONE', #4443, 1000.000000000000000 ) ;
#3542=CARTESIAN_POINT ( 'NONE',  ( 10.00000000000000000, 27.26034713664097353, -7.182859710736244629 ) ) ;
#3547=ORIENTED_EDGE ( 'NONE', *, *, #18928, .T. ) ;
#3548=ORIENTED_EDGE ( 'NONE', *, *, #10020, .F. ) ;
#3549=DIRECTION ( 'NONE',  ( 0.000000000000000000, 0.000000000000000000, -1.000000000000000000 ) ) ;
#3550=VERTEX_POINT ( 'NONE', #1668 ) ;
#3551=CIRCLE ( 'NONE', #20497, 11.99999999999999822 ) ;
#3555=PRODUCT_CONTEXT ( 'NONE', #17866, 'mechanical' ) ;
#3556=EDGE_CURVE ( 'NONE', #11575, #9822, #5317, .T. ) ;
#3558=ORIENTED_EDGE ( 'NONE', *, *, #7628, .F. ) ;
#3567=CARTESIAN_POINT ( 'NONE',  ( 10.00000000000000000, -31.75612719289738095, -3.943144139962873940 ) ) ;
#3569=CARTESIAN_POINT ( 'NONE',  ( 0.000000000000000000, -6.063030049135288202, 31.42037024962122871 ) ) ;
#3570=COLOUR_RGB ( '', 0.40784314, 0.44705882, 0.49803922) ;
#3572=DIRECTION ( 'NONE',  ( 0.000000000000000000, 0.000000000000000000, 1.000000000000000000 ) ) ;
#3591=VERTEX_POINT ( 'NONE', #15236 ) ;
#3593=DIRECTION ( 'NONE',  ( 0.000000000000000000, 0.000000000000000000, 1.000000000000000000 ) ) ;
#3594=ORIENTED_EDGE ( 'NONE', *, *, #12454, .F. ) ;
#3602=ORIENTED_EDGE ( 'NONE', *, *, #7155, .F. ) ;
#3604=ORIENTED_EDGE ( 'NONE', *, *, #10789, .F. ) ;
#3607=DIRECTION ( 'NONE',  ( 0.000000000000000000, -0.2079116908177469081, -0.9781476007338083534 ) ) ;
#3616=FACE_OUTER_BOUND ( 'NONE', #1282, .T. ) ;
#3620=DIRECTION ( 'NONE',  ( 0.000000000000000000, 0.000000000000000000, -1.000000000000000000 ) ) ;
#3621=VERTEX_POINT ( 'NONE', #229 ) ;
#3628=VERTEX_POINT ( 'NONE', #3754 ) ;
#3636=VECTOR ( 'NONE', #14719, 1000.000000000000000 ) ;
#3639=DIRECTION ( 'NONE',  ( -1.000000000000000000, -0.000000000000000000, -0.000000000000000000 ) ) ;
#3645=EDGE_CURVE ( 'NONE', #2453, #10528, #255, .T. ) ;
#3658=ADVANCED_FACE ( 'NONE', ( #5523 ), #12255, .T. ) ;
#3661=CIRCLE ( 'NONE', #5437, 11.99999999999999822 ) ;
#3664=CARTESIAN_POINT ( 'NONE',  ( -10.00000000000000000, 0.000000000000000000, 0.000000000000000000 ) ) ;
#3667=DIRECTION ( 'NONE',  ( 0.000000000000000000, 0.4067366430758008744, -0.9135454576426006446 ) ) ;
#3691=LINE ( 'NONE', #10538, #9094 ) ;
#3694=AXIS2_PLACEMENT_3D ( 'NONE', #19034, #11854, #5227 ) ;
#3699=DIRECTION ( 'NONE',  ( -1.000000000000000000, 0.000000000000000000, 0.000000000000000000 ) ) ;
#3708=VERTEX_POINT ( 'NONE', #5637 ) ;
#3716=CARTESIAN_POINT ( 'NONE',  ( 10.00000000000000000, 28.15804365424195765, 1.358152127006451826 ) ) ;
#3718=ORIENTED_EDGE ( 'NONE', *, *, #11950, .T. ) ;
#3723=VECTOR ( 'NONE', #6474, 1000.000000000000000 ) ;
#3726=CYLINDRICAL_SURFACE ( 'NONE', #7671, 11.99999999999999822 ) ;
#3728=FACE_OUTER_BOUND ( 'NONE', #5127, .T. ) ;
#3741=EDGE_LOOP ( 'NONE', ( #19875, #14357, #8100, #6667 ) ) ;
#3745=ORIENTED_EDGE ( 'NONE', *, *, #2425, .F. ) ;
#3747=DIRECTION ( 'NONE',  ( 0.000000000000000000, 0.000000000000000000, 1.000000000000000000 ) ) ;
#3753=DIRECTION ( 'NONE',  ( 0.000000000000000000, -0.5877852522924797984, 0.8090169943749426773 ) ) ;
#3754=CARTESIAN_POINT ( 'NONE',  ( 10.00000000000000000, -21.69483248597410707, -16.89761061231802586 ) ) ;
#3767=EDGE_CURVE ( 'NONE', #13692, #11651, #10925, .T. ) ;
#3769=AXIS2_PLACEMENT_3D ( 'NONE', #11283, #1445, #13258 ) ;
#3771=ORIENTED_EDGE ( 'NONE', *, *, #1108, .F. ) ;
#3774=EDGE_CURVE ( 'NONE', #6248, #16691, #4500, .T. ) ;
#3784=EDGE_CURVE ( 'NONE', #14878, #10281, #20729, .T. ) ;
#3788=CARTESIAN_POINT ( 'NONE',  ( 10.00000000000000000, 7.409634587003093742, 27.19958299168160565 ) ) ;
#3791=EDGE_LOOP ( 'NONE', ( #6911, #9614, #12618, #20334 ) ) ;
#3796=ORIENTED_EDGE ( 'NONE', *, *, #4354, .T. ) ;
#3798=LINE ( 'NONE', #7018, #16310 ) ;
#3799=ADVANCED_FACE ( 'NONE', ( #14023 ), #20770, .F. ) ;
#3800=CIRCLE ( 'NONE', #16146, 27.49900000000000233 ) ;
#3808=DIRECTION ( 'NONE',  ( -1.000000000000000000, 0.000000000000000000, 0.000000000000000000 ) ) ;
#3818=EDGE_CURVE ( 'NONE', #8125, #21757, #11198, .T. ) ;
#3827=VERTEX_POINT ( 'NONE', #1199 ) ;
#3835=CARTESIAN_POINT ( 'NONE',  ( -10.00000000000000000, 0.000000000000000000, 0.000000000000000000 ) ) ;
#3839=CYLINDRICAL_SURFACE ( 'NONE', #6126, 11.99999999999999822 ) ;
#3842=ORIENTED_EDGE ( 'NONE', *, *, #1649, .F. ) ;
#3861=CARTESIAN_POINT ( 'NONE',  ( 0.000000000000000000, -26.27606311335958011, 10.21217444509402661 ) ) ;
#3865=CARTESIAN_POINT ( 'NONE',  ( 10.00000000000000000, -31.75612719289743779, 3.943144139962448058 ) ) ;
#3868=DIRECTION ( 'NONE',  ( -1.000000000000000000, -0.000000000000000000, -0.000000000000000000 ) ) ;
#3879=ORIENTED_EDGE ( 'NONE', *, *, #4229, .F. ) ;
#3884=CYLINDRICAL_SURFACE ( 'NONE', #7496, 27.49900000000000233 ) ;
#3888=LINE ( 'NONE', #10727, #3417 ) ;
#3889=DIRECTION ( 'NONE',  ( 0.000000000000000000, 0.000000000000000000, 1.000000000000000000 ) ) ;
#3907=DIRECTION ( 'NONE',  ( -1.000000000000000000, 0.000000000000000000, -0.000000000000000000 ) ) ;
#3921=CARTESIAN_POINT ( 'NONE',  ( 0.000000000000000000, 0.000000000000000000, 0.000000000000000000 ) ) ;
#3922=ADVANCED_FACE ( 'NONE', ( #4036 ), #9435, .T. ) ;
#3946=DIRECTION ( 'NONE',  ( -1.000000000000000000, -0.000000000000000000, -0.000000000000000000 ) ) ;
#3951=CARTESIAN_POINT ( 'NONE',  ( 0.000000000000000000, -19.85071254963791176, 20.01672328094525000 ) ) ;
#3953=ORIENTED_EDGE ( 'NONE', *, *, #13959, .F. ) ;
#3956=EDGE_CURVE ( 'NONE', #6083, #771, #941, .T. ) ;
#3957=FACE_OUTER_BOUND ( 'NONE', #2771, .T. ) ;
#3960=DIRECTION ( 'NONE',  ( 1.000000000000000000, 0.000000000000000000, 0.000000000000000000 ) ) ;
#3965=LINE ( 'NONE', #10699, #11739 ) ;
#3973=CARTESIAN_POINT ( 'NONE',  ( 10.00000000000000000, 0.000000000000000000, 0.000000000000000000 ) ) ;
#3980=ORIENTED_EDGE ( 'NONE', *, *, #13439, .F. ) ;
#3988=CIRCLE ( 'NONE', #17766, 11.99999999999999822 ) ;
#3989=DIRECTION ( 'NONE',  ( -1.000000000000000000, 0.000000000000000000, 0.000000000000000000 ) ) ;
#3994=DIRECTION ( 'NONE',  ( 0.000000000000000000, 0.000000000000000000, 1.000000000000000000 ) ) ;
#4002=EDGE_LOOP ( 'NONE', ( #12148, #789, #19935, #6591 ) ) ;
#4003=EDGE_CURVE ( 'NONE', #19412, #13513, #3800, .T. ) ;
#4010=DIRECTION ( 'NONE',  ( -1.000000000000000000, -0.000000000000000000, -0.000000000000000000 ) ) ;
#4015=CARTESIAN_POINT ( 'NONE',  ( 10.00000000000000000, 0.000000000000000000, 0.000000000000000000 ) ) ;
#4024=ORIENTED_EDGE ( 'NONE', *, *, #17683, .T. ) ;
#4036=FACE_OUTER_BOUND ( 'NONE', #13707, .T. ) ;
#4047=VERTEX_POINT ( 'NONE', #20944 ) ;
#4048=DIRECTION ( 'NONE',  ( 1.000000000000000000, -0.000000000000000000, 0.000000000000000000 ) ) ;
#4050=CYLINDRICAL_SURFACE ( 'NONE', #6907, 12.00000000000000000 ) ;
#4052=VECTOR ( 'NONE', #11459, 1000.000000000000000 ) ;
#4054=CIRCLE ( 'NONE', #14289, 11.99999999999999822 ) ;
#4056=EDGE_CURVE ( 'NONE', #6639, #9318, #17219, .T. ) ;
#4058=EDGE_CURVE ( 'NONE', #11265, #3283, #11217, .T. ) ;
#4061=DIRECTION ( 'NONE',  ( 1.000000000000000000, -0.000000000000000000, -0.000000000000000000 ) ) ;
#4064=EDGE_CURVE ( 'NONE', #20840, #7792, #10154, .T. ) ;
#4073=AXIS2_PLACEMENT_3D ( 'NONE', #7700, #11121, #15883 ) ;
#4077=EDGE_CURVE ( 'NONE', #7508, #13187, #6563, .T. ) ;
#4087=AXIS2_PLACEMENT_3D ( 'NONE', #15709, #6997, #2015 ) ;
#4095=CIRCLE ( 'NONE', #12906, 27.49900000000000233 ) ;
#4099=LINE ( 'NONE', #1104, #3122 ) ;
#4101=CARTESIAN_POINT ( 'NONE',  ( 10.00000000000000000, 24.17932380791747349, -20.96092317126980831 ) ) ;
#4107=ADVANCED_FACE ( 'NONE', ( #129 ), #20028, .T. ) ;
#4118=CIRCLE ( 'NONE', #19290, 32.00000000000000000 ) ;
#4129=CARTESIAN_POINT ( 'NONE',  ( 0.000000000000000000, 0.000000000000000000, 0.000000000000000000 ) ) ;
#4130=CARTESIAN_POINT ( 'NONE',  ( 5.000000000000000000, 13.56333590714055681, -28.98337314858420299 ) ) ;
#4135=CARTESIAN_POINT ( 'NONE',  ( 10.00000000000000000, 27.26034713664097353, -7.182859710736244629 ) ) ;
#4137=CIRCLE ( 'NONE', #962, 27.49900000000000233 ) ;
#4141=ORIENTED_EDGE ( 'NONE', *, *, #20775, .F. ) ;
#4143=ORIENTED_EDGE ( 'NONE', *, *, #9428, .T. ) ;
#4144=CARTESIAN_POINT ( 'NONE',  ( 0.000000000000000000, -4.294029059349679045, -27.86182539015970505 ) ) ;
#4149=ORIENTED_EDGE ( 'NONE', *, *, #7188, .T. ) ;
#4153=DIRECTION ( 'NONE',  ( -1.000000000000000000, 0.000000000000000000, 0.000000000000000000 ) ) ;
#4158=DIRECTION ( 'NONE',  ( 0.000000000000000000, 0.000000000000000000, 1.000000000000000000 ) ) ;
#4160=DIRECTION ( 'NONE',  ( -1.000000000000000000, 0.000000000000000000, 0.000000000000000000 ) ) ;
#4165=CARTESIAN_POINT ( 'NONE',  ( 10.00000000000000000, 25.17124263951009411, -12.69364185792227495 ) ) ;
#4174=DIRECTION ( 'NONE',  ( 0.000000000000000000, 0.000000000000000000, -1.000000000000000000 ) ) ;
#4177=ORIENTED_EDGE ( 'NONE', *, *, #16896, .F. ) ;
#4179=ORIENTED_EDGE ( 'NONE', *, *, #6665, .T. ) ;
#4183=DIRECTION ( 'NONE',  ( -1.000000000000000000, 0.000000000000000000, 0.000000000000000000 ) ) ;
#4184=VECTOR ( 'NONE', #4061, 1000.000000000000000 ) ;
#4185=CIRCLE ( 'NONE', #18318, 11.99999999999999645 ) ;
#4189=EDGE_CURVE ( 'NONE', #5507, #839, #15254, .T. ) ;
#4206=EDGE_CURVE ( 'NONE', #771, #21218, #5229, .T. ) ;
#4207=DIRECTION ( 'NONE',  ( 0.000000000000000000, 0.000000000000000000, 1.000000000000000000 ) ) ;
#4217=CYLINDRICAL_SURFACE ( 'NONE', #14326, 27.49900000000000233 ) ;
#4220=ADVANCED_FACE ( 'NONE', ( #6775 ), #18914, .T. ) ;
#4224=EDGE_CURVE ( 'NONE', #3550, #21750, #9060, .T. ) ;
#4226=ORIENTED_EDGE ( 'NONE', *, *, #18289, .F. ) ;
#4229=EDGE_CURVE ( 'NONE', #10281, #7770, #21091, .T. ) ;
#4230=AXIS2_PLACEMENT_3D ( 'NONE', #14436, #1067, #19741 ) ;
#4234=ORIENTED_EDGE ( 'NONE', *, *, #19701, .T. ) ;
#4249=ORIENTED_EDGE ( 'NONE', *, *, #16050, .T. ) ;
#4250=CARTESIAN_POINT ( 'NONE',  ( 10.00000000000000000, 0.000000000000000000, 0.000000000000000000 ) ) ;
#4252=DIRECTION ( 'NONE',  ( -1.000000000000000000, 0.000000000000000000, 0.000000000000000000 ) ) ;
#4260=AXIS2_PLACEMENT_3D ( 'NONE', #16811, #6555, #10179 ) ;
#4267=CARTESIAN_POINT ( 'NONE',  ( 0.000000000000000000, -12.46320060045744071, 29.47318494484024853 ) ) ;
#4282=ORIENTED_EDGE ( 'NONE', *, *, #15080, .T. ) ;
#4283=CYLINDRICAL_SURFACE ( 'NONE', #13723, 11.99999999999999822 ) ;
#4285=DIRECTION ( 'NONE',  ( -1.000000000000000000, -0.000000000000000000, -0.000000000000000000 ) ) ;
#4287=CARTESIAN_POINT ( 'NONE',  ( 10.00000000000000000, -26.69209308833503513, -6.612652082459592684 ) ) ;
#4295=ORIENTED_EDGE ( 'NONE', *, *, #8354, .T. ) ;
#4307=FACE_OUTER_BOUND ( 'NONE', #7904, .T. ) ;
#4314=DIRECTION ( 'NONE',  ( -1.000000000000000000, -0.000000000000000000, -0.000000000000000000 ) ) ;
#4316=VERTEX_POINT ( 'NONE', #7310 ) ;
#4318=DIRECTION ( 'NONE',  ( 0.000000000000000000, 0.000000000000000000, 1.000000000000000000 ) ) ;
#4319=ORIENTED_EDGE ( 'NONE', *, *, #18289, .T. ) ;
#4320=CIRCLE ( 'NONE', #16314, 27.49900000000000588 ) ;
#4321=FACE_OUTER_BOUND ( 'NONE', #3378, .T. ) ;
#4324=ORIENTED_EDGE ( 'NONE', *, *, #21635, .F. ) ;
#4331=LINE ( 'NONE', #16374, #3636 ) ;
#4332=EDGE_CURVE ( 'NONE', #2463, #16061, #7100, .T. ) ;
#4334=ORIENTED_EDGE ( 'NONE', *, *, #14960, .F. ) ;
#4337=LINE ( 'NONE', #17940, #19039 ) ;
#4341=DIRECTION ( 'NONE',  ( -1.000000000000000000, 0.000000000000000000, -0.000000000000000000 ) ) ;
#4346=EDGE_CURVE ( 'NONE', #17286, #16668, #12377, .T. ) ;
#4347=DIRECTION ( 'NONE',  ( -1.000000000000000000, -0.000000000000000000, 0.000000000000000000 ) ) ;
#4348=ORIENTED_EDGE ( 'NONE', *, *, #18814, .T. ) ;
#4353=ORIENTED_EDGE ( 'NONE', *, *, #14178, .F. ) ;
#4354=EDGE_CURVE ( 'NONE', #21233, #11274, #4099, .T. ) ;
#4358=CYLINDRICAL_SURFACE ( 'NONE', #17629, 27.49900000000000233 ) ;
#4361=SURFACE_SIDE_STYLE ('',( #6370 ) ) ;
#4373=DIRECTION ( 'NONE',  ( 1.000000000000000000, -0.000000000000000000, 0.000000000000000000 ) ) ;
#4376=CIRCLE ( 'NONE', #13897, 12.00000000000000178 ) ;
#4385=ORIENTED_EDGE ( 'NONE', *, *, #8949, .F. ) ;
#4391=AXIS2_PLACEMENT_3D ( 'NONE', #13090, #7799, #14757 ) ;
#4393=ORIENTED_EDGE ( 'NONE', *, *, #20113, .T. ) ;
#4402=DIRECTION ( 'NONE',  ( 0.000000000000000000, 0.000000000000000000, 1.000000000000000000 ) ) ;
#4406=AXIS2_PLACEMENT_3D ( 'NONE', #20312, #19553, #11583 ) ;
#4409=AXIS2_PLACEMENT_3D ( 'NONE', #11983, #15514, #6804 ) ;
#4411=DIRECTION ( 'NONE',  ( 0.000000000000000000, 0.000000000000000000, 1.000000000000000000 ) ) ;
#4418=AXIS2_PLACEMENT_3D ( 'NONE', #18934, #6901, #13841 ) ;
#4421=CIRCLE ( 'NONE', #188, 11.99999999999999822 ) ;
#4422=CARTESIAN_POINT ( 'NONE',  ( 10.00000000000000000, 17.70753755129037188, 21.03896658273978559 ) ) ;
#4426=CARTESIAN_POINT ( 'NONE',  ( 5.000000000000000000, 27.40684453873966575, 16.51862198942017557 ) ) ;
#4427=CYLINDRICAL_SURFACE ( 'NONE', #13599, 11.99999999999999822 ) ;
#4428=CYLINDRICAL_SURFACE ( 'NONE', #3127, 11.99999999999999822 ) ;
#4432=FACE_OUTER_BOUND ( 'NONE', #19077, .T. ) ;
#4434=EDGE_CURVE ( 'NONE', #12524, #11232, #5955, .T. ) ;
#4436=ORIENTED_EDGE ( 'NONE', *, *, #15759, .T. ) ;
#4437=AXIS2_PLACEMENT_3D ( 'NONE', #2812, #2579, #9310 ) ;
#4443=DIRECTION ( 'NONE',  ( 1.000000000000000000, 0.000000000000000000, -0.000000000000000000 ) ) ;
#4444=ORIENTED_EDGE ( 'NONE', *, *, #1369, .F. ) ;
#4446=ORIENTED_EDGE ( 'NONE', *, *, #12270, .F. ) ;
#4458=DIRECTION ( 'NONE',  ( 0.000000000000000000, 0.000000000000000000, 1.000000000000000000 ) ) ;
#4464=EDGE_CURVE ( 'NONE', #5258, #8125, #9264, .T. ) ;
#4477=ADVANCED_FACE ( 'NONE', ( #2770 ), #15914, .T. ) ;
#4483=ORIENTED_EDGE ( 'NONE', *, *, #2566, .T. ) ;
#4486=PLANE ( 'NONE',  #1566 ) ;
#4492=CARTESIAN_POINT ( 'NONE',  ( 10.00000000000000000, 0.000000000000000000, 0.000000000000000000 ) ) ;
#4498=CYLINDRICAL_SURFACE ( 'NONE', #2021, 32.00000000000000000 ) ;
#4500=CIRCLE ( 'NONE', #18621, 11.99999999999999822 ) ;
#4514=DIRECTION ( 'NONE',  ( -1.000000000000000000, -0.000000000000000000, 0.000000000000000000 ) ) ;
#4520=VECTOR ( 'NONE', #3117, 1000.000000000000000 ) ;
#4521=DIRECTION ( 'NONE',  ( -1.000000000000000000, 0.000000000000000000, 0.000000000000000000 ) ) ;
#4526=CARTESIAN_POINT ( 'NONE',  ( 5.000000000000000000, 19.29292659244040564, -25.53004080487742300 ) ) ;
#4527=AXIS2_PLACEMENT_3D ( 'NONE', #3664, #10398, #17152 ) ;
#4536=AXIS2_PLACEMENT_3D ( 'NONE', #12814, #21228, #7325 ) ;
#4544=DIRECTION ( 'NONE',  ( 0.000000000000000000, 0.2079116908177597312, -0.9781476007338054668 ) ) ;
#4548=VECTOR ( 'NONE', #14115, 1000.000000000000000 ) ;
#4552=EDGE_LOOP ( 'NONE', ( #15827, #10119, #5327, #8191 ) ) ;
#4562=ORIENTED_EDGE ( 'NONE', *, *, #1236, .F. ) ;
#4565=ORIENTED_EDGE ( 'NONE', *, *, #18915, .F. ) ;
#4566=CARTESIAN_POINT ( 'NONE',  ( 10.00000000000000000, 12.94633825542266869, 24.26081875733338933 ) ) ;
#4574=CARTESIAN_POINT ( 'NONE',  ( 10.00000000000000000, 0.000000000000000000, 0.000000000000000000 ) ) ;
#4578=ORIENTED_EDGE ( 'NONE', *, *, #5120, .F. ) ;
#4581=AXIS2_PLACEMENT_3D ( 'NONE', #12293, #5451, #8760 ) ;
#4582=CARTESIAN_POINT ( 'NONE',  ( 5.000000000000000888, -6.063030049134863653, -31.42037024962131397 ) ) ;
#4585=EDGE_LOOP ( 'NONE', ( #11923, #10689, #21215, #18356 ) ) ;
#4595=DIRECTION ( 'NONE',  ( 0.000000000000000000, 0.000000000000000000, 1.000000000000000000 ) ) ;
#4596=CARTESIAN_POINT ( 'NONE',  ( 0.000000000000000000, 31.88200538760793634, -2.745493118647102548 ) ) ;
#4598=VECTOR ( 'NONE', #18261, 1000.000000000000000 ) ;
#4600=DIRECTION ( 'NONE',  ( 0.000000000000000000, 0.000000000000000000, -1.000000000000000000 ) ) ;
#4603=CARTESIAN_POINT ( 'NONE',  ( 10.00000000000000000, 6.063030049135491595, -31.42037024962118608 ) ) ;
#4610=DIRECTION ( 'NONE',  ( -1.000000000000000000, -0.000000000000000000, -0.000000000000000000 ) ) ;
#4614=DIRECTION ( 'NONE',  ( 0.000000000000000000, 0.000000000000000000, -1.000000000000000000 ) ) ;
#4615=ORIENTED_EDGE ( 'NONE', *, *, #18018, .F. ) ;
#4620=VERTEX_POINT ( 'NONE', #3198 ) ;
#4622=EDGE_CURVE ( 'NONE', #18476, #17888, #18124, .T. ) ;
#4625=DIRECTION ( 'NONE',  ( -1.000000000000000000, 0.000000000000000000, -0.000000000000000000 ) ) ;
#4627=CARTESIAN_POINT ( 'NONE',  ( 10.00000000000000000, 12.46320060045723643, 29.47318494484032314 ) ) ;
#4641=VERTEX_POINT ( 'NONE', #10593 ) ;
#4648=DIRECTION ( 'NONE',  ( 0.000000000000000000, 0.000000000000000000, 1.000000000000000000 ) ) ;
#4650=DIRECTION ( 'NONE',  ( -1.000000000000000000, 0.000000000000000000, 0.000000000000000000 ) ) ;
#4661=CARTESIAN_POINT ( 'NONE',  ( 0.000000000000000000, -12.90282758292996235, 25.06465718894773431 ) ) ;
#4662=ORIENTED_EDGE ( 'NONE', *, *, #6004, .T. ) ;
#4663=ORIENTED_EDGE ( 'NONE', *, *, #12138, .T. ) ;
#4664=CARTESIAN_POINT ( 'NONE',  ( 10.00000000000000000, -17.83210509884655792, 21.83428559348755371 ) ) ;
#4665=ORIENTED_EDGE ( 'NONE', *, *, #9488, .T. ) ;
#4666=CARTESIAN_POINT ( 'NONE',  ( 0.000000000000000000, 26.27606311335951617, 10.21217444509420424 ) ) ;
#4671=FILL_AREA_STYLE ('',( #1254 ) ) ;
#4677=ORIENTED_EDGE ( 'NONE', *, *, #9150, .T. ) ;
#4678=AXIS2_PLACEMENT_3D ( 'NONE', #1088, #15999, #21305 ) ;
#4692=DIRECTION ( 'NONE',  ( -1.000000000000000000, 0.000000000000000000, -0.000000000000000000 ) ) ;
#4694=EDGE_LOOP ( 'NONE', ( #20163, #17216, #11298, #7833 ) ) ;
#4695=DIRECTION ( 'NONE',  ( 0.000000000000000000, -0.8660254037844432595, 0.4999999999999920064 ) ) ;
#4701=VECTOR ( 'NONE', #201, 1000.000000000000000 ) ;
#4703=FACE_OUTER_BOUND ( 'NONE', #18858, .T. ) ;
#4709=CYLINDRICAL_SURFACE ( 'NONE', #21075, 32.00000000000000000 ) ;
#4719=ORIENTED_EDGE ( 'NONE', *, *, #11950, .F. ) ;
#4720=CARTESIAN_POINT ( 'NONE',  ( -140.0000507999999968, 0.000000000000000000, -1.000000000000000000 ) ) ;
#4732=LINE ( 'NONE', #4526, #8809 ) ;
#4734=EDGE_CURVE ( 'NONE', #5926, #17286, #1378, .T. ) ;
#4742=ORIENTED_EDGE ( 'NONE', *, *, #17135, .T. ) ;
#4747=EDGE_CURVE ( 'NONE', #10528, #9780, #21142, .T. ) ;
#4750=EDGE_LOOP ( 'NONE', ( #14626, #8922, #796, #2137 ) ) ;
#4760=DIRECTION ( 'NONE',  ( 0.000000000000000000, 0.000000000000000000, 1.000000000000000000 ) ) ;
#4773=ORIENTED_EDGE ( 'NONE', *, *, #17566, .F. ) ;
#4789=AXIS2_PLACEMENT_3D ( 'NONE', #8762, #1911, #10629 ) ;
#4798=CARTESIAN_POINT ( 'NONE',  ( 10.00000000000000000, 14.53731623274928708, 23.34226719384910709 ) ) ;
#4799=VERTEX_POINT ( 'NONE', #21195 ) ;
#4807=EDGE_LOOP ( 'NONE', ( #6388, #242, #531, #6959 ) ) ;
#4811=VERTEX_POINT ( 'NONE', #9146 ) ;
#4813=DIRECTION ( 'NONE',  ( 1.000000000000000000, 0.000000000000000000, 0.000000000000000000 ) ) ;
#4821=AXIS2_PLACEMENT_3D ( 'NONE', #16469, #21656, #16250 ) ;
#4826=DIRECTION ( 'NONE',  ( -1.000000000000000000, 0.000000000000000000, 0.000000000000000000 ) ) ;
#4832=VECTOR ( 'NONE', #16253, 1000.000000000000000 ) ;
#4837=VECTOR ( 'NONE', #4521, 1000.000000000000000 ) ;
#4842=ADVANCED_FACE ( 'NONE', ( #17666 ), #4283, .T. ) ;
#4848=LINE ( 'NONE', #11590, #19374 ) ;
#4853=DIRECTION ( 'NONE',  ( -1.000000000000000000, -0.000000000000000000, -0.000000000000000000 ) ) ;
#4855=ORIENTED_EDGE ( 'NONE', *, *, #991, .F. ) ;
#4885=CARTESIAN_POINT ( 'NONE',  ( 0.000000000000000000, 0.000000000000000000, 0.000000000000000000 ) ) ;
#4886=VERTEX_POINT ( 'NONE', #10916 ) ;
#4897=CIRCLE ( 'NONE', #21472, 3.000000000000000444 ) ;
#4903=DIRECTION ( 'NONE',  ( -1.000000000000000000, 0.000000000000000000, 0.000000000000000000 ) ) ;
#4906=EDGE_CURVE ( 'NONE', #1686, #1185, #21297, .T. ) ;
#4910=VECTOR ( 'NONE', #16109, 1000.000000000000000 ) ;
#4911=DIRECTION ( 'NONE',  ( 1.000000000000000000, -0.000000000000000000, -0.000000000000000000 ) ) ;
#4914=EDGE_CURVE ( 'NONE', #18417, #16952, #10188, .T. ) ;
#4918=AXIS2_PLACEMENT_3D ( 'NONE', #12146, #10491, #20658 ) ;
#4920=ADVANCED_FACE ( 'NONE', ( #14555 ), #12899, .T. ) ;
#4932=CARTESIAN_POINT ( 'NONE',  ( 10.00000000000000000, 0.000000000000000000, 0.000000000000000000 ) ) ;
#4935=CIRCLE ( 'NONE', #1025, 11.99999999999999822 ) ;
#4943=CARTESIAN_POINT ( 'NONE',  ( 0.000000000000000000, 12.90282758293013643, -25.06465718894764194 ) ) ;
#4945=CARTESIAN_POINT ( 'NONE',  ( 10.00000000000000000, -7.409634587003275819, 27.19958299168154880 ) ) ;
#4948=CARTESIAN_POINT ( 'NONE',  ( 10.00000000000000000, -27.07404830566974141, 4.815694066514342175 ) ) ;
#4951=AXIS2_PLACEMENT_3D ( 'NONE', #20483, #2232, #2024 ) ;
#4965=VERTEX_POINT ( 'NONE', #16553 ) ;
#4966=CARTESIAN_POINT ( 'NONE',  ( 10.00000000000000000, -24.73395913766455578, -12.01774797440602427 ) ) ;
#4968=ORIENTED_EDGE ( 'NONE', *, *, #9054, .F. ) ;
#4982=VERTEX_POINT ( 'NONE', #9567 ) ;
#4983=DIRECTION ( 'NONE',  ( -1.000000000000000000, -0.000000000000000000, -0.000000000000000000 ) ) ;
#4984=ADVANCED_FACE ( 'NONE', ( #11347 ), #21624, .F. ) ;
#4986=ORIENTED_EDGE ( 'NONE', *, *, #716, .T. ) ;
#4988=VERTEX_POINT ( 'NONE', #8260 ) ;
#4990=VERTEX_POINT ( 'NONE', #20089 ) ;
#4995=CARTESIAN_POINT ( 'NONE',  ( 10.00000000000000000, 0.6021240089801420670, 31.99433460282944708 ) ) ;
#4996=ADVANCED_FACE ( 'NONE', ( #11689 ), #21413, .T. ) ;
#4998=DIRECTION ( 'NONE',  ( 0.000000000000000000, 0.4067366430758010964, -0.9135454576426006446 ) ) ;
#5002=CARTESIAN_POINT ( 'NONE',  ( 10.00000000000000000, -9.992993448021419312, -26.36019881529895770 ) ) ;
#5004=ORIENTED_EDGE ( 'NONE', *, *, #3956, .F. ) ;
#5012=EDGE_LOOP ( 'NONE', ( #3495, #13267, #15775, #2234 ) ) ;
#5016=EDGE_LOOP ( 'NONE', ( #3219, #12191, #15836, #7510 ) ) ;
#5019=ORIENTED_EDGE ( 'NONE', *, *, #4734, .F. ) ;
#5022=DIRECTION ( 'NONE',  ( 0.000000000000000000, 0.000000000000000000, -1.000000000000000000 ) ) ;
#5024=EDGE_CURVE ( 'NONE', #4316, #15667, #21159, .T. ) ;
#5027=CARTESIAN_POINT ( 'NONE',  ( 10.00000000000000000, -7.619321854369744074, 26.42235673590688094 ) ) ;
#5040=ORIENTED_EDGE ( 'NONE', *, *, #17566, .T. ) ;
#5042=EDGE_CURVE ( 'NONE', #11544, #20880, #3284, .T. ) ;
#5046=AXIS2_PLACEMENT_3D ( 'NONE', #5609, #12230, #7267 ) ;
#5048=ADVANCED_FACE ( 'NONE', ( #3070 ), #2853, .T. ) ;
#5051=VERTEX_POINT ( 'NONE', #13555 ) ;
#5057=CARTESIAN_POINT ( 'NONE',  ( 10.00000000000000000, 0.000000000000000000, 0.000000000000000000 ) ) ;
#5058=CARTESIAN_POINT ( 'NONE',  ( 10.00000000000000000, 0.000000000000000000, 0.000000000000000000 ) ) ;
#5064=DIRECTION ( 'NONE',  ( -1.000000000000000000, 0.000000000000000000, 0.000000000000000000 ) ) ;
#5068=CYLINDRICAL_SURFACE ( 'NONE', #13032, 11.99999999999999645 ) ;
#5075=DIRECTION ( 'NONE',  ( 0.000000000000000000, 0.000000000000000000, 1.000000000000000000 ) ) ;
#5076=ORIENTED_EDGE ( 'NONE', *, *, #1198, .T. ) ;
#5080=ORIENTED_EDGE ( 'NONE', *, *, #15907, .T. ) ;
#5089=DIRECTION ( 'NONE',  ( 0.000000000000000000, 0.000000000000000000, 1.000000000000000000 ) ) ;
#5091=VECTOR ( 'NONE', #9546, 1000.000000000000000 ) ;
#5093=CIRCLE ( 'NONE', #1900, 12.00000000000000000 ) ;
#5096=ORIENTED_EDGE ( 'NONE', *, *, #8486, .T. ) ;
#5097=VERTEX_POINT ( 'NONE', #20419 ) ;
#5098=DIRECTION ( 'NONE',  ( -1.000000000000000000, 0.000000000000000000, 0.000000000000000000 ) ) ;
#5101=DIRECTION ( 'NONE',  ( 0.000000000000000000, -0.9510565162951566398, 0.3090169943749382364 ) ) ;
#5102=ORIENTED_EDGE ( 'NONE', *, *, #6305, .F. ) ;
#5105=AXIS2_PLACEMENT_3D ( 'NONE', #16731, #20494, #5251 ) ;
#5108=AXIS2_PLACEMENT_3D ( 'NONE', #7992, #14722, #9736 ) ;
#5112=ADVANCED_FACE ( 'NONE', ( #10340 ), #13667, .T. ) ;
#5113=CARTESIAN_POINT ( 'NONE',  ( 10.00000000000000000, -27.26034713664092379, -7.182859710736426706 ) ) ;
#5115=DIRECTION ( 'NONE',  ( -1.000000000000000000, -0.000000000000000000, -0.000000000000000000 ) ) ;
#5118=AXIS2_PLACEMENT_3D ( 'NONE', #13347, #8273, #16666 ) ;
#5120=EDGE_CURVE ( 'NONE', #7280, #13685, #4935, .T. ) ;
#5122=CIRCLE ( 'NONE', #6879, 32.00000000000000000 ) ;
#5124=CYLINDRICAL_SURFACE ( 'NONE', #6660, 11.99999999999999645 ) ;
#5127=EDGE_LOOP ( 'NONE', ( #10112, #15985, #21112, #14527 ) ) ;
#5129=EDGE_LOOP ( 'NONE', ( #10770, #14684, #17287, #14844 ) ) ;
#5132=ORIENTED_EDGE ( 'NONE', *, *, #12743, .F. ) ;
#5135=ORIENTED_EDGE ( 'NONE', *, *, #8124, .F. ) ;
#5136=CARTESIAN_POINT ( 'NONE',  ( 0.000000000000000000, -31.75612719289743779, 3.943144139962448058 ) ) ;
#5139=ORIENTED_EDGE ( 'NONE', *, *, #808, .T. ) ;
#5140=AXIS2_PLACEMENT_3D ( 'NONE', #19403, #5823, #4158 ) ;
#5154=DIRECTION ( 'NONE',  ( 0.000000000000000000, 0.000000000000000000, 1.000000000000000000 ) ) ;
#5156=AXIS2_PLACEMENT_3D ( 'NONE', #11387, #16145, #21232 ) ;
#5157=AXIS2_PLACEMENT_3D ( 'NONE', #15951, #21040, #5909 ) ;
#5159=EDGE_CURVE ( 'NONE', #13513, #18417, #18692, .T. ) ;
#5162=DIRECTION ( 'NONE',  ( 0.000000000000000000, 0.000000000000000000, 1.000000000000000000 ) ) ;
#5164=ORIENTED_EDGE ( 'NONE', *, *, #7713, .F. ) ;
#5167=ORIENTED_EDGE ( 'NONE', *, *, #18814, .F. ) ;
#5170=DIRECTION ( 'NONE',  ( 0.000000000000000000, 0.000000000000000000, 1.000000000000000000 ) ) ;
#5173=DIRECTION ( 'NONE',  ( 0.000000000000000000, -0.9945218953682722907, -0.1045284632676635739 ) ) ;
#5174=DIRECTION ( 'NONE',  ( 0.000000000000000000, -0.5877852522924632561, -0.8090169943749545567 ) ) ;
#5177=DIRECTION ( 'NONE',  ( 0.000000000000000000, 0.5877852522924743583, -0.8090169943749465631 ) ) ;
#5178=AXIS2_PLACEMENT_3D ( 'NONE', #17041, #6781, #8637 ) ;
#5183=DIRECTION ( 'NONE',  ( 0.000000000000000000, 0.000000000000000000, 1.000000000000000000 ) ) ;
#5186=DIRECTION ( 'NONE',  ( -1.000000000000000000, -0.000000000000000000, 0.000000000000000000 ) ) ;
#5188=CIRCLE ( 'NONE', #8350, 27.49900000000000588 ) ;
#5191=EDGE_CURVE ( 'NONE', #142, #20213, #10857, .T. ) ;
#5193=ORIENTED_EDGE ( 'NONE', *, *, #18415, .F. ) ;
#5195=EDGE_CURVE ( 'NONE', #14985, #2027, #15856, .T. ) ;
#5201=DIRECTION ( 'NONE',  ( 0.000000000000000000, 0.2079116908177597312, -0.9781476007338054668 ) ) ;
#5202=CARTESIAN_POINT ( 'NONE',  ( 10.00000000000000000, -13.56333590714035431, 28.98337314858429892 ) ) ;
#5203=CIRCLE ( 'NONE', #17900, 32.00000000000000000 ) ;
#5204=CARTESIAN_POINT ( 'NONE',  ( 10.00000000000000000, 21.98203405400955290, 17.64965094506551324 ) ) ;
#5208=DIRECTION ( 'NONE',  ( -1.000000000000000000, 0.000000000000000000, 0.000000000000000000 ) ) ;
#5213=ORIENTED_EDGE ( 'NONE', *, *, #1886, .F. ) ;
#5216=CARTESIAN_POINT ( 'NONE',  ( 10.00000000000000000, 4.294029059350239486, -27.86182539015961979 ) ) ;
#5218=VERTEX_POINT ( 'NONE', #12621 ) ;
#5221=ORIENTED_EDGE ( 'NONE', *, *, #15955, .F. ) ;
#5226=DIRECTION ( 'NONE',  ( -1.000000000000000000, 0.000000000000000000, 0.000000000000000000 ) ) ;
#5227=DIRECTION ( 'NONE',  ( 0.000000000000000000, 0.000000000000000000, 1.000000000000000000 ) ) ;
#5229=CIRCLE ( 'NONE', #6999, 27.49900000000000233 ) ;
#5233=AXIS2_PLACEMENT_3D ( 'NONE', #1259, #9864, #9747 ) ;
#5234=FACE_OUTER_BOUND ( 'NONE', #3197, .T. ) ;
#5236=ORIENTED_EDGE ( 'NONE', *, *, #4914, .F. ) ;
#5248=AXIS2_PLACEMENT_3D ( 'NONE', #9845, #6558, #9949 ) ;
#5249=DIRECTION ( 'NONE',  ( 0.000000000000000000, 0.000000000000000000, 1.000000000000000000 ) ) ;
#5251=DIRECTION ( 'NONE',  ( 0.000000000000000000, 0.000000000000000000, 1.000000000000000000 ) ) ;
#5256=LINE ( 'NONE', #19157, #9472 ) ;
#5258=VERTEX_POINT ( 'NONE', #11300 ) ;
#5264=AXIS2_PLACEMENT_3D ( 'NONE', #1073, #4610, #19517 ) ;
#5275=ORIENTED_EDGE ( 'NONE', *, *, #12054, .T. ) ;
#5279=CARTESIAN_POINT ( 'NONE',  ( -10.00000000000000000, 0.000000000000000000, 0.000000000000000000 ) ) ;
#5281=DIRECTION ( 'NONE',  ( 0.000000000000000000, 0.000000000000000000, 1.000000000000000000 ) ) ;
#5284=CIRCLE ( 'NONE', #1047, 5.000000000000000000 ) ;
#5286=LINE ( 'NONE', #20739, #14239 ) ;
#5290=DIRECTION ( 'NONE',  ( -1.000000000000000000, 0.000000000000000000, -0.000000000000000000 ) ) ;
#5299=ADVANCED_FACE ( 'NONE', ( #14723 ), #16271, .T. ) ;
#5301=CIRCLE ( 'NONE', #4951, 32.00000000000000000 ) ;
#5311=ADVANCED_FACE ( 'NONE', ( #6235 ), #9297, .T. ) ;
#5313=CARTESIAN_POINT ( 'NONE',  ( 10.00000000000000000, -7.409634587002906336, -27.19958299168165183 ) ) ;
#5315=CIRCLE ( 'NONE', #12023, 11.99999999999999822 ) ;
#5317=LINE ( 'NONE', #20454, #8363 ) ;
#5323=EDGE_LOOP ( 'NONE', ( #327, #17530, #20505, #5797 ) ) ;
#5324=ORIENTED_EDGE ( 'NONE', *, *, #5445, .F. ) ;
#5326=EDGE_CURVE ( 'NONE', #7775, #1381, #4337, .T. ) ;
#5327=ORIENTED_EDGE ( 'NONE', *, *, #14613, .F. ) ;
#5340=MECHANICAL_DESIGN_GEOMETRIC_PRESENTATION_REPRESENTATION('',(#21560),#11318);
#5342=EDGE_CURVE ( 'NONE', #20840, #10449, #14612, .T. ) ;
#5355=DIRECTION ( 'NONE',  ( 1.000000000000000000, 0.000000000000000000, -0.000000000000000000 ) ) ;
#5356=CARTESIAN_POINT ( 'NONE',  ( 10.00000000000000000, -14.53731623274945406, 23.34226719384900761 ) ) ;
#5371=DIRECTION ( 'NONE',  ( 0.000000000000000000, -1.000000000000000000, -0.000000000000000000 ) ) ;
#5374=VERTEX_POINT ( 'NONE', #16702 ) ;
#5381=FACE_OUTER_BOUND ( 'NONE', #11751, .T. ) ;
#5402=ORIENTED_EDGE ( 'NONE', *, *, #13439, .T. ) ;
#5403=ORIENTED_EDGE ( 'NONE', *, *, #4434, .F. ) ;
#5407=CARTESIAN_POINT ( 'NONE',  ( 10.00000000000000000, 0.000000000000000000, 0.000000000000000000 ) ) ;
#5409=CARTESIAN_POINT ( 'NONE',  ( 0.000000000000000000, 0.000000000000000000, 0.000000000000000000 ) ) ;
#5412=ADVANCED_FACE ( 'NONE', ( #18711 ), #10071, .T. ) ;
#5420=ADVANCED_FACE ( 'NONE', ( #8633 ), #16821, .T. ) ;
#5428=EDGE_CURVE ( 'NONE', #16041, #5374, #6567, .T. ) ;
#5430=ORIENTED_EDGE ( 'NONE', *, *, #5428, .F. ) ;
#5434=CIRCLE ( 'NONE', #11065, 11.99999999999999822 ) ;
#5437=AXIS2_PLACEMENT_3D ( 'NONE', #21254, #11195, #6127 ) ;
#5440=DIRECTION ( 'NONE',  ( -1.000000000000000000, 0.000000000000000000, 0.000000000000000000 ) ) ;
#5442=CARTESIAN_POINT ( 'NONE',  ( 10.00000000000000000, -27.26034713664101972, 7.182859710736059888 ) ) ;
#5443=CARTESIAN_POINT ( 'NONE',  ( 10.00000000000000000, 0.000000000000000000, 0.000000000000000000 ) ) ;
#5445=EDGE_CURVE ( 'NONE', #11869, #3708, #13132, .T. ) ;
#5451=DIRECTION ( 'NONE',  ( 1.000000000000000000, 0.000000000000000000, 0.000000000000000000 ) ) ;
#5455=ORIENTED_EDGE ( 'NONE', *, *, #21029, .F. ) ;
#5461=EDGE_CURVE ( 'NONE', #5499, #10823, #12780, .T. ) ;
#5463=DIRECTION ( 'NONE',  ( 0.000000000000000000, -0.9510565162951503115, -0.3090169943749573878 ) ) ;
#5466=DIRECTION ( 'NONE',  ( 0.000000000000000000, 0.4067366430758008744, -0.9135454576426006446 ) ) ;
#5479=CARTESIAN_POINT ( 'NONE',  ( 10.00000000000000000, 0.000000000000000000, 0.000000000000000000 ) ) ;
#5498=CIRCLE ( 'NONE', #18550, 11.99999999999999822 ) ;
#5499=VERTEX_POINT ( 'NONE', #4995 ) ;
#5505=ORIENTED_EDGE ( 'NONE', *, *, #9202, .F. ) ;
#5506=CARTESIAN_POINT ( 'NONE',  ( 10.00000000000000000, 9.366510754379232750, 25.85466064925429208 ) ) ;
#5507=VERTEX_POINT ( 'NONE', #11731 ) ;
#5512=COLOUR_RGB ( '', 0.40784314, 0.44705882, 0.49803922) ;
#5517=DIRECTION ( 'NONE',  ( 0.000000000000000000, 0.000000000000000000, -1.000000000000000000 ) ) ;
#5523=FACE_OUTER_BOUND ( 'NONE', #12943, .T. ) ;
#5524=DIRECTION ( 'NONE',  ( 0.000000000000000000, 0.4067366430757948237, 0.9135454576426033091 ) ) ;
#5527=DIRECTION ( 'NONE',  ( -1.000000000000000000, -0.000000000000000000, -0.000000000000000000 ) ) ;
#5529=ORIENTED_EDGE ( 'NONE', *, *, #3818, .T. ) ;
#5539=ADVANCED_FACE ( 'NONE', ( #8746 ), #3884, .T. ) ;
#5542=DIRECTION ( 'NONE',  ( -1.000000000000000000, 0.000000000000000000, 0.000000000000000000 ) ) ;
#5546=DIRECTION ( 'NONE',  ( 0.000000000000000000, 0.000000000000000000, 1.000000000000000000 ) ) ;
#5551=CARTESIAN_POINT ( 'NONE',  ( 10.00000000000000000, -27.82509854686807671, -4.525913221811426190 ) ) ;
#5553=EDGE_CURVE ( 'NONE', #19849, #9701, #15702, .T. ) ;
#5558=CARTESIAN_POINT ( 'NONE',  ( -140.0000507999999968, 0.000000000000000000, 1.000000000000000000 ) ) ;
#5559=ORIENTED_EDGE ( 'NONE', *, *, #15860, .F. ) ;
#5561=CARTESIAN_POINT ( 'NONE',  ( 0.000000000000000000, 0.000000000000000000, 0.000000000000000000 ) ) ;
#5562=ORIENTED_EDGE ( 'NONE', *, *, #6283, .T. ) ;
#5570=LINE ( 'NONE', #7662, #12160 ) ;
#5574=AXIS2_PLACEMENT_3D ( 'NONE', #834, #12653, #16080 ) ;
#5577=DIRECTION ( 'NONE',  ( -1.000000000000000000, 0.000000000000000000, 0.000000000000000000 ) ) ;
#5583=DIRECTION ( 'NONE',  ( 0.000000000000000000, -0.7431448254773999063, 0.6691306063588517983 ) ) ;
#5586=ADVANCED_FACE ( 'NONE', ( #8954 ), #14043, .T. ) ;
#5595=VERTEX_POINT ( 'NONE', #2330 ) ;
#5597=ADVANCED_FACE ( 'NONE', ( #18803 ), #12380, .T. ) ;
#5599=ORIENTED_EDGE ( 'NONE', *, *, #15518, .T. ) ;
#5603=DIRECTION ( 'NONE',  ( 0.000000000000000000, -0.4067366430758072582, 0.9135454576425977580 ) ) ;
#5604=DIRECTION ( 'NONE',  ( 0.000000000000000000, 0.000000000000000000, -1.000000000000000000 ) ) ;
#5609=CARTESIAN_POINT ( 'NONE',  ( 10.00000000000000000, 28.15804365424197186, -1.358152127006073684 ) ) ;
#5616=CARTESIAN_POINT ( 'NONE',  ( 0.000000000000000000, -24.73395913766471921, 12.01774797440568854 ) ) ;
#5620=CARTESIAN_POINT ( 'NONE',  ( 10.00000000000000000, 27.82509854686811224, 4.525913221811229903 ) ) ;
#5624=AXIS2_PLACEMENT_3D ( 'NONE', #3386, #13211, #1299 ) ;
#5625=ORIENTED_EDGE ( 'NONE', *, *, #9566, .F. ) ;
#5628=AXIS2_PLACEMENT_3D ( 'NONE', #16333, #1200, #7943 ) ;
#5637=CARTESIAN_POINT ( 'NONE',  ( 10.00000000000000000, 17.70753755129066320, -21.03896658273954046 ) ) ;
#5644=ORIENTED_EDGE ( 'NONE', *, *, #16357, .F. ) ;
#5649=VERTEX_POINT ( 'NONE', #1107 ) ;
#5655=DIRECTION ( 'NONE',  ( -1.000000000000000000, -0.000000000000000000, 0.000000000000000000 ) ) ;
#5656=DIRECTION ( 'NONE',  ( -1.000000000000000000, -0.000000000000000000, -0.000000000000000000 ) ) ;
#5658=DIRECTION ( 'NONE',  ( -1.000000000000000000, -0.000000000000000000, -0.000000000000000000 ) ) ;
#5665=DIRECTION ( 'NONE',  ( 0.000000000000000000, 0.000000000000000000, 1.000000000000000000 ) ) ;
#5675=CARTESIAN_POINT ( 'NONE',  ( 5.000000000000000888, -31.88200538760792213, -2.745493118647322817 ) ) ;
#5685=EDGE_CURVE ( 'NONE', #14063, #11424, #19448, .T. ) ;
#5686=VERTEX_POINT ( 'NONE', #13039 ) ;
#5688=ADVANCED_FACE ( 'NONE', ( #4307 ), #14371, .T. ) ;
#5690=DIRECTION ( 'NONE',  ( 0.000000000000000000, 0.000000000000000000, 1.000000000000000000 ) ) ;
#5692=EDGE_CURVE ( 'NONE', #1381, #16306, #12417, .T. ) ;
#5695=CARTESIAN_POINT ( 'NONE',  ( -140.0000507999999968, 0.000000000000000000, 0.000000000000000000 ) ) ;
#5699=VERTEX_POINT ( 'NONE', #5989 ) ;
#5700=ORIENTED_EDGE ( 'NONE', *, *, #8274, .T. ) ;
#5703=DIRECTION ( 'NONE',  ( -1.000000000000000000, -0.000000000000000000, 0.000000000000000000 ) ) ;
#5707=CYLINDRICAL_SURFACE ( 'NONE', #14381, 32.00000000000000000 ) ;
#5709=DIRECTION ( 'NONE',  ( 0.000000000000000000, -0.9945218953682744001, 0.1045284632676436454 ) ) ;
#5710=EDGE_CURVE ( 'NONE', #8125, #4886, #16304, .T. ) ;
#5752=VECTOR ( 'NONE', #18248, 1000.000000000000000 ) ;
#5761=DIRECTION ( 'NONE',  ( -1.000000000000000000, 0.000000000000000000, 0.000000000000000000 ) ) ;
#5766=CYLINDRICAL_SURFACE ( 'NONE', #3383, 27.49900000000000233 ) ;
#5768=DIRECTION ( 'NONE',  ( -1.000000000000000000, -0.000000000000000000, -0.000000000000000000 ) ) ;
#5773=CYLINDRICAL_SURFACE ( 'NONE', #8679, 11.99999999999999822 ) ;
#5775=FACE_OUTER_BOUND ( 'NONE', #5129, .T. ) ;
#5781=CYLINDRICAL_SURFACE ( 'NONE', #2573, 32.00000000000000000 ) ;
#5787=DIRECTION ( 'NONE',  ( -1.000000000000000000, -0.000000000000000000, -0.000000000000000000 ) ) ;
#5792=EDGE_CURVE ( 'NONE', #10821, #14214, #6463, .T. ) ;
#5793=CARTESIAN_POINT ( 'NONE',  ( 10.00000000000000000, 27.40684453873988957, -16.51862198941980608 ) ) ;
#5797=ORIENTED_EDGE ( 'NONE', *, *, #6305, .T. ) ;
#5802=CARTESIAN_POINT ( 'NONE',  ( 0.000000000000000000, 25.48117629651203941, -10.33947075754235989 ) ) ;
#5807=( NAMED_UNIT ( * ) PLANE_ANGLE_UNIT ( ) SI_UNIT ( $, .RADIAN. ) );
#5810=EDGE_LOOP ( 'NONE', ( #11980, #14903, #21542, #19256 ) ) ;
#5817=DIRECTION ( 'NONE',  ( -1.000000000000000000, 0.000000000000000000, 0.000000000000000000 ) ) ;
#5823=DIRECTION ( 'NONE',  ( -1.000000000000000000, 0.000000000000000000, 0.000000000000000000 ) ) ;
#5830=AXIS2_PLACEMENT_3D ( 'NONE', #9573, #1197, #19324 ) ;
#5833=EDGE_CURVE ( 'NONE', #10108, #13306, #6114, .T. ) ;
#5834=CARTESIAN_POINT ( 'NONE',  ( 10.00000000000000000, 7.619321854369562885, 26.42235673590693423 ) ) ;
#5837=DIRECTION ( 'NONE',  ( -1.000000000000000000, 0.000000000000000000, 0.000000000000000000 ) ) ;
#5838=ORIENTED_EDGE ( 'NONE', *, *, #1642, .F. ) ;
#5841=EDGE_LOOP ( 'NONE', ( #6043, #12072, #13711, #5139 ) ) ;
#5845=ORIENTED_EDGE ( 'NONE', *, *, #4058, .F. ) ;
#5847=EDGE_CURVE ( 'NONE', #5258, #4988, #99, .T. ) ;
#5851=CIRCLE ( 'NONE', #14654, 11.99999999999999645 ) ;
#5854=CARTESIAN_POINT ( 'NONE',  ( 10.00000000000000000, 15.25521607131237722, -23.70650506194154872 ) ) ;
#5856=DIRECTION ( 'NONE',  ( 0.000000000000000000, 0.000000000000000000, 1.000000000000000000 ) ) ;
#5859=EDGE_CURVE ( 'NONE', #13685, #21583, #21652, .T. ) ;
#5862=ORIENTED_EDGE ( 'NONE', *, *, #3134, .T. ) ;
#5863=AXIS2_PLACEMENT_3D ( 'NONE', #20400, #16971, #13539 ) ;
#5868=ADVANCED_FACE ( 'NONE', ( #6536, #3096 ), #8, .F. ) ;
#5872=EDGE_LOOP ( 'NONE', ( #6278, #501, #11103, #9344 ) ) ;
#5877=DIRECTION ( 'NONE',  ( 0.000000000000000000, 0.2079116908177532919, 0.9781476007338070211 ) ) ;
#5879=AXIS2_PLACEMENT_3D ( 'NONE', #15354, #15684, #20557 ) ;
#5880=CARTESIAN_POINT ( 'NONE',  ( 5.000000000000000000, 19.29292659244005392, 25.53004080487768590 ) ) ;
#5884=DIRECTION ( 'NONE',  ( -1.000000000000000000, 0.000000000000000000, 0.000000000000000000 ) ) ;
#5885=ORIENTED_EDGE ( 'NONE', *, *, #18533, .F. ) ;
#5896=ORIENTED_EDGE ( 'NONE', *, *, #21572, .T. ) ;
#5898=FACE_OUTER_BOUND ( 'NONE', #7369, .T. ) ;
#5907=EDGE_LOOP ( 'NONE', ( #13629, #3548, #14885, #3718 ) ) ;
#5909=DIRECTION ( 'NONE',  ( 0.000000000000000000, -0.8660254037844431485, 0.4999999999999919509 ) ) ;
#5916=PRODUCT_DEFINITION ( 'UNKNOWN', '', #16301, #20652 ) ;
#5918=AXIS2_PLACEMENT_3D ( 'NONE', #9004, #17972, #19399 ) ;
#5926=VERTEX_POINT ( 'NONE', #13467 ) ;
#5929=FACE_OUTER_BOUND ( 'NONE', #12501, .T. ) ;
#5947=DIRECTION ( 'NONE',  ( 0.000000000000000000, 0.000000000000000000, 1.000000000000000000 ) ) ;
#5955=CIRCLE ( 'NONE', #6314, 32.00000000000000000 ) ;
#5961=EDGE_CURVE ( 'NONE', #9187, #15746, #13491, .T. ) ;
#5965=CARTESIAN_POINT ( 'NONE',  ( 150.0000507999999968, 0.000000000000000000, 0.000000000000000000 ) ) ;
#5966=DIRECTION ( 'NONE',  ( 0.000000000000000000, 0.000000000000000000, 1.000000000000000000 ) ) ;
#5972=AXIS2_PLACEMENT_3D ( 'NONE', #19648, #4514, #7933 ) ;
#5974=ADVANCED_FACE ( 'NONE', ( #12140 ), #2305, .T. ) ;
#5977=CIRCLE ( 'NONE', #8790, 3.000000000000000444 ) ;
#5983=AXIS2_PLACEMENT_3D ( 'NONE', #18923, #5115, #16946 ) ;
#5989=CARTESIAN_POINT ( 'NONE',  ( 0.000000000000000000, 24.73395913766479737, -12.01774797440552689 ) ) ;
#5990=AXIS2_PLACEMENT_3D ( 'NONE', #18214, #14786, #9679 ) ;
#5991=CARTESIAN_POINT ( 'NONE',  ( 10.00000000000000888, 4.000000000000000000, -1.000000000000000000 ) ) ;
#5994=DIRECTION ( 'NONE',  ( 0.000000000000000000, 0.000000000000000000, 1.000000000000000000 ) ) ;
#5995=CIRCLE ( 'NONE', #7054, 27.49900000000000233 ) ;
#6004=EDGE_CURVE ( 'NONE', #5051, #1433, #13904, .T. ) ;
#6030=DIRECTION ( 'NONE',  ( -1.000000000000000000, -0.000000000000000000, 0.000000000000000000 ) ) ;
#6041=CARTESIAN_POINT ( 'NONE',  ( 0.000000000000000000, 0.000000000000000000, 0.000000000000000000 ) ) ;
#6042=EDGE_CURVE ( 'NONE', #9782, #13000, #20212, .T. ) ;
#6043=ORIENTED_EDGE ( 'NONE', *, *, #4332, .T. ) ;
#6050=ORIENTED_EDGE ( 'NONE', *, *, #6078, .T. ) ;
#6051=CARTESIAN_POINT ( 'NONE',  ( 0.000000000000000000, 0.6021240089801385142, 31.99433460282945063 ) ) ;
#6060=ORIENTED_EDGE ( 'NONE', *, *, #5195, .F. ) ;
#6062=ORIENTED_EDGE ( 'NONE', *, *, #5859, .T. ) ;
#6078=EDGE_CURVE ( 'NONE', #17973, #20213, #18820, .T. ) ;
#6080=CARTESIAN_POINT ( 'NONE',  ( 0.000000000000000000, 7.619321854369911051, -26.42235673590683476 ) ) ;
#6083=VERTEX_POINT ( 'NONE', #4287 ) ;
#6093=EDGE_CURVE ( 'NONE', #2453, #18773, #21089, .T. ) ;
#6096=DIRECTION ( 'NONE',  ( -1.000000000000000000, 0.000000000000000000, -0.000000000000000000 ) ) ;
#6097=DIRECTION ( 'NONE',  ( 1.000000000000000000, -0.000000000000000000, -0.000000000000000000 ) ) ;
#6100=ORIENTED_EDGE ( 'NONE', *, *, #9080, .F. ) ;
#6108=AXIS2_PLACEMENT_3D ( 'NONE', #9171, #2655, #7751 ) ;
#6114=CIRCLE ( 'NONE', #19143, 27.49900000000000588 ) ;
#6115=ORIENTED_EDGE ( 'NONE', *, *, #10789, .T. ) ;
#6126=AXIS2_PLACEMENT_3D ( 'NONE', #10577, #20428, #18296 ) ;
#6127=DIRECTION ( 'NONE',  ( 0.000000000000000000, -0.9945218953682744001, 0.1045284632676437286 ) ) ;
#6133=AXIS2_PLACEMENT_3D ( 'NONE', #17212, #1960, #5177 ) ;
#6137=VECTOR ( 'NONE', #15519, 1000.000000000000000 ) ;
#6144=( NAMED_UNIT ( * ) SI_UNIT ( $, .STERADIAN. ) SOLID_ANGLE_UNIT ( ) );
#6148=DIRECTION ( 'NONE',  ( 0.000000000000000000, -0.2079116908177666145, 0.9781476007338040235 ) ) ;
#6154=DIRECTION ( 'NONE',  ( -1.000000000000000000, 0.000000000000000000, 0.000000000000000000 ) ) ;
#6158=AXIS2_PLACEMENT_3D ( 'NONE', #11736, #12064, #35 ) ;
#6160=AXIS2_PLACEMENT_3D ( 'NONE', #18068, #8017, #2922 ) ;
#6177=DIRECTION ( 'NONE',  ( 0.000000000000000000, 0.000000000000000000, 1.000000000000000000 ) ) ;
#6184=DIRECTION ( 'NONE',  ( 1.000000000000000000, 0.000000000000000000, 0.000000000000000000 ) ) ;
#6188=DIRECTION ( 'NONE',  ( -1.000000000000000000, -0.000000000000000000, 0.000000000000000000 ) ) ;
#6191=ORIENTED_EDGE ( 'NONE', *, *, #11673, .T. ) ;
#6194=CIRCLE ( 'NONE', #7610, 11.99999999999999822 ) ;
#6208=CIRCLE ( 'NONE', #16062, 27.49900000000000233 ) ;
#6212=VECTOR ( 'NONE', #8301, 1000.000000000000000 ) ;
#6214=AXIS2_PLACEMENT_3D ( 'NONE', #6602, #1724, #13317 ) ;
#6221=CARTESIAN_POINT ( 'NONE',  ( -140.0000507999999968, 0.000000000000000000, 0.000000000000000000 ) ) ;
#6223=DIRECTION ( 'NONE',  ( 0.000000000000000000, 0.000000000000000000, 1.000000000000000000 ) ) ;
#6226=ORIENTED_EDGE ( 'NONE', *, *, #20416, .T. ) ;
#6235=FACE_OUTER_BOUND ( 'NONE', #8881, .T. ) ;
#6236=EDGE_CURVE ( 'NONE', #3708, #7417, #3988, .T. ) ;
#6248=VERTEX_POINT ( 'NONE', #18102 ) ;
#6250=EDGE_CURVE ( 'NONE', #15205, #667, #18116, .T. ) ;
#6254=CARTESIAN_POINT ( 'NONE',  ( 10.00000000000000000, 0.000000000000000000, 0.000000000000000000 ) ) ;
#6265=CARTESIAN_POINT ( 'NONE',  ( 5.000000000000000000, 18.31866948046803145, -26.23788002993705248 ) ) ;
#6275=EDGE_CURVE ( 'NONE', #6639, #14519, #15640, .T. ) ;
#6276=CARTESIAN_POINT ( 'NONE',  ( 150.0000507999999968, 4.000000000000000000, 1.000000000000000000 ) ) ;
#6278=ORIENTED_EDGE ( 'NONE', *, *, #20321, .T. ) ;
#6283=EDGE_CURVE ( 'NONE', #14005, #7793, #14998, .T. ) ;
#6288=ORIENTED_EDGE ( 'NONE', *, *, #8827, .F. ) ;
#6289=DIRECTION ( 'NONE',  ( -1.000000000000000000, 0.000000000000000000, 0.000000000000000000 ) ) ;
#6292=LINE ( 'NONE', #8258, #20633 ) ;
#6296=CYLINDRICAL_SURFACE ( 'NONE', #74, 32.00000000000000000 ) ;
#6298=AXIS2_PLACEMENT_3D ( 'NONE', #2326, #20470, #241 ) ;
#6299=VECTOR ( 'NONE', #14075, 1000.000000000000000 ) ;
#6303=AXIS2_PLACEMENT_3D ( 'NONE', #17533, #19505, #15875 ) ;
#6305=EDGE_CURVE ( 'NONE', #16815, #14063, #12807, .T. ) ;
#6312=ORIENTED_EDGE ( 'NONE', *, *, #4747, .F. ) ;
#6314=AXIS2_PLACEMENT_3D ( 'NONE', #12802, #11041, #4207 ) ;
#6316=CIRCLE ( 'NONE', #15123, 11.99999999999999822 ) ;
#6325=CARTESIAN_POINT ( 'NONE',  ( 10.00000000000000000, 12.90282758292980247, 25.06465718894781247 ) ) ;
#6334=CARTESIAN_POINT ( 'NONE',  ( 10.00000000000000000, -27.82509854686814066, 4.525913221811051379 ) ) ;
#6338=LINE ( 'NONE', #18371, #16949 ) ;
#6339=ORIENTED_EDGE ( 'NONE', *, *, #20674, .T. ) ;
#6341=VERTEX_POINT ( 'NONE', #10345 ) ;
#6348=ORIENTED_EDGE ( 'NONE', *, *, #21178, .F. ) ;
#6362=ORIENTED_EDGE ( 'NONE', *, *, #19758, .F. ) ;
#6365=DIRECTION ( 'NONE',  ( -1.000000000000000000, -0.000000000000000000, 0.000000000000000000 ) ) ;
#6370=SURFACE_STYLE_FILL_AREA ( #8012 ) ;
#6372=EDGE_LOOP ( 'NONE', ( #19956, #21497, #6604, #8400 ) ) ;
#6374=CARTESIAN_POINT ( 'NONE',  ( 10.00000000000000000, -27.26034713664101972, 7.182859710736059888 ) ) ;
#6376=EDGE_CURVE ( 'NONE', #13049, #20840, #9284, .T. ) ;
#6383=CYLINDRICAL_SURFACE ( 'NONE', #18146, 32.00000000000000000 ) ;
#6387=EDGE_CURVE ( 'NONE', #14519, #18351, #12114, .T. ) ;
#6388=ORIENTED_EDGE ( 'NONE', *, *, #18412, .F. ) ;
#6390=DIRECTION ( 'NONE',  ( 0.000000000000000000, 0.5877852522924688072, 0.8090169943749505599 ) ) ;
#6391=ORIENTED_EDGE ( 'NONE', *, *, #20113, .F. ) ;
#6396=AXIS2_PLACEMENT_3D ( 'NONE', #21407, #14781, #7815 ) ;
#6412=DIRECTION ( 'NONE',  ( 1.000000000000000000, 0.000000000000000000, 0.000000000000000000 ) ) ;
#6415=DIRECTION ( 'NONE',  ( 0.000000000000000000, 0.7431448254773953543, -0.6691306063588570163 ) ) ;
#6417=DIRECTION ( 'NONE',  ( -1.000000000000000000, -0.000000000000000000, 0.000000000000000000 ) ) ;
#6421=ADVANCED_FACE ( 'NONE', ( #1849 ), #18977, .T. ) ;
#6422=ORIENTED_EDGE ( 'NONE', *, *, #17164, .F. ) ;
#6424=EDGE_CURVE ( 'NONE', #9318, #11653, #5434, .T. ) ;
#6425=EDGE_CURVE ( 'NONE', #13306, #14528, #5286, .T. ) ;
#6426=ORIENTED_EDGE ( 'NONE', *, *, #8035, .F. ) ;
#6432=CYLINDRICAL_SURFACE ( 'NONE', #6951, 27.49900000000000233 ) ;
#6434=LINE ( 'NONE', #14590, #13291 ) ;
#6443=ORIENTED_EDGE ( 'NONE', *, *, #12112, .T. ) ;
#6446=ORIENTED_EDGE ( 'NONE', *, *, #3134, .F. ) ;
#6451=DIRECTION ( 'NONE',  ( -1.000000000000000000, 0.000000000000000000, 0.000000000000000000 ) ) ;
#6453=CARTESIAN_POINT ( 'NONE',  ( 10.00000000000000000, -19.85071254963763465, -20.01672328094552356 ) ) ;
#6454=DIRECTION ( 'NONE',  ( -1.000000000000000000, 0.000000000000000000, -0.000000000000000000 ) ) ;
#6459=CARTESIAN_POINT ( 'NONE',  ( 150.0000507999999968, 2.828427124746190291, -1.000000000000000000 ) ) ;
#6463=CIRCLE ( 'NONE', #2205, 11.99999999999999822 ) ;
#6464=EDGE_LOOP ( 'NONE', ( #19906, #13958, #4742, #354 ) ) ;
#6472=ORIENTED_EDGE ( 'NONE', *, *, #588, .F. ) ;
#6474=DIRECTION ( 'NONE',  ( 1.000000000000000000, -0.000000000000000000, -0.000000000000000000 ) ) ;
#6475=EDGE_CURVE ( 'NONE', #2850, #8227, #11417, .T. ) ;
#6480=DIRECTION ( 'NONE',  ( 0.000000000000000000, 0.000000000000000000, 1.000000000000000000 ) ) ;
#6483=DIRECTION ( 'NONE',  ( -1.000000000000000000, 0.000000000000000000, 0.000000000000000000 ) ) ;
#6487=CARTESIAN_POINT ( 'NONE',  ( -10.00000000000000000, 0.000000000000000000, 0.000000000000000000 ) ) ;
#6489=DIRECTION ( 'NONE',  ( 0.000000000000000000, 0.9510565162951544194, -0.3090169943749448422 ) ) ;
#6501=AXIS2_PLACEMENT_3D ( 'NONE', #4932, #18515, #16411 ) ;
#6506=DIRECTION ( 'NONE',  ( -1.000000000000000000, 0.000000000000000000, 0.000000000000000000 ) ) ;
#6512=DIRECTION ( 'NONE',  ( 0.000000000000000000, 0.9945218953682729568, 0.1045284632676570374 ) ) ;
#6517=EDGE_CURVE ( 'NONE', #17888, #9822, #10705, .T. ) ;
#6528=ORIENTED_EDGE ( 'NONE', *, *, #1892, .T. ) ;
#6529=ORIENTED_EDGE ( 'NONE', *, *, #18834, .F. ) ;
#6532=ORIENTED_EDGE ( 'NONE', *, *, #6424, .T. ) ;
#6535=CIRCLE ( 'NONE', #3694, 3.000000000000000444 ) ;
#6536=FACE_OUTER_BOUND ( 'NONE', #3374, .T. ) ;
#6540=CARTESIAN_POINT ( 'NONE',  ( 10.00000000000000000, 25.17124263951009411, -12.69364185792227495 ) ) ;
#6553=ORIENTED_EDGE ( 'NONE', *, *, #19852, .F. ) ;
#6554=CIRCLE ( 'NONE', #11834, 3.000000000000000444 ) ;
#6555=DIRECTION ( 'NONE',  ( -1.000000000000000000, 0.000000000000000000, 0.000000000000000000 ) ) ;
#6556=EDGE_CURVE ( 'NONE', #14635, #18240, #16349, .T. ) ;
#6558=DIRECTION ( 'NONE',  ( -1.000000000000000000, -0.000000000000000000, 0.000000000000000000 ) ) ;
#6559=ORIENTED_EDGE ( 'NONE', *, *, #16071, .F. ) ;
#6563=LINE ( 'NONE', #14933, #4520 ) ;
#6567=LINE ( 'NONE', #3224, #12077 ) ;
#6580=AXIS2_PLACEMENT_3D ( 'NONE', #13817, #235, #7091 ) ;
#6586=CARTESIAN_POINT ( 'NONE',  ( 10.00000000000000000, 7.240962358591573889, 31.16999300804317130 ) ) ;
#6587=ORIENTED_EDGE ( 'NONE', *, *, #3774, .F. ) ;
#6591=ORIENTED_EDGE ( 'NONE', *, *, #13411, .T. ) ;
#6592=DIRECTION ( 'NONE',  ( 0.000000000000000000, 0.000000000000000000, 1.000000000000000000 ) ) ;
#6600=ORIENTED_EDGE ( 'NONE', *, *, #597, .F. ) ;
#6601=AXIS2_PLACEMENT_3D ( 'NONE', #19674, #11379, #4544 ) ;
#6602=CARTESIAN_POINT ( 'NONE',  ( 10.00000000000000000, 0.000000000000000000, 0.000000000000000000 ) ) ;
#6604=ORIENTED_EDGE ( 'NONE', *, *, #15247, .T. ) ;
#6608=DIRECTION ( 'NONE',  ( 1.000000000000000000, -0.000000000000000000, 0.000000000000000000 ) ) ;
#6613=VERTEX_POINT ( 'NONE', #4267 ) ;
#6614=AXIS2_PLACEMENT_3D ( 'NONE', #4943, #18320, #1296 ) ;
#6616=DIRECTION ( 'NONE',  ( -1.000000000000000000, -0.000000000000000000, -0.000000000000000000 ) ) ;
#6622=DIRECTION ( 'NONE',  ( 0.000000000000000000, -0.9945218953682744001, 0.1045284632676437286 ) ) ;
#6629=DIRECTION ( 'NONE',  ( 0.000000000000000000, 0.000000000000000000, -1.000000000000000000 ) ) ;
#6630=CIRCLE ( 'NONE', #18263, 11.99999999999999822 ) ;
#6637=EDGE_CURVE ( 'NONE', #18968, #5218, #14430, .T. ) ;
#6639=VERTEX_POINT ( 'NONE', #3258 ) ;
#6642=AXIS2_PLACEMENT_3D ( 'NONE', #15963, #11401, #1456 ) ;
#6643=ORIENTED_EDGE ( 'NONE', *, *, #6078, .F. ) ;
#6645=VECTOR ( 'NONE', #19945, 1000.000000000000000 ) ;
#6648=EDGE_CURVE ( 'NONE', #4047, #839, #17072, .T. ) ;
#6654=CIRCLE ( 'NONE', #18993, 32.00000000000000000 ) ;
#6660=AXIS2_PLACEMENT_3D ( 'NONE', #3788, #13838, #15169 ) ;
#6665=EDGE_CURVE ( 'NONE', #9782, #628, #7198, .T. ) ;
#6666=CARTESIAN_POINT ( 'NONE',  ( 0.000000000000000000, -23.57863763525709189, -15.45211464167688753 ) ) ;
#6667=ORIENTED_EDGE ( 'NONE', *, *, #6275, .T. ) ;
#6669=ORIENTED_EDGE ( 'NONE', *, *, #4206, .T. ) ;
#6673=EDGE_CURVE ( 'NONE', #10108, #1056, #2930, .T. ) ;
#6703=DIRECTION ( 'NONE',  ( 1.000000000000000000, 0.000000000000000000, 0.000000000000000000 ) ) ;
#6706=LINE ( 'NONE', #11661, #3723 ) ;
#6708=ADVANCED_FACE ( 'NONE', ( #14761 ), #6383, .T. ) ;
#6711=CARTESIAN_POINT ( 'NONE',  ( 10.00000000000000000, 14.53731623274928708, 23.34226719384910709 ) ) ;
#6715=AXIS2_PLACEMENT_3D ( 'NONE', #16163, #9406, #11189 ) ;
#6723=CYLINDRICAL_SURFACE ( 'NONE', #21489, 27.49900000000000233 ) ;
#6732=VERTEX_POINT ( 'NONE', #14966 ) ;
#6734=DIRECTION ( 'NONE',  ( 0.000000000000000000, 0.9510565162951544194, -0.3090169943749449533 ) ) ;
#6743=DIRECTION ( 'NONE',  ( -1.000000000000000000, 0.000000000000000000, -0.000000000000000000 ) ) ;
#6758=CARTESIAN_POINT ( 'NONE',  ( 10.00000000000000000, 26.27606311335951617, 10.21217444509420424 ) ) ;
#6771=CARTESIAN_POINT ( 'NONE',  ( 10.00000000000000000, -15.25521607131190294, -23.70650506194185425 ) ) ;
#6772=VERTEX_POINT ( 'NONE', #18626 ) ;
#6774=SHAPE_DEFINITION_REPRESENTATION ( #13742, #11927 ) ;
#6775=FACE_OUTER_BOUND ( 'NONE', #1761, .T. ) ;
#6781=DIRECTION ( 'NONE',  ( -1.000000000000000000, 0.000000000000000000, 0.000000000000000000 ) ) ;
#6782=DIRECTION ( 'NONE',  ( -1.000000000000000000, -0.000000000000000000, -0.000000000000000000 ) ) ;
#6784=EDGE_CURVE ( 'NONE', #10646, #17995, #10220, .T. ) ;
#6788=EDGE_CURVE ( 'NONE', #18503, #628, #16966, .T. ) ;
#6799=ORIENTED_EDGE ( 'NONE', *, *, #5, .F. ) ;
#6804=DIRECTION ( 'NONE',  ( 0.000000000000000000, -0.9510565162951566398, 0.3090169943749382364 ) ) ;
#6816=CARTESIAN_POINT ( 'NONE',  ( 10.00000000000000000, 17.83210509884670714, -21.83428559348744002 ) ) ;
#6823=DIRECTION ( 'NONE',  ( -1.000000000000000000, 0.000000000000000000, 0.000000000000000000 ) ) ;
#6825=ORIENTED_EDGE ( 'NONE', *, *, #8964, .T. ) ;
#6831=DIRECTION ( 'NONE',  ( -1.000000000000000000, 0.000000000000000000, 0.000000000000000000 ) ) ;
#6836=CARTESIAN_POINT ( 'NONE',  ( 10.00000000000000000, -7.409634587002906336, -27.19958299168165183 ) ) ;
#6839=CARTESIAN_POINT ( 'NONE',  ( 10.00000000000000000, 18.31866948046765842, 26.23788002993730117 ) ) ;
#6842=CARTESIAN_POINT ( 'NONE',  ( 10.00000000000000000, -25.17124263951018293, 12.69364185792209909 ) ) ;
#6854=DIRECTION ( 'NONE',  ( -1.000000000000000000, -0.000000000000000000, -0.000000000000000000 ) ) ;
#6861=CARTESIAN_POINT ( 'NONE',  ( 10.00000000000000000, -28.15804365424196121, -1.358152127006266197 ) ) ;
#6872=AXIS2_PLACEMENT_3D ( 'NONE', #5204, #11938, #9526 ) ;
#6873=ORIENTED_EDGE ( 'NONE', *, *, #20358, .F. ) ;
#6877=ORIENTED_EDGE ( 'NONE', *, *, #21396, .F. ) ;
#6879=AXIS2_PLACEMENT_3D ( 'NONE', #3153, #21707, #6592 ) ;
#6884=LINE ( 'NONE', #8431, #18893 ) ;
#6898=CARTESIAN_POINT ( 'NONE',  ( 10.00000000000000000, -1.959304526717615902, -27.42911093658677402 ) ) ;
#6899=DIRECTION ( 'NONE',  ( -1.000000000000000000, 0.000000000000000000, 0.000000000000000000 ) ) ;
#6901=DIRECTION ( 'NONE',  ( -1.000000000000000000, 0.000000000000000000, 0.000000000000000000 ) ) ;
#6907=AXIS2_PLACEMENT_3D ( 'NONE', #16205, #1068, #20957 ) ;
#6911=ORIENTED_EDGE ( 'NONE', *, *, #9054, .T. ) ;
#6914=LINE ( 'NONE', #21820, #7576 ) ;
#6915=CARTESIAN_POINT ( 'NONE',  ( 0.000000000000000000, 24.73395913766463750, 12.01774797440586084 ) ) ;
#6922=AXIS2_PLACEMENT_3D ( 'NONE', #9766, #4692, #9882 ) ;
#6927=DIRECTION ( 'NONE',  ( 0.000000000000000000, 0.000000000000000000, 1.000000000000000000 ) ) ;
#6929=VECTOR ( 'NONE', #20503, 1000.000000000000000 ) ;
#6936=ORIENTED_EDGE ( 'NONE', *, *, #21606, .F. ) ;
#6946=CARTESIAN_POINT ( 'NONE',  ( 0.000000000000000000, 26.69209308833507777, 6.612652082459410607 ) ) ;
#6951=AXIS2_PLACEMENT_3D ( 'NONE', #13143, #19890, #18249 ) ;
#6959=ORIENTED_EDGE ( 'NONE', *, *, #6475, .F. ) ;
#6961=ORIENTED_EDGE ( 'NONE', *, *, #7423, .T. ) ;
#6969=CARTESIAN_POINT ( 'NONE',  ( 10.00000000000000000, 0.000000000000000000, 0.000000000000000000 ) ) ;
#6982=EDGE_LOOP ( 'NONE', ( #1697, #20377, #18611, #15913 ) ) ;
#6983=ORIENTED_EDGE ( 'NONE', *, *, #11908, .F. ) ;
#6997=DIRECTION ( 'NONE',  ( -1.000000000000000000, 0.000000000000000000, -0.000000000000000000 ) ) ;
#6999=AXIS2_PLACEMENT_3D ( 'NONE', #8426, #15153, #27 ) ;
#7003=ORIENTED_EDGE ( 'NONE', *, *, #9162, .T. ) ;
#7009=EDGE_LOOP ( 'NONE', ( #11576, #9675, #6348, #15047 ) ) ;
#7011=EDGE_LOOP ( 'NONE', ( #20829, #7621, #16237, #9192 ) ) ;
#7013=ORIENTED_EDGE ( 'NONE', *, *, #944, .F. ) ;
#7018=CARTESIAN_POINT ( 'NONE',  ( 5.000000000000000888, -13.56333590713994575, -28.98337314858449076 ) ) ;
#7031=CARTESIAN_POINT ( 'NONE',  ( 10.00000000000000000, -24.73395913766455578, -12.01774797440602427 ) ) ;
#7033=CIRCLE ( 'NONE', #15844, 3.000000000000000444 ) ;
#7034=CIRCLE ( 'NONE', #1746, 12.00000000000000000 ) ;
#7038=CARTESIAN_POINT ( 'NONE',  ( 0.000000000000000000, 21.69483248597422076, 16.89761061231787309 ) ) ;
#7053=CARTESIAN_POINT ( 'NONE',  ( 10.00000000000000000, 9.992993448021948666, -26.36019881529875519 ) ) ;
#7054=AXIS2_PLACEMENT_3D ( 'NONE', #3273, #11888, #3385 ) ;
#7057=LINE ( 'NONE', #20425, #234 ) ;
#7069=VECTOR ( 'NONE', #15602, 1000.000000000000000 ) ;
#7070=CARTESIAN_POINT ( 'NONE',  ( 0.000000000000000000, -18.31866948046748078, -26.23788002993743262 ) ) ;
#7073=ORIENTED_EDGE ( 'NONE', *, *, #16128, .T. ) ;
#7079=CARTESIAN_POINT ( 'NONE',  ( 10.00000000000000000, 15.25521607131237722, -23.70650506194154872 ) ) ;
#7080=CARTESIAN_POINT ( 'NONE',  ( 5.000000000000000000, -12.46320060045744071, 29.47318494484024853 ) ) ;
#7084=DIRECTION ( 'NONE',  ( -1.000000000000000000, 0.000000000000000000, 0.000000000000000000 ) ) ;
#7090=ADVANCED_FACE ( 'NONE', ( #19705 ), #2807, .T. ) ;
#7091=DIRECTION ( 'NONE',  ( 0.000000000000000000, 0.9510565162951523099, 0.3090169943749512260 ) ) ;
#7093=EDGE_CURVE ( 'NONE', #11653, #17995, #18527, .T. ) ;
#7098=AXIS2_PLACEMENT_3D ( 'NONE', #18908, #353, #451 ) ;
#7100=LINE ( 'NONE', #17362, #14052 ) ;
#7102=CARTESIAN_POINT ( 'NONE',  ( 10.00000000000000000, 0.000000000000000000, 0.000000000000000000 ) ) ;
#7103=CARTESIAN_POINT ( 'NONE',  ( 10.00000000000000000, 25.17124263951009411, 12.69364185792227495 ) ) ;
#7114=CARTESIAN_POINT ( 'NONE',  ( 10.00000000000000888, 4.000000000000000000, 1.000000000000000000 ) ) ;
#7128=DIRECTION ( 'NONE',  ( -1.000000000000000000, 0.000000000000000000, -0.000000000000000000 ) ) ;
#7131=DIRECTION ( 'NONE',  ( 0.000000000000000000, 0.000000000000000000, 1.000000000000000000 ) ) ;
#7132=ORIENTED_EDGE ( 'NONE', *, *, #13274, .F. ) ;
#7133=CARTESIAN_POINT ( 'NONE',  ( 10.00000000000000000, 17.70753755129066320, -21.03896658273954046 ) ) ;
#7134=CARTESIAN_POINT ( 'NONE',  ( 10.00000000000000000, 14.53731623274961571, -23.34226719384889748 ) ) ;
#7135=VERTEX_POINT ( 'NONE', #1255 ) ;
#7136=EDGE_CURVE ( 'NONE', #2434, #9160, #7938, .T. ) ;
#7137=ORIENTED_EDGE ( 'NONE', *, *, #9915, .T. ) ;
#7142=CARTESIAN_POINT ( 'NONE',  ( 5.000000000000000000, -23.37352460145268651, -21.85585385440903750 ) ) ;
#7144=DIRECTION ( 'NONE',  ( -1.000000000000000000, -0.000000000000000000, -0.000000000000000000 ) ) ;
#7149=CARTESIAN_POINT ( 'NONE',  ( 0.000000000000000000, 31.75612719289740937, 3.943144139962659445 ) ) ;
#7154=EDGE_CURVE ( 'NONE', #15205, #9318, #11410, .T. ) ;
#7155=EDGE_CURVE ( 'NONE', #16266, #10715, #16498, .T. ) ;
#7163=DIRECTION ( 'NONE',  ( -1.000000000000000000, 0.000000000000000000, 0.000000000000000000 ) ) ;
#7177=CARTESIAN_POINT ( 'NONE',  ( 0.000000000000000000, 27.26034713664097353, -7.182859710736244629 ) ) ;
#7185=CYLINDRICAL_SURFACE ( 'NONE', #8698, 32.00000000000000000 ) ;
#7187=ORIENTED_EDGE ( 'NONE', *, *, #2457, .F. ) ;
#7188=EDGE_CURVE ( 'NONE', #11274, #19400, #10746, .T. ) ;
#7189=ORIENTED_EDGE ( 'NONE', *, *, #19225, .T. ) ;
#7190=CIRCLE ( 'NONE', #19532, 27.49900000000000233 ) ;
#7191=ORIENTED_EDGE ( 'NONE', *, *, #4332, .F. ) ;
#7193=CIRCLE ( 'NONE', #123, 11.99999999999999822 ) ;
#7198=CIRCLE ( 'NONE', #13549, 27.49900000000000233 ) ;
#7203=CIRCLE ( 'NONE', #13177, 32.00000000000000000 ) ;
#7208=AXIS2_PLACEMENT_3D ( 'NONE', #13750, #9980, #11660 ) ;
#7210=DIRECTION ( 'NONE',  ( 0.000000000000000000, -6.982962677686266711E-15, 1.000000000000000000 ) ) ;
#7213=VERTEX_POINT ( 'NONE', #344 ) ;
#7216=DIRECTION ( 'NONE',  ( 0.000000000000000000, -0.5877852522924632561, -0.8090169943749546677 ) ) ;
#7231=AXIS2_PLACEMENT_3D ( 'NONE', #8170, #14899, #20101 ) ;
#7234=AXIS2_PLACEMENT_3D ( 'NONE', #19977, #10018, #1636 ) ;
#7246=DIRECTION ( 'NONE',  ( -1.000000000000000000, 0.000000000000000000, -0.000000000000000000 ) ) ;
#7254=AXIS2_PLACEMENT_3D ( 'NONE', #12485, #13936, #680 ) ;
#7255=ORIENTED_EDGE ( 'NONE', *, *, #15632, .F. ) ;
#7260=LINE ( 'NONE', #7373, #147 ) ;
#7262=ADVANCED_FACE ( 'NONE', ( #13704 ), #18786, .T. ) ;
#7267=DIRECTION ( 'NONE',  ( 0.000000000000000000, 0.000000000000000000, 1.000000000000000000 ) ) ;
#7268=VECTOR ( 'NONE', #7890, 1000.000000000000000 ) ;
#7270=EDGE_CURVE ( 'NONE', #8974, #4047, #1922, .T. ) ;
#7280=VERTEX_POINT ( 'NONE', #3865 ) ;
#7295=CARTESIAN_POINT ( 'NONE',  ( -10.00000000000000000, 0.000000000000000000, 0.000000000000000000 ) ) ;
#7300=AXIS2_PLACEMENT_3D ( 'NONE', #3100, #6096, #17918 ) ;
#7305=ORIENTED_EDGE ( 'NONE', *, *, #14080, .F. ) ;
#7308=ORIENTED_EDGE ( 'NONE', *, *, #7707, .T. ) ;
#7310=CARTESIAN_POINT ( 'NONE',  ( 0.000000000000000000, 1.959304526717801975, 27.42911093658675981 ) ) ;
#7325=DIRECTION ( 'NONE',  ( 0.000000000000000000, 0.000000000000000000, 1.000000000000000000 ) ) ;
#7338=DIRECTION ( 'NONE',  ( -1.000000000000000000, -0.000000000000000000, -0.000000000000000000 ) ) ;
#7344=DIRECTION ( 'NONE',  ( 0.000000000000000000, -6.938893903907230744E-15, 1.000000000000000000 ) ) ;
#7345=AXIS2_PLACEMENT_3D ( 'NONE', #17275, #11746, #20693 ) ;
#7350=CARTESIAN_POINT ( 'NONE',  ( 0.000000000000000000, 27.40684453873966575, 16.51862198942017557 ) ) ;
#7356=FACE_OUTER_BOUND ( 'NONE', #3356, .T. ) ;
#7362=CARTESIAN_POINT ( 'NONE',  ( 0.000000000000000000, -7.409634587002906336, -27.19958299168165183 ) ) ;
#7369=EDGE_LOOP ( 'NONE', ( #10759, #15540, #18537, #4319 ) ) ;
#7373=CARTESIAN_POINT ( 'NONE',  ( 10.00000000000000000, 28.15804365424197186, 10.64184787299392454 ) ) ;
#7374=CARTESIAN_POINT ( 'NONE',  ( -140.0000508000000536, 2.828427124746190291, -1.000000000000000000 ) ) ;
#7377=FACE_OUTER_BOUND ( 'NONE', #13302, .T. ) ;
#7382=CIRCLE ( 'NONE', #4918, 12.00000000000000000 ) ;
#7392=ORIENTED_EDGE ( 'NONE', *, *, #18412, .T. ) ;
#7394=AXIS2_PLACEMENT_3D ( 'NONE', #9902, #17307, #12528 ) ;
#7405=FACE_OUTER_BOUND ( 'NONE', #882, .T. ) ;
#7411=EDGE_CURVE ( 'NONE', #16782, #7213, #16045, .T. ) ;
#7417=VERTEX_POINT ( 'NONE', #2859 ) ;
#7421=CARTESIAN_POINT ( 'NONE',  ( 10.00000000000000000, -9.366510754379408610, 25.85466064925422458 ) ) ;
#7423=EDGE_CURVE ( 'NONE', #11372, #16515, #8641, .T. ) ;
#7433=ADVANCED_FACE ( 'NONE', ( #11147 ), #17896, .T. ) ;
#7442=CARTESIAN_POINT ( 'NONE',  ( 0.000000000000000000, 0.000000000000000000, 0.000000000000000000 ) ) ;
#7446=EDGE_CURVE ( 'NONE', #9701, #16531, #19502, .T. ) ;
#7448=LINE ( 'NONE', #4130, #21106 ) ;
#7454=CYLINDRICAL_SURFACE ( 'NONE', #17567, 11.99999999999999822 ) ;
#7455=DIRECTION ( 'NONE',  ( -1.000000000000000000, 0.000000000000000000, 0.000000000000000000 ) ) ;
#7460=ORIENTED_EDGE ( 'NONE', *, *, #11908, .T. ) ;
#7463=DIRECTION ( 'NONE',  ( -1.000000000000000000, -0.000000000000000000, -0.000000000000000000 ) ) ;
#7466=VERTEX_POINT ( 'NONE', #18105 ) ;
#7477=CARTESIAN_POINT ( 'NONE',  ( 5.000000000000000888, -30.61448696004458725, 9.314139153634121371 ) ) ;
#7485=AXIS2_PLACEMENT_3D ( 'NONE', #16142, #12490, #11170 ) ;
#7487=LINE ( 'NONE', #20962, #17615 ) ;
#7494=ORIENTED_EDGE ( 'NONE', *, *, #21076, .F. ) ;
#7496=AXIS2_PLACEMENT_3D ( 'NONE', #7102, #13935, #15484 ) ;
#7508=VERTEX_POINT ( 'NONE', #8490 ) ;
#7510=ORIENTED_EDGE ( 'NONE', *, *, #1428, .F. ) ;
#7516=DIRECTION ( 'NONE',  ( -1.000000000000000000, 0.000000000000000000, 0.000000000000000000 ) ) ;
#7522=FACE_OUTER_BOUND ( 'NONE', #8219, .T. ) ;
#7531=DIRECTION ( 'NONE',  ( -1.000000000000000000, 0.000000000000000000, 0.000000000000000000 ) ) ;
#7541=ORIENTED_EDGE ( 'NONE', *, *, #11673, .F. ) ;
#7561=DIRECTION ( 'NONE',  ( 1.000000000000000000, 0.000000000000000000, 0.000000000000000000 ) ) ;
#7572=CARTESIAN_POINT ( 'NONE',  ( -140.0000508000000536, 2.828427124746190291, 1.000000000000000000 ) ) ;
#7575=ORIENTED_EDGE ( 'NONE', *, *, #2444, .T. ) ;
#7576=VECTOR ( 'NONE', #3367, 1000.000000000000000 ) ;
#7577=EDGE_CURVE ( 'NONE', #8085, #2294, #8167, .T. ) ;
#7579=DIRECTION ( 'NONE',  ( -1.000000000000000000, -0.000000000000000000, -0.000000000000000000 ) ) ;
#7582=EDGE_CURVE ( 'NONE', #2434, #10630, #19850, .T. ) ;
#7596=ORIENTED_EDGE ( 'NONE', *, *, #12871, .F. ) ;
#7604=CARTESIAN_POINT ( 'NONE',  ( 10.00000000000000000, -25.48117629651196125, 10.33947075754252332 ) ) ;
#7608=DIRECTION ( 'NONE',  ( -1.000000000000000000, -0.000000000000000000, 0.000000000000000000 ) ) ;
#7610=AXIS2_PLACEMENT_3D ( 'NONE', #1467, #14731, #3231 ) ;
#7611=CIRCLE ( 'NONE', #15359, 12.00000000000000000 ) ;
#7621=ORIENTED_EDGE ( 'NONE', *, *, #12260, .F. ) ;
#7625=ORIENTED_EDGE ( 'NONE', *, *, #21606, .T. ) ;
#7628=EDGE_CURVE ( 'NONE', #17995, #15667, #11744, .T. ) ;
#7629=ORIENTED_EDGE ( 'NONE', *, *, #15542, .T. ) ;
#7642=CARTESIAN_POINT ( 'NONE',  ( 10.00000000000000000, 0.000000000000000000, 0.000000000000000000 ) ) ;
#7644=DIRECTION ( 'NONE',  ( 0.000000000000000000, 0.000000000000000000, 1.000000000000000000 ) ) ;
#7654=ORIENTED_EDGE ( 'NONE', *, *, #10199, .F. ) ;
#7657=LINE ( 'NONE', #2677, #1882 ) ;
#7658=ORIENTED_EDGE ( 'NONE', *, *, #15237, .F. ) ;
#7662=CARTESIAN_POINT ( 'NONE',  ( 5.000000000000000888, 0.6021240089805670603, -31.99433460282943997 ) ) ;
#7666=CARTESIAN_POINT ( 'NONE',  ( 0.000000000000000000, 22.77465461094694632, -15.41136296218063428 ) ) ;
#7667=DIRECTION ( 'NONE',  ( -1.000000000000000000, -0.000000000000000000, 0.000000000000000000 ) ) ;
#7670=EDGE_LOOP ( 'NONE', ( #11705, #3604, #9537, #14442 ) ) ;
#7671=AXIS2_PLACEMENT_3D ( 'NONE', #4135, #7455, #9529 ) ;
#7672=DIRECTION ( 'NONE',  ( -1.000000000000000000, 0.000000000000000000, 0.000000000000000000 ) ) ;
#7676=EDGE_CURVE ( 'NONE', #289, #2742, #3276, .T. ) ;
#7687=ADVANCED_FACE ( 'NONE', ( #3728 ), #16992, .T. ) ;
#7689=CARTESIAN_POINT ( 'NONE',  ( 10.00000000000000000, 31.88200538760793634, 2.745493118647100772 ) ) ;
#7700=CARTESIAN_POINT ( 'NONE',  ( 10.00000000000000000, 0.000000000000000000, 0.000000000000000000 ) ) ;
#7704=ORIENTED_EDGE ( 'NONE', *, *, #21592, .T. ) ;
#7707=EDGE_CURVE ( 'NONE', #10823, #14878, #4320, .T. ) ;
#7709=VERTEX_POINT ( 'NONE', #7149 ) ;
#7713=EDGE_CURVE ( 'NONE', #14091, #8622, #16679, .T. ) ;
#7716=CARTESIAN_POINT ( 'NONE',  ( 10.00000000000000000, -12.94633825542284278, 24.26081875733330406 ) ) ;
#7717=VERTEX_POINT ( 'NONE', #8591 ) ;
#7720=CARTESIAN_POINT ( 'NONE',  ( 0.000000000000000000, -21.69483248597410707, -16.89761061231802586 ) ) ;
#7721=FACE_OUTER_BOUND ( 'NONE', #44, .T. ) ;
#7724=AXIS2_PLACEMENT_3D ( 'NONE', #9389, #19131, #3994 ) ;
#7729=DIRECTION ( 'NONE',  ( -1.000000000000000000, 0.000000000000000000, 0.000000000000000000 ) ) ;
#7730=ADVANCED_FACE ( 'NONE', ( #15548 ), #3839, .T. ) ;
#7731=CARTESIAN_POINT ( 'NONE',  ( 0.000000000000000000, 0.000000000000000000, 0.000000000000000000 ) ) ;
#7734=ORIENTED_EDGE ( 'NONE', *, *, #18697, .T. ) ;
#7747=DIRECTION ( 'NONE',  ( -1.000000000000000000, 0.000000000000000000, 0.000000000000000000 ) ) ;
#7748=VECTOR ( 'NONE', #404, 1000.000000000000000 ) ;
#7750=DIRECTION ( 'NONE',  ( -1.000000000000000000, 0.000000000000000000, 0.000000000000000000 ) ) ;
#7751=DIRECTION ( 'NONE',  ( 0.000000000000000000, 0.000000000000000000, 1.000000000000000000 ) ) ;
#7754=CIRCLE ( 'NONE', #20458, 12.00000000000000178 ) ;
#7756=CARTESIAN_POINT ( 'NONE',  ( 5.000000000000000000, 0.6021240089801385142, 31.99433460282945063 ) ) ;
#7758=DIRECTION ( 'NONE',  ( 0.000000000000000000, 0.000000000000000000, 1.000000000000000000 ) ) ;
#7762=ADVANCED_BREP_SHAPE_REPRESENTATION ( '', ( #13088, #15567 ), #19439 ) ;
#7765=CARTESIAN_POINT ( 'NONE',  ( 10.00000000000000000, -26.27606311335944511, -10.21217444509438188 ) ) ;
#7770=VERTEX_POINT ( 'NONE', #6586 ) ;
#7775=VERTEX_POINT ( 'NONE', #11978 ) ;
#7777=DIRECTION ( 'NONE',  ( -1.000000000000000000, -0.000000000000000000, 0.000000000000000000 ) ) ;
#7779=CARTESIAN_POINT ( 'NONE',  ( 0.000000000000000000, -25.17124263951018293, 12.69364185792209909 ) ) ;
#7787=ORIENTED_EDGE ( 'NONE', *, *, #19896, .F. ) ;
#7788=CARTESIAN_POINT ( 'NONE',  ( 10.00000000000000000, -30.61448696004458370, 9.314139153634121371 ) ) ;
#7792=VERTEX_POINT ( 'NONE', #50 ) ;
#7793=VERTEX_POINT ( 'NONE', #16724 ) ;
#7798=ORIENTED_EDGE ( 'NONE', *, *, #18556, .F. ) ;
#7799=DIRECTION ( 'NONE',  ( -1.000000000000000000, -0.000000000000000000, -0.000000000000000000 ) ) ;
#7809=ADVANCED_FACE ( 'NONE', ( #18726 ), #17059, .T. ) ;
#7814=ORIENTED_EDGE ( 'NONE', *, *, #10385, .F. ) ;
#7815=DIRECTION ( 'NONE',  ( 0.000000000000000000, -0.9510565162951502005, -0.3090169943749575543 ) ) ;
#7822=FACE_OUTER_BOUND ( 'NONE', #7011, .T. ) ;
#7826=EDGE_CURVE ( 'NONE', #3440, #8227, #18470, .T. ) ;
#7832=DIRECTION ( 'NONE',  ( -1.000000000000000000, 0.000000000000000000, 0.000000000000000000 ) ) ;
#7833=ORIENTED_EDGE ( 'NONE', *, *, #7154, .T. ) ;
#7859=AXIS2_PLACEMENT_3D ( 'NONE', #6969, #8725, #648 ) ;
#7860=EDGE_LOOP ( 'NONE', ( #6961, #14275 ) ) ;
#7861=AXIS2_PLACEMENT_3D ( 'NONE', #2076, #1852, #13675 ) ;
#7870=ORIENTED_EDGE ( 'NONE', *, *, #29, .F. ) ;
#7877=CARTESIAN_POINT ( 'NONE',  ( 10.00000000000000000, -25.48117629651182270, -10.33947075754286793 ) ) ;
#7878=DIRECTION ( 'NONE',  ( 0.000000000000000000, 0.000000000000000000, 1.000000000000000000 ) ) ;
#7881=CARTESIAN_POINT ( 'NONE',  ( 10.00000000000000000, 6.063030049135075039, 31.42037024962127134 ) ) ;
#7886=LINE ( 'NONE', #14403, #11947 ) ;
#7887=DIRECTION ( 'NONE',  ( -1.000000000000000000, 0.000000000000000000, 0.000000000000000000 ) ) ;
#7890=DIRECTION ( 'NONE',  ( 1.000000000000000000, -0.000000000000000000, -0.000000000000000000 ) ) ;
#7895=CARTESIAN_POINT ( 'NONE',  ( 10.00000000000000000, 0.000000000000000000, 0.000000000000000000 ) ) ;
#7896=ORIENTED_EDGE ( 'NONE', *, *, #20433, .F. ) ;
#7898=SURFACE_STYLE_USAGE ( .BOTH. , #4361 ) ;
#7900=EDGE_LOOP ( 'NONE', ( #424, #6643, #20073, #1715 ) ) ;
#7901=ORIENTED_EDGE ( 'NONE', *, *, #6517, .F. ) ;
#7902=DIRECTION ( 'NONE',  ( -1.000000000000000000, 0.000000000000000000, -0.000000000000000000 ) ) ;
#7904=EDGE_LOOP ( 'NONE', ( #8313, #13463, #13974, #18147 ) ) ;
#7907=CYLINDRICAL_SURFACE ( 'NONE', #11807, 11.99999999999999822 ) ;
#7933=DIRECTION ( 'NONE',  ( 0.000000000000000000, 0.000000000000000000, 1.000000000000000000 ) ) ;
#7934=DIRECTION ( 'NONE',  ( 0.000000000000000000, 0.000000000000000000, 1.000000000000000000 ) ) ;
#7935=CARTESIAN_POINT ( 'NONE',  ( 10.00000000000000000, 1.592605004253184964, -28.14575649959892445 ) ) ;
#7938=CIRCLE ( 'NONE', #8976, 11.99999999999999645 ) ;
#7939=CARTESIAN_POINT ( 'NONE',  ( 0.000000000000000000, -27.26034713664092379, -7.182859710736426706 ) ) ;
#7943=DIRECTION ( 'NONE',  ( 0.000000000000000000, 0.4067366430758010409, -0.9135454576426005335 ) ) ;
#7946=CIRCLE ( 'NONE', #12502, 11.99999999999999822 ) ;
#7950=ORIENTED_EDGE ( 'NONE', *, *, #423, .F. ) ;
#7951=ORIENTED_EDGE ( 'NONE', *, *, #17163, .F. ) ;
#7968=AXIS2_PLACEMENT_3D ( 'NONE', #1229, #7972, #4318 ) ;
#7970=AXIS2_PLACEMENT_3D ( 'NONE', #4250, #7672, #14406 ) ;
#7972=DIRECTION ( 'NONE',  ( -1.000000000000000000, -0.000000000000000000, -0.000000000000000000 ) ) ;
#7978=ADVANCED_FACE ( 'NONE', ( #592 ), #5781, .T. ) ;
#7980=EDGE_CURVE ( 'NONE', #5374, #17052, #20235, .T. ) ;
#7992=CARTESIAN_POINT ( 'NONE',  ( 10.00000000000000000, -21.98203405400942856, -17.64965094506566246 ) ) ;
#7998=CARTESIAN_POINT ( 'NONE',  ( 0.000000000000000000, -1.592605004252595213, -28.14575649959895998 ) ) ;
#7999=DIRECTION ( 'NONE',  ( 0.000000000000000000, 0.000000000000000000, 1.000000000000000000 ) ) ;
#8012=FILL_AREA_STYLE ('',( #933 ) ) ;
#8014=ADVANCED_FACE ( 'NONE', ( #17382 ), #18827, .T. ) ;
#8017=DIRECTION ( 'NONE',  ( -1.000000000000000000, 0.000000000000000000, 0.000000000000000000 ) ) ;
#8021=DIRECTION ( 'NONE',  ( -1.000000000000000000, 0.000000000000000000, 0.000000000000000000 ) ) ;
#8022=FACE_BOUND ( 'NONE', #19747, .T. ) ;
#8030=EDGE_CURVE ( 'NONE', #11017, #21218, #4331, .T. ) ;
#8031=CARTESIAN_POINT ( 'NONE',  ( 10.00000000000000000, -27.48365448817206058, -0.9185515634844814148 ) ) ;
#8035=EDGE_CURVE ( 'NONE', #2943, #428, #20937, .T. ) ;
#8040=AXIS2_PLACEMENT_3D ( 'NONE', #817, #7561, #14295 ) ;
#8043=VECTOR ( 'NONE', #14460, 1000.000000000000000 ) ;
#8050=DIRECTION ( 'NONE',  ( -1.000000000000000000, 0.000000000000000000, 0.000000000000000000 ) ) ;
#8057=CARTESIAN_POINT ( 'NONE',  ( 0.000000000000000000, -31.88200538760792213, -2.745493118647326369 ) ) ;
#8059=AXIS2_PLACEMENT_3D ( 'NONE', #19729, #21821, #6480 ) ;
#8064=CARTESIAN_POINT ( 'NONE',  ( 10.00000000000000000, 19.07277123396568896, -19.80970465344728737 ) ) ;
#8070=AXIS2_PLACEMENT_3D ( 'NONE', #6771, #5186, #11919 ) ;
#8071=ORIENTED_EDGE ( 'NONE', *, *, #18556, .T. ) ;
#8077=DIRECTION ( 'NONE',  ( -1.000000000000000000, 0.000000000000000000, -0.000000000000000000 ) ) ;
#8085=VERTEX_POINT ( 'NONE', #11296 ) ;
#8086=PRODUCT ( 'spur gear_iso_ISO - Spur gear 2M 30T 20PA 10FW ---S30B10H150L6.0S1', 'spur gear_iso_ISO - Spur gear 2M 30T 20PA 10FW ---S30B10H150L6.0S1', '', ( #3555 ) ) ;
#8092=CARTESIAN_POINT ( 'NONE',  ( 10.00000000000000000, 27.48365448817206769, -0.9185515634842869037 ) ) ;
#8094=DIRECTION ( 'NONE',  ( -1.000000000000000000, 0.000000000000000000, 0.000000000000000000 ) ) ;
#8095=ORIENTED_EDGE ( 'NONE', *, *, #13959, .T. ) ;
#8098=AXIS2_PLACEMENT_3D ( 'NONE', #1421, #18435, #18002 ) ;
#8100=ORIENTED_EDGE ( 'NONE', *, *, #207, .T. ) ;
#8101=CARTESIAN_POINT ( 'NONE',  ( 0.000000000000000000, 6.123233995736766282E-16, 5.000000000000000000 ) ) ;
#8105=CARTESIAN_POINT ( 'NONE',  ( 0.000000000000000000, 4.294029059349855793, 27.86182539015968018 ) ) ;
#8109=CARTESIAN_POINT ( 'NONE',  ( 0.000000000000000000, -27.48365448817207479, 0.9185515634840949462 ) ) ;
#8124=EDGE_CURVE ( 'NONE', #19281, #10630, #7657, .T. ) ;
#8125=VERTEX_POINT ( 'NONE', #14503 ) ;
#8126=DIRECTION ( 'NONE',  ( -1.000000000000000000, 0.000000000000000000, 0.000000000000000000 ) ) ;
#8129=CYLINDRICAL_SURFACE ( 'NONE', #6160, 11.99999999999999645 ) ;
#8130=DIRECTION ( 'NONE',  ( -1.000000000000000000, -0.000000000000000000, -0.000000000000000000 ) ) ;
#8131=ORIENTED_EDGE ( 'NONE', *, *, #16764, .T. ) ;
#8137=CARTESIAN_POINT ( 'NONE',  ( -10.00000000000000000, 0.000000000000000000, 0.000000000000000000 ) ) ;
#8147=EDGE_LOOP ( 'NONE', ( #20742, #1420, #17739, #3319 ) ) ;
#8152=CARTESIAN_POINT ( 'NONE',  ( 10.00000000000000000, 0.000000000000000000, 0.000000000000000000 ) ) ;
#8154=ORIENTED_EDGE ( 'NONE', *, *, #3439, .F. ) ;
#8156=LINE ( 'NONE', #4720, #4052 ) ;
#8162=DIRECTION ( 'NONE',  ( -1.000000000000000000, 0.000000000000000000, 0.000000000000000000 ) ) ;
#8167=LINE ( 'NONE', #14896, #20221 ) ;
#8170=CARTESIAN_POINT ( 'NONE',  ( 10.00000000000000000, 0.000000000000000000, 0.000000000000000000 ) ) ;
#8174=EDGE_LOOP ( 'NONE', ( #18210, #2921, #19286, #16676 ) ) ;
#8175=VERTEX_POINT ( 'NONE', #8581 ) ;
#8182=DIRECTION ( 'NONE',  ( -1.000000000000000000, 0.000000000000000000, -0.000000000000000000 ) ) ;
#8191=ORIENTED_EDGE ( 'NONE', *, *, #11496, .T. ) ;
#8196=ORIENTED_EDGE ( 'NONE', *, *, #9538, .F. ) ;
#8205=DIRECTION ( 'NONE',  ( -1.000000000000000000, 0.000000000000000000, 0.000000000000000000 ) ) ;
#8209=DIRECTION ( 'NONE',  ( 0.000000000000000000, -0.5877852522924799095, 0.8090169943749425663 ) ) ;
#8210=DIRECTION ( 'NONE',  ( -1.000000000000000000, 0.000000000000000000, 0.000000000000000000 ) ) ;
#8219=EDGE_LOOP ( 'NONE', ( #16980, #14570, #5845, #16492 ) ) ;
#8223=CARTESIAN_POINT ( 'NONE',  ( 10.00000000000000000, 0.000000000000000000, 0.000000000000000000 ) ) ;
#8224=CIRCLE ( 'NONE', #15628, 27.49900000000000944 ) ;
#8226=ADVANCED_FACE ( 'NONE', ( #11899 ), #13553, .T. ) ;
#8227=VERTEX_POINT ( 'NONE', #1737 ) ;
#8240=CYLINDRICAL_SURFACE ( 'NONE', #6214, 27.49900000000000233 ) ;
#8243=CARTESIAN_POINT ( 'NONE',  ( 10.00000000000000000, 23.37352460145313060, -21.85585385440855433 ) ) ;
#8253=ORIENTED_EDGE ( 'NONE', *, *, #12112, .F. ) ;
#8258=CARTESIAN_POINT ( 'NONE',  ( 5.000000000000000888, -30.61448696004446290, -9.314139153634542367 ) ) ;
#8260=CARTESIAN_POINT ( 'NONE',  ( 10.00000000000000000, 19.07277123396541185, 19.80970465344755027 ) ) ;
#8261=CIRCLE ( 'NONE', #1552, 27.49900000000000233 ) ;
#8262=ADVANCED_FACE ( 'NONE', ( #12106 ), #18857, .T. ) ;
#8270=CARTESIAN_POINT ( 'NONE',  ( 0.000000000000000000, -12.90282758292962662, -25.06465718894790484 ) ) ;
#8273=DIRECTION ( 'NONE',  ( -1.000000000000000000, 0.000000000000000000, 0.000000000000000000 ) ) ;
#8274=EDGE_CURVE ( 'NONE', #16260, #910, #7190, .T. ) ;
#8277=CIRCLE ( 'NONE', #4391, 32.00000000000000000 ) ;
#8287=VECTOR ( 'NONE', #3020, 1000.000000000000000 ) ;
#8288=EDGE_CURVE ( 'NONE', #16396, #9611, #12817, .T. ) ;
#8297=CARTESIAN_POINT ( 'NONE',  ( 5.000000000000000000, 24.17932380791746994, -20.96092317126981186 ) ) ;
#8301=DIRECTION ( 'NONE',  ( -1.000000000000000000, 0.000000000000000000, 0.000000000000000000 ) ) ;
#8303=EDGE_LOOP ( 'NONE', ( #14358, #9941, #7013, #19909 ) ) ;
#8305=CIRCLE ( 'NONE', #12516, 11.99999999999999822 ) ;
#8307=ORIENTED_EDGE ( 'NONE', *, *, #11503, .F. ) ;
#8313=ORIENTED_EDGE ( 'NONE', *, *, #15167, .T. ) ;
#8320=CIRCLE ( 'NONE', #4418, 12.00000000000000178 ) ;
#8329=LINE ( 'NONE', #4582, #15803 ) ;
#8330=CARTESIAN_POINT ( 'NONE',  ( 0.000000000000000000, 0.000000000000000000, 0.000000000000000000 ) ) ;
#8334=ORIENTED_EDGE ( 'NONE', *, *, #21341, .T. ) ;
#8335=MECHANICAL_DESIGN_GEOMETRIC_PRESENTATION_REPRESENTATION('',(#17869),#13976);
#8336=CIRCLE ( 'NONE', #12212, 32.00000000000000000 ) ;
#8344=CARTESIAN_POINT ( 'NONE',  ( 10.00000000000000000, 31.88200538760793634, -2.745493118647100772 ) ) ;
#8350=AXIS2_PLACEMENT_3D ( 'NONE', #21309, #6188, #12911 ) ;
#8354=EDGE_CURVE ( 'NONE', #10634, #4641, #731, .T. ) ;
#8360=ORIENTED_EDGE ( 'NONE', *, *, #15860, .T. ) ;
#8362=DIRECTION ( 'NONE',  ( -1.000000000000000000, -0.000000000000000000, -0.000000000000000000 ) ) ;
#8363=VECTOR ( 'NONE', #8409, 1000.000000000000000 ) ;
#8364=ORIENTED_EDGE ( 'NONE', *, *, #19225, .F. ) ;
#8382=DIRECTION ( 'NONE',  ( -1.000000000000000000, 0.000000000000000000, -0.000000000000000000 ) ) ;
#8400=ORIENTED_EDGE ( 'NONE', *, *, #3439, .T. ) ;
#8403=CIRCLE ( 'NONE', #20746, 11.99999999999999822 ) ;
#8409=DIRECTION ( 'NONE',  ( -1.000000000000000000, -0.000000000000000000, 0.000000000000000000 ) ) ;
#8420=VERTEX_POINT ( 'NONE', #619 ) ;
#8422=ORIENTED_EDGE ( 'NONE', *, *, #5120, .T. ) ;
#8423=VERTEX_POINT ( 'NONE', #7572 ) ;
#8426=CARTESIAN_POINT ( 'NONE',  ( 0.000000000000000000, 0.000000000000000000, 0.000000000000000000 ) ) ;
#8431=CARTESIAN_POINT ( 'NONE',  ( 10.00000000000000000, -21.69483248597410707, -16.89761061231802586 ) ) ;
#8432=DIRECTION ( 'NONE',  ( -1.000000000000000000, 0.000000000000000000, 0.000000000000000000 ) ) ;
#8434=CARTESIAN_POINT ( 'NONE',  ( 10.00000000000000000, 27.07404830566971299, 4.815694066514526028 ) ) ;
#8445=AXIS2_PLACEMENT_3D ( 'NONE', #1513, #6506, #19973 ) ;
#8449=AXIS2_PLACEMENT_3D ( 'NONE', #4945, #18426, #5162 ) ;
#8456=CYLINDRICAL_SURFACE ( 'NONE', #7208, 27.49900000000000233 ) ;
#8460=DIRECTION ( 'NONE',  ( -1.000000000000000000, 0.000000000000000000, 0.000000000000000000 ) ) ;
#8461=CARTESIAN_POINT ( 'NONE',  ( 0.000000000000000000, -4.294029059350045863, 27.86182539015965176 ) ) ;
#8465=AXIS2_PLACEMENT_3D ( 'NONE', #1357, #14395, #7878 ) ;
#8485=DIRECTION ( 'NONE',  ( 0.000000000000000000, 0.000000000000000000, 1.000000000000000000 ) ) ;
#8486=EDGE_CURVE ( 'NONE', #14805, #7717, #10362, .T. ) ;
#8489=LINE ( 'NONE', #11909, #11201 ) ;
#8490=CARTESIAN_POINT ( 'NONE',  ( 10.00000000000000000, 30.61448696004464409, -9.314139153633922419 ) ) ;
#8494=CIRCLE ( 'NONE', #18733, 27.49900000000000588 ) ;
#8495=CARTESIAN_POINT ( 'NONE',  ( 0.000000000000000000, 21.98203405400978383, -17.64965094506522192 ) ) ;
#8498=ORIENTED_EDGE ( 'NONE', *, *, #7707, .F. ) ;
#8500=ORIENTED_EDGE ( 'NONE', *, *, #20674, .F. ) ;
#8504=EDGE_LOOP ( 'NONE', ( #4663, #3329, #21237, #2515 ) ) ;
#8506=EDGE_CURVE ( 'NONE', #15166, #11424, #5093, .T. ) ;
#8510=LINE ( 'NONE', #15233, #5752 ) ;
#8515=ORIENTED_EDGE ( 'NONE', *, *, #8835, .T. ) ;
#8529=EDGE_CURVE ( 'NONE', #11017, #11720, #14953, .T. ) ;
#8541=ADVANCED_FACE ( 'NONE', ( #19724 ), #8129, .T. ) ;
#8553=VERTEX_POINT ( 'NONE', #13188 ) ;
#8554=CARTESIAN_POINT ( 'NONE',  ( 10.00000000000000000, 19.29292659244005037, 25.53004080487768235 ) ) ;
#8555=DIRECTION ( 'NONE',  ( -1.000000000000000000, 0.000000000000000000, 0.000000000000000000 ) ) ;
#8560=DIRECTION ( 'NONE',  ( 0.000000000000000000, 0.2079116908177532363, 0.9781476007338069101 ) ) ;
#8563=LINE ( 'NONE', #21824, #6137 ) ;
#8568=VERTEX_POINT ( 'NONE', #5136 ) ;
#8581=CARTESIAN_POINT ( 'NONE',  ( 10.00000000000000000, -7.619321854369379032, -26.42235673590698397 ) ) ;
#8582=ORIENTED_EDGE ( 'NONE', *, *, #12290, .T. ) ;
#8584=AXIS2_PLACEMENT_3D ( 'NONE', #20198, #11466, #16441 ) ;
#8587=DIRECTION ( 'NONE',  ( -1.000000000000000000, 0.000000000000000000, -0.000000000000000000 ) ) ;
#8588=DIRECTION ( 'NONE',  ( 0.000000000000000000, 0.9945218953682729568, 0.1045284632676570374 ) ) ;
#8590=DIRECTION ( 'NONE',  ( -1.000000000000000000, 0.000000000000000000, 0.000000000000000000 ) ) ;
#8591=CARTESIAN_POINT ( 'NONE',  ( 0.000000000000000000, 6.063030049135076816, 31.42037024962127134 ) ) ;
#8593=CARTESIAN_POINT ( 'NONE',  ( 10.00000000000000000, -18.31866948046747723, -26.23788002993743262 ) ) ;
#8603=EDGE_LOOP ( 'NONE', ( #13380, #873, #13303, #18060 ) ) ;
#8607=ORIENTED_EDGE ( 'NONE', *, *, #13405, .T. ) ;
#8608=DIRECTION ( 'NONE',  ( 0.000000000000000000, 1.000000000000000000, 0.000000000000000000 ) ) ;
#8609=DIRECTION ( 'NONE',  ( 0.000000000000000000, 0.000000000000000000, 1.000000000000000000 ) ) ;
#8610=VECTOR ( 'NONE', #1824, 1000.000000000000000 ) ;
#8619=AXIS2_PLACEMENT_3D ( 'NONE', #13960, #705, #8872 ) ;
#8621=ADVANCED_FACE ( 'NONE', ( #1595 ), #8456, .T. ) ;
#8622=VERTEX_POINT ( 'NONE', #8554 ) ;
#8631=ORIENTED_EDGE ( 'NONE', *, *, #1892, .F. ) ;
#8633=FACE_OUTER_BOUND ( 'NONE', #14120, .T. ) ;
#8636=CARTESIAN_POINT ( 'NONE',  ( 0.000000000000000000, 0.000000000000000000, 0.000000000000000000 ) ) ;
#8637=DIRECTION ( 'NONE',  ( 0.000000000000000000, 0.9945218953682729568, 0.1045284632676570374 ) ) ;
#8640=FACE_OUTER_BOUND ( 'NONE', #9002, .T. ) ;
#8641=CIRCLE ( 'NONE', #5830, 5.000000000000000000 ) ;
#8643=ORIENTED_EDGE ( 'NONE', *, *, #7270, .T. ) ;
#8644=AXIS2_PLACEMENT_3D ( 'NONE', #15643, #8587, #15318 ) ;
#8652=ORIENTED_EDGE ( 'NONE', *, *, #17949, .T. ) ;
#8655=ORIENTED_EDGE ( 'NONE', *, *, #12813, .T. ) ;
#8656=ORIENTED_EDGE ( 'NONE', *, *, #14887, .T. ) ;
#8660=ORIENTED_EDGE ( 'NONE', *, *, #4747, .T. ) ;
#8662=DIRECTION ( 'NONE',  ( -1.000000000000000000, -0.000000000000000000, 0.000000000000000000 ) ) ;
#8673=CARTESIAN_POINT ( 'NONE',  ( 10.00000000000000000, -23.37352460145297783, 21.85585385440871775 ) ) ;
#8679=AXIS2_PLACEMENT_3D ( 'NONE', #6816, #784, #3593 ) ;
#8684=ORIENTED_EDGE ( 'NONE', *, *, #19758, .T. ) ;
#8686=LINE ( 'NONE', #11568, #11266 ) ;
#8691=VERTEX_POINT ( 'NONE', #13633 ) ;
#8693=ORIENTED_EDGE ( 'NONE', *, *, #10150, .F. ) ;
#8695=DIRECTION ( 'NONE',  ( 0.000000000000000000, -0.8660254037844327124, -0.5000000000000103251 ) ) ;
#8698=AXIS2_PLACEMENT_3D ( 'NONE', #20661, #5527, #19012 ) ;
#8702=CIRCLE ( 'NONE', #1652, 32.00000000000000000 ) ;
#8715=CARTESIAN_POINT ( 'NONE',  ( -140.0000507999999968, 0.000000000000000000, 0.000000000000000000 ) ) ;
#8724=DIRECTION ( 'NONE',  ( -1.000000000000000000, -0.000000000000000000, 0.000000000000000000 ) ) ;
#8725=DIRECTION ( 'NONE',  ( -1.000000000000000000, -0.000000000000000000, -0.000000000000000000 ) ) ;
#8735=DIRECTION ( 'NONE',  ( 0.000000000000000000, 0.000000000000000000, 1.000000000000000000 ) ) ;
#8743=AXIS2_PLACEMENT_3D ( 'NONE', #7939, #6412, #9366 ) ;
#8746=FACE_OUTER_BOUND ( 'NONE', #12704, .T. ) ;
#8748=LINE ( 'NONE', #20475, #16875 ) ;
#8758=ADVANCED_FACE ( 'NONE', ( #5898 ), #2242, .T. ) ;
#8760=DIRECTION ( 'NONE',  ( 0.000000000000000000, 0.000000000000000000, -1.000000000000000000 ) ) ;
#8762=CARTESIAN_POINT ( 'NONE',  ( 0.000000000000000000, 25.17124263951009411, 12.69364185792227495 ) ) ;
#8763=ORIENTED_EDGE ( 'NONE', *, *, #16924, .T. ) ;
#8766=DIRECTION ( 'NONE',  ( -1.000000000000000000, 0.000000000000000000, -0.000000000000000000 ) ) ;
#8776=EDGE_CURVE ( 'NONE', #2079, #7213, #21326, .T. ) ;
#8788=CIRCLE ( 'NONE', #11252, 11.99999999999999645 ) ;
#8790=AXIS2_PLACEMENT_3D ( 'NONE', #11336, #14547, #9668 ) ;
#8794=CARTESIAN_POINT ( 'NONE',  ( 10.00000000000000000, 0.000000000000000000, 0.000000000000000000 ) ) ;
#8797=( LENGTH_UNIT ( ) NAMED_UNIT ( * ) SI_UNIT ( .MILLI., .METRE. ) );
#8802=DIRECTION ( 'NONE',  ( -1.000000000000000000, -0.000000000000000000, 0.000000000000000000 ) ) ;
#8809=VECTOR ( 'NONE', #11260, 1000.000000000000000 ) ;
#8813=DIRECTION ( 'NONE',  ( -1.000000000000000000, -0.000000000000000000, -0.000000000000000000 ) ) ;
#8816=DIRECTION ( 'NONE',  ( 0.000000000000000000, 0.000000000000000000, -1.000000000000000000 ) ) ;
#8819=EDGE_LOOP ( 'NONE', ( #18453, #7870, #253, #3501 ) ) ;
#8825=ORIENTED_EDGE ( 'NONE', *, *, #423, .T. ) ;
#8827=EDGE_CURVE ( 'NONE', #13950, #12094, #2140, .T. ) ;
#8835=EDGE_CURVE ( 'NONE', #1233, #1686, #11443, .T. ) ;
#8838=AXIS2_PLACEMENT_3D ( 'NONE', #12721, #21236, #6223 ) ;
#8857=CARTESIAN_POINT ( 'NONE',  ( 10.00000000000000000, -28.15804365424197897, 1.358152127005888055 ) ) ;
#8872=DIRECTION ( 'NONE',  ( 0.000000000000000000, 0.000000000000000000, 1.000000000000000000 ) ) ;
#8878=CARTESIAN_POINT ( 'NONE',  ( -10.00000000000000000, 0.000000000000000000, 32.00000000000000000 ) ) ;
#8881=EDGE_LOOP ( 'NONE', ( #19689, #5167, #15685, #3796 ) ) ;
#8883=ORIENTED_EDGE ( 'NONE', *, *, #3409, .T. ) ;
#8917=EDGE_LOOP ( 'NONE', ( #15194, #11457, #4444, #16954 ) ) ;
#8918=ADVANCED_FACE ( 'NONE', ( #2564 ), #21146, .T. ) ;
#8922=ORIENTED_EDGE ( 'NONE', *, *, #6424, .F. ) ;
#8926=DIRECTION ( 'NONE',  ( -1.000000000000000000, 0.000000000000000000, 0.000000000000000000 ) ) ;
#8932=DIRECTION ( 'NONE',  ( 0.000000000000000000, -0.9945218953682721796, -0.1045284632676636571 ) ) ;
#8936=VECTOR ( 'NONE', #12683, 1000.000000000000000 ) ;
#8947=ORIENTED_EDGE ( 'NONE', *, *, #17683, .F. ) ;
#8949=EDGE_CURVE ( 'NONE', #21757, #20880, #20625, .T. ) ;
#8952=ORIENTED_EDGE ( 'NONE', *, *, #16081, .F. ) ;
#8953=CARTESIAN_POINT ( 'NONE',  ( 10.00000000000000000, 22.77465461094674026, 15.41136296218094159 ) ) ;
#8954=FACE_OUTER_BOUND ( 'NONE', #19097, .T. ) ;
#8955=CIRCLE ( 'NONE', #19540, 32.00000000000000000 ) ;
#8956=CARTESIAN_POINT ( 'NONE',  ( 10.00000000000000000, 31.75612719289740937, 3.943144139962659445 ) ) ;
#8962=DIRECTION ( 'NONE',  ( 0.000000000000000000, 0.9510565162951521989, 0.3090169943749513926 ) ) ;
#8964=EDGE_CURVE ( 'NONE', #17498, #9215, #11403, .T. ) ;
#8969=ORIENTED_EDGE ( 'NONE', *, *, #6250, .F. ) ;
#8974=VERTEX_POINT ( 'NONE', #21354 ) ;
#8976=AXIS2_PLACEMENT_3D ( 'NONE', #7998, #14728, #13067 ) ;
#8990=ORIENTED_EDGE ( 'NONE', *, *, #7188, .F. ) ;
#8993=DIRECTION ( 'NONE',  ( -1.000000000000000000, 0.000000000000000000, -0.000000000000000000 ) ) ;
#8997=AXIS2_PLACEMENT_3D ( 'NONE', #14105, #407, #5604 ) ;
#9001=VERTEX_POINT ( 'NONE', #4566 ) ;
#9002=EDGE_LOOP ( 'NONE', ( #19362, #17573, #3953, #8643 ) ) ;
#9004=CARTESIAN_POINT ( 'NONE',  ( -10.00000000000000000, 0.000000000000000000, 0.000000000000000000 ) ) ;
#9005=ORIENTED_EDGE ( 'NONE', *, *, #7411, .T. ) ;
#9006=CARTESIAN_POINT ( 'NONE',  ( 10.00000000000000000, 0.000000000000000000, 0.000000000000000000 ) ) ;
#9014=CIRCLE ( 'NONE', #9669, 11.99999999999999822 ) ;
#9018=CIRCLE ( 'NONE', #1616, 11.99999999999999822 ) ;
#9020=EDGE_CURVE ( 'NONE', #2027, #6083, #19559, .T. ) ;
#9022=VERTEX_POINT ( 'NONE', #8101 ) ;
#9024=ORIENTED_EDGE ( 'NONE', *, *, #20972, .T. ) ;
#9040=CYLINDRICAL_SURFACE ( 'NONE', #15991, 32.00000000000000000 ) ;
#9047=EDGE_CURVE ( 'NONE', #5097, #18503, #12166, .T. ) ;
#9049=ORIENTED_EDGE ( 'NONE', *, *, #20511, .F. ) ;
#9053=ORIENTED_EDGE ( 'NONE', *, *, #1373, .F. ) ;
#9054=EDGE_CURVE ( 'NONE', #14985, #18973, #3120, .T. ) ;
#9056=ORIENTED_EDGE ( 'NONE', *, *, #6475, .T. ) ;
#9060=LINE ( 'NONE', #15365, #10858 ) ;
#9077=VECTOR ( 'NONE', #5064, 1000.000000000000000 ) ;
#9078=DIRECTION ( 'NONE',  ( 0.000000000000000000, 0.000000000000000000, 1.000000000000000000 ) ) ;
#9080=EDGE_CURVE ( 'NONE', #11720, #11543, #3223, .T. ) ;
#9081=DIRECTION ( 'NONE',  ( 0.000000000000000000, 0.000000000000000000, 1.000000000000000000 ) ) ;
#9094=VECTOR ( 'NONE', #17291, 1000.000000000000000 ) ;
#9095=CARTESIAN_POINT ( 'NONE',  ( 10.00000000000000000, 26.69209308833507777, 6.612652082459410607 ) ) ;
#9109=AXIS2_PLACEMENT_3D ( 'NONE', #2870, #7516, #9492 ) ;
#9112=AXIS2_PLACEMENT_3D ( 'NONE', #5216, #16929, #5101 ) ;
#9117=EDGE_LOOP ( 'NONE', ( #16750, #10065, #21778, #19902 ) ) ;
#9120=DIRECTION ( 'NONE',  ( -1.000000000000000000, 0.000000000000000000, -0.000000000000000000 ) ) ;
#9122=CARTESIAN_POINT ( 'NONE',  ( 0.000000000000000000, -7.240962358591786163, 31.16999300804312156 ) ) ;
#9127=AXIS2_PLACEMENT_3D ( 'NONE', #15454, #3960, #2096 ) ;
#9131=DIRECTION ( 'NONE',  ( -1.000000000000000000, 0.000000000000000000, 0.000000000000000000 ) ) ;
#9137=ORIENTED_EDGE ( 'NONE', *, *, #2382, .F. ) ;
#9145=ORIENTED_EDGE ( 'NONE', *, *, #16212, .F. ) ;
#9146=CARTESIAN_POINT ( 'NONE',  ( 0.000000000000000000, 30.24235385705252099, -10.45944707835077381 ) ) ;
#9149=CARTESIAN_POINT ( 'NONE',  ( 10.00000000000000000, 27.26034713664097353, 4.817140289263753594 ) ) ;
#9150=EDGE_CURVE ( 'NONE', #18200, #5699, #17819, .T. ) ;
#9155=CARTESIAN_POINT ( 'NONE',  ( -10.00000000000000000, 0.000000000000000000, 0.000000000000000000 ) ) ;
#9160=VERTEX_POINT ( 'NONE', #338 ) ;
#9162=EDGE_CURVE ( 'NONE', #15688, #12744, #7946, .T. ) ;
#9171=CARTESIAN_POINT ( 'NONE',  ( -10.00000000000000000, 0.000000000000000000, 0.000000000000000000 ) ) ;
#9172=DIRECTION ( 'NONE',  ( 1.000000000000000000, -0.000000000000000000, -0.000000000000000000 ) ) ;
#9187=VERTEX_POINT ( 'NONE', #7720 ) ;
#9192=ORIENTED_EDGE ( 'NONE', *, *, #6648, .T. ) ;
#9195=DIRECTION ( 'NONE',  ( -1.000000000000000000, 0.000000000000000000, -0.000000000000000000 ) ) ;
#9196=DIRECTION ( 'NONE',  ( -1.000000000000000000, -0.000000000000000000, 0.000000000000000000 ) ) ;
#9197=CARTESIAN_POINT ( 'NONE',  ( 0.000000000000000000, -30.61448696004446290, -9.314139153634542367 ) ) ;
#9202=EDGE_CURVE ( 'NONE', #6772, #11604, #20761, .T. ) ;
#9211=CARTESIAN_POINT ( 'NONE',  ( 10.00000000000000000, -17.70753755129023332, -21.03896658273990639 ) ) ;
#9215=VERTEX_POINT ( 'NONE', #12573 ) ;
#9219=DIRECTION ( 'NONE',  ( 0.000000000000000000, 0.5877852522924689183, 0.8090169943749505599 ) ) ;
#9220=DIRECTION ( 'NONE',  ( -1.000000000000000000, -0.000000000000000000, 0.000000000000000000 ) ) ;
#9226=CARTESIAN_POINT ( 'NONE',  ( 5.000000000000000000, 27.40684453873989668, -16.51862198941980608 ) ) ;
#9231=FACE_OUTER_BOUND ( 'NONE', #3043, .T. ) ;
#9232=EDGE_LOOP ( 'NONE', ( #11707, #21639, #4024, #2353 ) ) ;
#9236=DIRECTION ( 'NONE',  ( 0.000000000000000000, 0.000000000000000000, 1.000000000000000000 ) ) ;
#9244=DIRECTION ( 'NONE',  ( 0.000000000000000000, 0.8660254037844398178, -0.4999999999999980016 ) ) ;
#9247=DIRECTION ( 'NONE',  ( 0.000000000000000000, 0.000000000000000000, 1.000000000000000000 ) ) ;
#9254=ORIENTED_EDGE ( 'NONE', *, *, #12026, .F. ) ;
#9262=AXIS2_PLACEMENT_3D ( 'NONE', #7442, #264, #2239 ) ;
#9263=EDGE_LOOP ( 'NONE', ( #20704, #6191, #6983, #3558 ) ) ;
#9264=LINE ( 'NONE', #4422, #12282 ) ;
#9265=ORIENTED_EDGE ( 'NONE', *, *, #4058, .T. ) ;
#9269=AXIS2_PLACEMENT_3D ( 'NONE', #19208, #10806, #9363 ) ;
#9284=CIRCLE ( 'NONE', #18842, 12.00000000000000000 ) ;
#9285=VERTEX_POINT ( 'NONE', #2412 ) ;
#9291=AXIS2_PLACEMENT_3D ( 'NONE', #3456, #18486, #3667 ) ;
#9297=CYLINDRICAL_SURFACE ( 'NONE', #8465, 27.49900000000000233 ) ;
#9303=FACE_OUTER_BOUND ( 'NONE', #11369, .T. ) ;
#9310=DIRECTION ( 'NONE',  ( 0.000000000000000000, 0.000000000000000000, 1.000000000000000000 ) ) ;
#9317=FACE_OUTER_BOUND ( 'NONE', #9263, .T. ) ;
#9318=VERTEX_POINT ( 'NONE', #16225 ) ;
#9329=ADVANCED_FACE ( 'NONE', ( #974 ), #9912, .T. ) ;
#9335=AXIS2_PLACEMENT_3D ( 'NONE', #12036, #17121, #15458 ) ;
#9336=DIRECTION ( 'NONE',  ( 1.000000000000000000, -0.000000000000000000, 0.000000000000000000 ) ) ;
#9340=FACE_OUTER_BOUND ( 'NONE', #21272, .T. ) ;
#9341=AXIS2_PLACEMENT_3D ( 'NONE', #4165, #10902, #17653 ) ;
#9344=ORIENTED_EDGE ( 'NONE', *, *, #6556, .T. ) ;
#9348=CIRCLE ( 'NONE', #16059, 27.49900000000000588 ) ;
#9354=LINE ( 'NONE', #15665, #10751 ) ;
#9363=DIRECTION ( 'NONE',  ( 0.000000000000000000, -0.7431448254773997952, 0.6691306063588520203 ) ) ;
#9366=DIRECTION ( 'NONE',  ( 0.000000000000000000, 0.000000000000000000, -1.000000000000000000 ) ) ;
#9375=ORIENTED_EDGE ( 'NONE', *, *, #15955, .T. ) ;
#9376=ORIENTED_EDGE ( 'NONE', *, *, #4003, .F. ) ;
#9381=DIRECTION ( 'NONE',  ( 1.000000000000000000, 0.000000000000000000, 0.000000000000000000 ) ) ;
#9387=DIRECTION ( 'NONE',  ( 0.000000000000000000, 0.000000000000000000, -1.000000000000000000 ) ) ;
#9389=CARTESIAN_POINT ( 'NONE',  ( -10.00000000000000000, 0.000000000000000000, 0.000000000000000000 ) ) ;
#9406=DIRECTION ( 'NONE',  ( -1.000000000000000000, 0.000000000000000000, 0.000000000000000000 ) ) ;
#9407=DIRECTION ( 'NONE',  ( 0.000000000000000000, 0.9510565162951523099, 0.3090169943749512260 ) ) ;
#9422=DIRECTION ( 'NONE',  ( -1.000000000000000000, -0.000000000000000000, 0.000000000000000000 ) ) ;
#9423=CARTESIAN_POINT ( 'NONE',  ( 10.00000000000000000, 28.15804365424197186, -1.358152127006073684 ) ) ;
#9428=EDGE_CURVE ( 'NONE', #13513, #910, #19649, .T. ) ;
#9435=CYLINDRICAL_SURFACE ( 'NONE', #5918, 32.00000000000000000 ) ;
#9440=DIRECTION ( 'NONE',  ( 0.000000000000000000, 0.7431448254773910245, 0.6691306063588617903 ) ) ;
#9447=AXIS2_PLACEMENT_3D ( 'NONE', #21033, #9196, #19590 ) ;
#9452=EDGE_CURVE ( 'NONE', #20371, #12792, #2955, .T. ) ;
#9457=VERTEX_POINT ( 'NONE', #3286 ) ;
#9458=CARTESIAN_POINT ( 'NONE',  ( 5.000000000000000888, 31.75612719289740937, 3.943144139962659445 ) ) ;
#9459=ORIENTED_EDGE ( 'NONE', *, *, #11657, .T. ) ;
#9464=ORIENTED_EDGE ( 'NONE', *, *, #9987, .T. ) ;
#9465=CARTESIAN_POINT ( 'NONE',  ( 10.00000000000000000, 0.000000000000000000, 0.000000000000000000 ) ) ;
#9472=VECTOR ( 'NONE', #1929, 1000.000000000000000 ) ;
#9478=DIRECTION ( 'NONE',  ( 0.000000000000000000, 0.000000000000000000, -1.000000000000000000 ) ) ;
#9483=ORIENTED_EDGE ( 'NONE', *, *, #1217, .F. ) ;
#9488=EDGE_CURVE ( 'NONE', #5595, #11274, #9348, .T. ) ;
#9491=EDGE_LOOP ( 'NONE', ( #7460, #20614, #13268, #17883 ) ) ;
#9492=DIRECTION ( 'NONE',  ( 0.000000000000000000, 0.000000000000000000, 1.000000000000000000 ) ) ;
#9493=EDGE_CURVE ( 'NONE', #11265, #7508, #21711, .T. ) ;
#9498=CARTESIAN_POINT ( 'NONE',  ( 10.00000000000000000, 0.000000000000000000, 32.00000000000000000 ) ) ;
#9505=LINE ( 'NONE', #13259, #317 ) ;
#9512=ORIENTED_EDGE ( 'NONE', *, *, #19701, .F. ) ;
#9523=CARTESIAN_POINT ( 'NONE',  ( -140.0000507999999968, 0.000000000000000000, 0.000000000000000000 ) ) ;
#9526=DIRECTION ( 'NONE',  ( 0.000000000000000000, 0.000000000000000000, 1.000000000000000000 ) ) ;
#9529=DIRECTION ( 'NONE',  ( 0.000000000000000000, 0.000000000000000000, 1.000000000000000000 ) ) ;
#9531=CARTESIAN_POINT ( 'NONE',  ( 10.00000000000000000, 30.24235385705238244, 10.45944707835118059 ) ) ;
#9533=ORIENTED_EDGE ( 'NONE', *, *, #9889, .T. ) ;
#9537=ORIENTED_EDGE ( 'NONE', *, *, #3767, .F. ) ;
#9538=EDGE_CURVE ( 'NONE', #17965, #20371, #18192, .T. ) ;
#9542=AXIS2_PLACEMENT_3D ( 'NONE', #21616, #16315, #4614 ) ;
#9546=DIRECTION ( 'NONE',  ( 1.000000000000000000, -0.000000000000000000, 0.000000000000000000 ) ) ;
#9549=CARTESIAN_POINT ( 'NONE',  ( 10.00000000000000000, 26.69209308833507777, 6.612652082459410607 ) ) ;
#9553=CARTESIAN_POINT ( 'NONE',  ( 0.000000000000000000, 19.85071254963777676, 20.01672328094538145 ) ) ;
#9566=EDGE_CURVE ( 'NONE', #1295, #16815, #1206, .T. ) ;
#9567=CARTESIAN_POINT ( 'NONE',  ( 0.000000000000000000, 24.17932380791746994, -20.96092317126981186 ) ) ;
#9568=DIRECTION ( 'NONE',  ( -1.000000000000000000, 0.000000000000000000, -0.000000000000000000 ) ) ;
#9573=CARTESIAN_POINT ( 'NONE',  ( -140.0000507999999968, 0.000000000000000000, 0.000000000000000000 ) ) ;
#9575=DIRECTION ( 'NONE',  ( 0.000000000000000000, 0.000000000000000000, 1.000000000000000000 ) ) ;
#9596=CYLINDRICAL_SURFACE ( 'NONE', #10531, 11.99999999999999822 ) ;
#9603=CYLINDRICAL_SURFACE ( 'NONE', #21719, 12.00000000000000000 ) ;
#9604=AXIS2_PLACEMENT_3D ( 'NONE', #14915, #18461, #1770 ) ;
#9606=VERTEX_POINT ( 'NONE', #9122 ) ;
#9609=DIRECTION ( 'NONE',  ( 1.000000000000000000, -0.000000000000000000, -0.000000000000000000 ) ) ;
#9611=VERTEX_POINT ( 'NONE', #12652 ) ;
#9614=ORIENTED_EDGE ( 'NONE', *, *, #20020, .F. ) ;
#9616=DIRECTION ( 'NONE',  ( -1.000000000000000000, -0.000000000000000000, 0.000000000000000000 ) ) ;
#9624=AXIS2_PLACEMENT_3D ( 'NONE', #19762, #4285, #19530 ) ;
#9625=DIRECTION ( 'NONE',  ( 0.000000000000000000, 0.000000000000000000, 1.000000000000000000 ) ) ;
#9626=CARTESIAN_POINT ( 'NONE',  ( 0.000000000000000000, -7.409634587003275819, 27.19958299168154880 ) ) ;
#9636=VECTOR ( 'NONE', #10246, 1000.000000000000000 ) ;
#9637=ORIENTED_EDGE ( 'NONE', *, *, #12026, .T. ) ;
#9647=ORIENTED_EDGE ( 'NONE', *, *, #17576, .T. ) ;
#9652=FACE_BOUND ( 'NONE', #15122, .T. ) ;
#9665=LINE ( 'NONE', #16744, #2714 ) ;
#9668=DIRECTION ( 'NONE',  ( 0.000000000000000000, 0.000000000000000000, 1.000000000000000000 ) ) ;
#9669=AXIS2_PLACEMENT_3D ( 'NONE', #18955, #3699, #14083 ) ;
#9675=ORIENTED_EDGE ( 'NONE', *, *, #9915, .F. ) ;
#9679=DIRECTION ( 'NONE',  ( 0.000000000000000000, 0.000000000000000000, -1.000000000000000000 ) ) ;
#9680=CARTESIAN_POINT ( 'NONE',  ( 10.00000000000000000, 9.366510754379232750, 25.85466064925429208 ) ) ;
#9689=CARTESIAN_POINT ( 'NONE',  ( 0.000000000000000000, 0.000000000000000000, 0.000000000000000000 ) ) ;
#9691=CARTESIAN_POINT ( 'NONE',  ( 10.00000000000000000, -28.15804365424197897, 1.358152127005888055 ) ) ;
#9693=DIRECTION ( 'NONE',  ( 0.000000000000000000, 0.000000000000000000, 1.000000000000000000 ) ) ;
#9694=ORIENTED_EDGE ( 'NONE', *, *, #19219, .T. ) ;
#9701=VERTEX_POINT ( 'NONE', #21172 ) ;
#9707=EDGE_CURVE ( 'NONE', #3550, #7280, #19911, .T. ) ;
#9714=CIRCLE ( 'NONE', #4087, 11.99999999999999467 ) ;
#9715=FACE_OUTER_BOUND ( 'NONE', #6464, .T. ) ;
#9722=EDGE_CURVE ( 'NONE', #17553, #4799, #7260, .T. ) ;
#9723=VECTOR ( 'NONE', #14122, 1000.000000000000000 ) ;
#9725=ORIENTED_EDGE ( 'NONE', *, *, #7136, .T. ) ;
#9728=ORIENTED_EDGE ( 'NONE', *, *, #3784, .T. ) ;
#9736=DIRECTION ( 'NONE',  ( 0.000000000000000000, -0.2079116908177666145, 0.9781476007338040235 ) ) ;
#9739=CIRCLE ( 'NONE', #19994, 11.99999999999999822 ) ;
#9745=DIRECTION ( 'NONE',  ( 1.000000000000000000, -0.000000000000000000, -0.000000000000000000 ) ) ;
#9747=DIRECTION ( 'NONE',  ( 0.000000000000000000, -0.4067366430758070917, 0.9135454576425978690 ) ) ;
#9759=ORIENTED_EDGE ( 'NONE', *, *, #11380, .F. ) ;
#9762=ORIENTED_EDGE ( 'NONE', *, *, #8776, .F. ) ;
#9766=CARTESIAN_POINT ( 'NONE',  ( 10.00000000000000000, -4.294029059350045863, 27.86182539015965176 ) ) ;
#9780=VERTEX_POINT ( 'NONE', #7689 ) ;
#9781=CARTESIAN_POINT ( 'NONE',  ( 10.00000000000000000, 17.83210509884640871, 21.83428559348767806 ) ) ;
#9782=VERTEX_POINT ( 'NONE', #19504 ) ;
#9786=DIRECTION ( 'NONE',  ( 0.000000000000000000, -6.938893903907230744E-15, 1.000000000000000000 ) ) ;
#9805=AXIS2_PLACEMENT_3D ( 'NONE', #5551, #18601, #2016 ) ;
#9815=VECTOR ( 'NONE', #15808, 1000.000000000000000 ) ;
#9819=CIRCLE ( 'NONE', #19704, 12.00000000000000000 ) ;
#9821=ADVANCED_FACE ( 'NONE', ( #19620, #9652 ), #4486, .T. ) ;
#9822=VERTEX_POINT ( 'NONE', #20061 ) ;
#9826=DIRECTION ( 'NONE',  ( -1.000000000000000000, 0.000000000000000000, -0.000000000000000000 ) ) ;
#9827=DIRECTION ( 'NONE',  ( -1.000000000000000000, 0.000000000000000000, 0.000000000000000000 ) ) ;
#9844=ORIENTED_EDGE ( 'NONE', *, *, #16128, .F. ) ;
#9845=CARTESIAN_POINT ( 'NONE',  ( 0.000000000000000000, 0.000000000000000000, 0.000000000000000000 ) ) ;
#9847=ORIENTED_EDGE ( 'NONE', *, *, #2741, .F. ) ;
#9849=VECTOR ( 'NONE', #8050, 1000.000000000000000 ) ;
#9854=AXIS2_PLACEMENT_3D ( 'NONE', #8794, #14187, #20934 ) ;
#9858=CYLINDRICAL_SURFACE ( 'NONE', #15344, 11.99999999999999822 ) ;
#9862=EDGE_CURVE ( 'NONE', #2871, #19585, #8277, .T. ) ;
#9864=DIRECTION ( 'NONE',  ( -1.000000000000000000, 0.000000000000000000, 0.000000000000000000 ) ) ;
#9867=EDGE_CURVE ( 'NONE', #21189, #1350, #11323, .T. ) ;
#9868=ADVANCED_FACE ( 'NONE', ( #17860 ), #7907, .T. ) ;
#9879=EDGE_LOOP ( 'NONE', ( #21186, #9759, #4719, #20825 ) ) ;
#9880=ORIENTED_EDGE ( 'NONE', *, *, #10402, .F. ) ;
#9882=DIRECTION ( 'NONE',  ( 0.000000000000000000, 0.9510565162951544194, -0.3090169943749448977 ) ) ;
#9885=CARTESIAN_POINT ( 'NONE',  ( -140.0000507999999968, 0.000000000000000000, 0.000000000000000000 ) ) ;
#9889=EDGE_CURVE ( 'NONE', #19281, #15418, #20261, .T. ) ;
#9891=DIRECTION ( 'NONE',  ( 0.000000000000000000, 0.000000000000000000, 1.000000000000000000 ) ) ;
#9892=DIRECTION ( 'NONE',  ( -1.000000000000000000, -0.000000000000000000, -0.000000000000000000 ) ) ;
#9893=UNCERTAINTY_MEASURE_WITH_UNIT (LENGTH_MEASURE( 1.000000000000000082E-05 ), #8797, 'distance_accuracy_value', 'NONE');
#9895=EDGE_CURVE ( 'NONE', #2536, #2434, #21598, .T. ) ;
#9898=EDGE_LOOP ( 'NONE', ( #13765, #15887, #11297, #14551 ) ) ;
#9902=CARTESIAN_POINT ( 'NONE',  ( 10.00000000000000000, 12.90282758293013643, -25.06465718894764194 ) ) ;
#9906=CARTESIAN_POINT ( 'NONE',  ( 10.00000000000000000, 0.000000000000000000, 0.000000000000000000 ) ) ;
#9908=ORIENTED_EDGE ( 'NONE', *, *, #19434, .F. ) ;
#9912=CYLINDRICAL_SURFACE ( 'NONE', #10051, 12.00000000000000000 ) ;
#9914=DIRECTION ( 'NONE',  ( -1.000000000000000000, -0.000000000000000000, -0.000000000000000000 ) ) ;
#9915=EDGE_CURVE ( 'NONE', #11955, #3827, #5122, .T. ) ;
#9916=CARTESIAN_POINT ( 'NONE',  ( 10.00000000000000000, 7.409634587003466777, -27.19958299168149907 ) ) ;
#9922=DIRECTION ( 'NONE',  ( 0.000000000000000000, 0.000000000000000000, 1.000000000000000000 ) ) ;
#9926=ORIENTED_EDGE ( 'NONE', *, *, #3168, .T. ) ;
#9941=ORIENTED_EDGE ( 'NONE', *, *, #15632, .T. ) ;
#9943=CARTESIAN_POINT ( 'NONE',  ( 0.000000000000000000, -17.83210509884655792, 21.83428559348755371 ) ) ;
#9949=DIRECTION ( 'NONE',  ( 0.000000000000000000, -0.7431448254773861395, -0.6691306063588672304 ) ) ;
#9954=VERTEX_POINT ( 'NONE', #8344 ) ;
#9958=LINE ( 'NONE', #18383, #880 ) ;
#9962=CYLINDRICAL_SURFACE ( 'NONE', #6158, 12.00000000000000000 ) ;
#9969=EDGE_CURVE ( 'NONE', #667, #11653, #6914, .T. ) ;
#9970=CARTESIAN_POINT ( 'NONE',  ( 5.000000000000000888, -7.240962358591358061, -31.16999300804322104 ) ) ;
#9976=ORIENTED_EDGE ( 'NONE', *, *, #29, .T. ) ;
#9980=DIRECTION ( 'NONE',  ( -1.000000000000000000, 0.000000000000000000, 0.000000000000000000 ) ) ;
#9983=ORIENTED_EDGE ( 'NONE', *, *, #5692, .T. ) ;
#9985=FACE_OUTER_BOUND ( 'NONE', #10358, .T. ) ;
#9987=EDGE_CURVE ( 'NONE', #5218, #11931, #17108, .T. ) ;
#9988=CARTESIAN_POINT ( 'NONE',  ( 10.00000000000000000, 7.240962358591984227, -31.16999300804307182 ) ) ;
#10000=AXIS2_PLACEMENT_3D ( 'NONE', #20943, #4153, #9219 ) ;
#10003=ORIENTED_EDGE ( 'NONE', *, *, #31, .F. ) ;
#10007=DIRECTION ( 'NONE',  ( 0.000000000000000000, 0.000000000000000000, -1.000000000000000000 ) ) ;
#10014=CARTESIAN_POINT ( 'NONE',  ( 10.00000000000000000, 26.27606311335965827, -10.21217444509384364 ) ) ;
#10018=DIRECTION ( 'NONE',  ( -1.000000000000000000, -0.000000000000000000, -0.000000000000000000 ) ) ;
#10020=EDGE_CURVE ( 'NONE', #13874, #7135, #10427, .T. ) ;
#10025=DIRECTION ( 'NONE',  ( 0.000000000000000000, 0.000000000000000000, 1.000000000000000000 ) ) ;
#10027=ADVANCED_FACE ( 'NONE', ( #9985 ), #16963, .T. ) ;
#10030=DIRECTION ( 'NONE',  ( -1.000000000000000000, 0.000000000000000000, -0.000000000000000000 ) ) ;
#10042=ORIENTED_EDGE ( 'NONE', *, *, #19630, .F. ) ;
#10050=DIRECTION ( 'NONE',  ( -1.000000000000000000, 0.000000000000000000, 0.000000000000000000 ) ) ;
#10051=AXIS2_PLACEMENT_3D ( 'NONE', #3183, #16765, #7934 ) ;
#10053=CARTESIAN_POINT ( 'NONE',  ( 0.000000000000000000, 0.000000000000000000, 0.000000000000000000 ) ) ;
#10055=FACE_OUTER_BOUND ( 'NONE', #21857, .T. ) ;
#10058=ORIENTED_EDGE ( 'NONE', *, *, #17728, .F. ) ;
#10065=ORIENTED_EDGE ( 'NONE', *, *, #991, .T. ) ;
#10071=CYLINDRICAL_SURFACE ( 'NONE', #13388, 27.49900000000000233 ) ;
#10078=DIRECTION ( 'NONE',  ( 0.000000000000000000, 0.000000000000000000, 1.000000000000000000 ) ) ;
#10083=CARTESIAN_POINT ( 'NONE',  ( 0.000000000000000000, 0.000000000000000000, 0.000000000000000000 ) ) ;
#10105=DIRECTION ( 'NONE',  ( 0.000000000000000000, -0.7431448254773997952, 0.6691306063588520203 ) ) ;
#10108=VERTEX_POINT ( 'NONE', #9095 ) ;
#10112=ORIENTED_EDGE ( 'NONE', *, *, #9722, .F. ) ;
#10116=EDGE_CURVE ( 'NONE', #17553, #16041, #11109, .T. ) ;
#10119=ORIENTED_EDGE ( 'NONE', *, *, #8835, .F. ) ;
#10121=AXIS2_PLACEMENT_3D ( 'NONE', #3542, #12145, #17131 ) ;
#10124=EDGE_LOOP ( 'NONE', ( #15810, #10791, #13220, #4177 ) ) ;
#10134=DIRECTION ( 'NONE',  ( -1.000000000000000000, 0.000000000000000000, 0.000000000000000000 ) ) ;
#10137=EDGE_CURVE ( 'NONE', #11343, #16375, #18171, .T. ) ;
#10140=CARTESIAN_POINT ( 'NONE',  ( 10.00000000000000000, 7.409634587003093742, 27.19958299168160565 ) ) ;
#10142=AXIS2_PLACEMENT_3D ( 'NONE', #14895, #1426, #11256 ) ;
#10150=EDGE_CURVE ( 'NONE', #12524, #19400, #5570, .T. ) ;
#10152=ORIENTED_EDGE ( 'NONE', *, *, #14582, .T. ) ;
#10154=CIRCLE ( 'NONE', #6642, 27.49900000000000588 ) ;
#10168=DIRECTION ( 'NONE',  ( -1.000000000000000000, 0.000000000000000000, 0.000000000000000000 ) ) ;
#10174=VECTOR ( 'NONE', #11921, 1000.000000000000000 ) ;
#10177=AXIS2_PLACEMENT_3D ( 'NONE', #21123, #5884, #2779 ) ;
#10179=DIRECTION ( 'NONE',  ( 0.000000000000000000, 0.000000000000000000, 1.000000000000000000 ) ) ;
#10180=EDGE_CURVE ( 'NONE', #9022, #569, #1220, .T. ) ;
#10182=CARTESIAN_POINT ( 'NONE',  ( 0.000000000000000000, -23.37352460145268651, -21.85585385440903750 ) ) ;
#10183=ORIENTED_EDGE ( 'NONE', *, *, #10825, .T. ) ;
#10188=CIRCLE ( 'NONE', #10895, 32.00000000000000000 ) ;
#10189=DIRECTION ( 'NONE',  ( -1.000000000000000000, 0.000000000000000000, 0.000000000000000000 ) ) ;
#10190=FACE_OUTER_BOUND ( 'NONE', #4552, .T. ) ;
#10194=CIRCLE ( 'NONE', #666, 11.99999999999999822 ) ;
#10195=CYLINDRICAL_SURFACE ( 'NONE', #14241, 11.99999999999999645 ) ;
#10199=EDGE_CURVE ( 'NONE', #8423, #9701, #801, .T. ) ;
#10200=CYLINDRICAL_SURFACE ( 'NONE', #12266, 11.99999999999999645 ) ;
#10201=DIRECTION ( 'NONE',  ( 1.000000000000000000, 0.000000000000000000, -0.000000000000000000 ) ) ;
#10215=CARTESIAN_POINT ( 'NONE',  ( 0.000000000000000000, 0.000000000000000000, 0.000000000000000000 ) ) ;
#10220=LINE ( 'NONE', #8878, #10720 ) ;
#10222=LINE ( 'NONE', #3372, #10262 ) ;
#10232=DIRECTION ( 'NONE',  ( 0.000000000000000000, 0.000000000000000000, 1.000000000000000000 ) ) ;
#10234=ORIENTED_EDGE ( 'NONE', *, *, #12260, .T. ) ;
#10238=ORIENTED_EDGE ( 'NONE', *, *, #6665, .F. ) ;
#10242=DIRECTION ( 'NONE',  ( -1.000000000000000000, -0.000000000000000000, 0.000000000000000000 ) ) ;
#10243=DIRECTION ( 'NONE',  ( -1.000000000000000000, -0.000000000000000000, 0.000000000000000000 ) ) ;
#10246=DIRECTION ( 'NONE',  ( 1.000000000000000000, -0.000000000000000000, -0.000000000000000000 ) ) ;
#10248=DIRECTION ( 'NONE',  ( 1.000000000000000000, -0.000000000000000000, -0.000000000000000000 ) ) ;
#10249=CARTESIAN_POINT ( 'NONE',  ( 10.00000000000000000, 0.000000000000000000, 0.000000000000000000 ) ) ;
#10254=CARTESIAN_POINT ( 'NONE',  ( 10.00000000000000000, 24.17932380791719282, 20.96092317127012095 ) ) ;
#10255=VERTEX_POINT ( 'NONE', #21575 ) ;
#10256=LINE ( 'NONE', #3302, #10552 ) ;
#10258=CARTESIAN_POINT ( 'NONE',  ( 0.000000000000000000, 27.26034713664097353, 4.817140289263753594 ) ) ;
#10261=VERTEX_POINT ( 'NONE', #19699 ) ;
#10262=VECTOR ( 'NONE', #1288, 1000.000000000000000 ) ;
#10265=ORIENTED_EDGE ( 'NONE', *, *, #11092, .T. ) ;
#10269=CARTESIAN_POINT ( 'NONE',  ( 0.000000000000000000, 17.70753755129066320, -21.03896658273954046 ) ) ;
#10270=EDGE_CURVE ( 'NONE', #8175, #18968, #3366, .T. ) ;
#10272=DIRECTION ( 'NONE',  ( 0.000000000000000000, 0.000000000000000000, 1.000000000000000000 ) ) ;
#10280=ORIENTED_EDGE ( 'NONE', *, *, #6376, .F. ) ;
#10281=VERTEX_POINT ( 'NONE', #7881 ) ;
#10282=EDGE_CURVE ( 'NONE', #8423, #5649, #6554, .T. ) ;
#10290=DIRECTION ( 'NONE',  ( -1.000000000000000000, -0.000000000000000000, 0.000000000000000000 ) ) ;
#10293=DIRECTION ( 'NONE',  ( 1.000000000000000000, -0.000000000000000000, -0.000000000000000000 ) ) ;
#10297=CARTESIAN_POINT ( 'NONE',  ( 0.000000000000000000, 27.07404830566971299, 4.815694066514526028 ) ) ;
#10298=EDGE_CURVE ( 'NONE', #15579, #9606, #12888, .T. ) ;
#10304=ADVANCED_FACE ( 'NONE', ( #3123 ), #9858, .T. ) ;
#10305=ORIENTED_EDGE ( 'NONE', *, *, #16491, .T. ) ;
#10306=EDGE_LOOP ( 'NONE', ( #17250, #10772, #13048, #10305 ) ) ;
#10321=CARTESIAN_POINT ( 'NONE',  ( 10.00000000000000000, 14.53731623274961571, -23.34226719384889748 ) ) ;
#10324=AXIS2_PLACEMENT_3D ( 'NONE', #16578, #8182, #14913 ) ;
#10335=ORIENTED_EDGE ( 'NONE', *, *, #9722, .T. ) ;
#10340=FACE_OUTER_BOUND ( 'NONE', #10546, .T. ) ;
#10345=CARTESIAN_POINT ( 'NONE',  ( 10.00000000000000000, 22.77465461094694632, -15.41136296218063428 ) ) ;
#10356=ORIENTED_EDGE ( 'NONE', *, *, #21369, .T. ) ;
#10358=EDGE_LOOP ( 'NONE', ( #7814, #2760, #3980, #19604 ) ) ;
#10362=CIRCLE ( 'NONE', #18139, 11.99999999999999822 ) ;
#10385=EDGE_CURVE ( 'NONE', #14091, #10683, #9958, .T. ) ;
#10398=DIRECTION ( 'NONE',  ( -1.000000000000000000, -0.000000000000000000, -0.000000000000000000 ) ) ;
#10402=EDGE_CURVE ( 'NONE', #3628, #9187, #6884, .T. ) ;
#10408=AXIS2_PLACEMENT_3D ( 'NONE', #2805, #2902, #12840 ) ;
#10413=CIRCLE ( 'NONE', #6922, 11.99999999999999822 ) ;
#10418=CARTESIAN_POINT ( 'NONE',  ( 10.00000000000000000, 0.000000000000000000, 0.000000000000000000 ) ) ;
#10423=DIRECTION ( 'NONE',  ( 0.000000000000000000, 0.000000000000000000, -1.000000000000000000 ) ) ;
#10426=AXIS2_PLACEMENT_3D ( 'NONE', #20711, #1823, #8560 ) ;
#10427=LINE ( 'NONE', #5356, #11456 ) ;
#10431=CARTESIAN_POINT ( 'NONE',  ( 0.000000000000000000, -0.6021240089799234640, -31.99433460282945063 ) ) ;
#10432=DIRECTION ( 'NONE',  ( -1.000000000000000000, 0.000000000000000000, -0.000000000000000000 ) ) ;
#10436=CARTESIAN_POINT ( 'NONE',  ( 10.00000000000000000, 24.73395913766480447, -12.01774797440553044 ) ) ;
#10437=ORIENTED_EDGE ( 'NONE', *, *, #842, .T. ) ;
#10438=AXIS2_PLACEMENT_3D ( 'NONE', #17076, #2454, #15412 ) ;
#10440=CIRCLE ( 'NONE', #7970, 27.49900000000000944 ) ;
#10446=DIRECTION ( 'NONE',  ( -1.000000000000000000, 0.000000000000000000, -0.000000000000000000 ) ) ;
#10447=CYLINDRICAL_SURFACE ( 'NONE', #16919, 12.00000000000000000 ) ;
#10448=ORIENTED_EDGE ( 'NONE', *, *, #2425, .T. ) ;
#10449=VERTEX_POINT ( 'NONE', #20474 ) ;
#10458=CIRCLE ( 'NONE', #13625, 11.99999999999999822 ) ;
#10460=CARTESIAN_POINT ( 'NONE',  ( 5.000000000000000000, 12.46320060045723999, 29.47318494484033025 ) ) ;
#10464=DIRECTION ( 'NONE',  ( 0.000000000000000000, 0.000000000000000000, 1.000000000000000000 ) ) ;
#10466=DIRECTION ( 'NONE',  ( -1.000000000000000000, -0.000000000000000000, 0.000000000000000000 ) ) ;
#10470=VECTOR ( 'NONE', #1550, 1000.000000000000000 ) ;
#10477=EDGE_LOOP ( 'NONE', ( #7191, #1734, #17665, #9926 ) ) ;
#10491=DIRECTION ( 'NONE',  ( -1.000000000000000000, 0.000000000000000000, -0.000000000000000000 ) ) ;
#10504=CIRCLE ( 'NONE', #21452, 32.00000000000000000 ) ;
#10508=CARTESIAN_POINT ( 'NONE',  ( 10.00000000000000000, 9.992993448021948666, -26.36019881529875519 ) ) ;
#10513=CARTESIAN_POINT ( 'NONE',  ( 10.00000000000000000, 0.000000000000000000, 0.000000000000000000 ) ) ;
#10516=ADVANCED_FACE ( 'NONE', ( #14045 ), #15703, .T. ) ;
#10518=ORIENTED_EDGE ( 'NONE', *, *, #17021, .T. ) ;
#10528=VERTEX_POINT ( 'NONE', #8956 ) ;
#10529=AXIS2_PLACEMENT_3D ( 'NONE', #10735, #900, #9078 ) ;
#10531=AXIS2_PLACEMENT_3D ( 'NONE', #11498, #1110, #4648 ) ;
#10532=DIRECTION ( 'NONE',  ( 1.000000000000000000, 0.000000000000000000, 0.000000000000000000 ) ) ;
#10535=AXIS2_PLACEMENT_3D ( 'NONE', #7731, #14133, #10812 ) ;
#10536=EDGE_CURVE ( 'NONE', #9780, #17002, #4421, .T. ) ;
#10538=CARTESIAN_POINT ( 'NONE',  ( 5.000000000000000000, -13.56333590714035253, 28.98337314858430602 ) ) ;
#10541=CARTESIAN_POINT ( 'NONE',  ( 10.00000000000000000, 26.69209308833516658, -6.612652082459054448 ) ) ;
#10543=EDGE_CURVE ( 'NONE', #5699, #17767, #21367, .T. ) ;
#10544=ADVANCED_FACE ( 'NONE', ( #12169 ), #17264, .T. ) ;
#10546=EDGE_LOOP ( 'NONE', ( #4968, #907, #12300, #18090 ) ) ;
#10552=VECTOR ( 'NONE', #10030, 1000.000000000000000 ) ;
#10558=ORIENTED_EDGE ( 'NONE', *, *, #144, .T. ) ;
#10573=VECTOR ( 'NONE', #4048, 1000.000000000000000 ) ;
#10574=DIRECTION ( 'NONE',  ( -1.000000000000000000, -0.000000000000000000, -0.000000000000000000 ) ) ;
#10577=CARTESIAN_POINT ( 'NONE',  ( 10.00000000000000000, -9.992993448021419312, -26.36019881529895770 ) ) ;
#10580=EDGE_CURVE ( 'NONE', #13685, #21761, #4054, .T. ) ;
#10584=CARTESIAN_POINT ( 'NONE',  ( 10.00000000000000000, -19.07277123396528395, -19.80970465344768172 ) ) ;
#10587=DIRECTION ( 'NONE',  ( -1.000000000000000000, 0.000000000000000000, -0.000000000000000000 ) ) ;
#10593=CARTESIAN_POINT ( 'NONE',  ( -140.0000507999999968, 4.000000000000000000, -1.000000000000000000 ) ) ;
#10599=CARTESIAN_POINT ( 'NONE',  ( 0.000000000000000000, -19.29292659244022801, 25.53004080487755800 ) ) ;
#10616=DIRECTION ( 'NONE',  ( 0.000000000000000000, 0.000000000000000000, 1.000000000000000000 ) ) ;
#10623=CYLINDRICAL_SURFACE ( 'NONE', #9805, 11.99999999999999822 ) ;
#10628=EDGE_LOOP ( 'NONE', ( #10909, #1159, #7073, #2229 ) ) ;
#10629=DIRECTION ( 'NONE',  ( 0.000000000000000000, 0.000000000000000000, -1.000000000000000000 ) ) ;
#10630=VERTEX_POINT ( 'NONE', #19556 ) ;
#10634=VERTEX_POINT ( 'NONE', #5991 ) ;
#10643=AXIS2_PLACEMENT_3D ( 'NONE', #19650, #4625, #9244 ) ;
#10646=VERTEX_POINT ( 'NONE', #9498 ) ;
#10657=ADVANCED_FACE ( 'NONE', ( #16465 ), #4427, .T. ) ;
#10658=CIRCLE ( 'NONE', #19843, 12.00000000000000000 ) ;
#10668=CARTESIAN_POINT ( 'NONE',  ( 0.000000000000000000, -25.48117629651196125, 10.33947075754252332 ) ) ;
#10669=DIRECTION ( 'NONE',  ( -1.000000000000000000, 0.000000000000000000, 0.000000000000000000 ) ) ;
#10674=ORIENTED_EDGE ( 'NONE', *, *, #4224, .F. ) ;
#10678=VECTOR ( 'NONE', #17236, 1000.000000000000000 ) ;
#10683=VERTEX_POINT ( 'NONE', #21222 ) ;
#10689=ORIENTED_EDGE ( 'NONE', *, *, #14705, .T. ) ;
#10691=DIRECTION ( 'NONE',  ( 0.000000000000000000, 0.000000000000000000, 1.000000000000000000 ) ) ;
#10694=CIRCLE ( 'NONE', #21282, 11.99999999999999822 ) ;
#10699=CARTESIAN_POINT ( 'NONE',  ( 5.000000000000000888, -18.31866948046748078, -26.23788002993743262 ) ) ;
#10705=CIRCLE ( 'NONE', #1893, 27.49900000000000233 ) ;
#10708=DIRECTION ( 'NONE',  ( -1.000000000000000000, 0.000000000000000000, 0.000000000000000000 ) ) ;
#10709=VECTOR ( 'NONE', #9745, 1000.000000000000000 ) ;
#10715=VERTEX_POINT ( 'NONE', #21552 ) ;
#10720=VECTOR ( 'NONE', #13641, 1000.000000000000000 ) ;
#10722=LINE ( 'NONE', #8953, #10782 ) ;
#10724=AXIS2_PLACEMENT_3D ( 'NONE', #18304, #8021, #4695 ) ;
#10727=CARTESIAN_POINT ( 'NONE',  ( 10.00000000000000000, 21.69483248597444813, -16.89761061231758177 ) ) ;
#10730=DIRECTION ( 'NONE',  ( 0.000000000000000000, 0.000000000000000000, 1.000000000000000000 ) ) ;
#10733=CYLINDRICAL_SURFACE ( 'NONE', #14670, 3.000000000000000444 ) ;
#10735=CARTESIAN_POINT ( 'NONE',  ( 0.000000000000000000, 0.000000000000000000, 0.000000000000000000 ) ) ;
#10737=CARTESIAN_POINT ( 'NONE',  ( 0.000000000000000000, 27.26034713664087406, 7.182859710736605230 ) ) ;
#10746=CIRCLE ( 'NONE', #15325, 12.00000000000000178 ) ;
#10751=VECTOR ( 'NONE', #14665, 1000.000000000000000 ) ;
#10757=CARTESIAN_POINT ( 'NONE',  ( 0.000000000000000000, 0.000000000000000000, 0.000000000000000000 ) ) ;
#10759=ORIENTED_EDGE ( 'NONE', *, *, #2457, .T. ) ;
#10762=PLANE ( 'NONE',  #1402 ) ;
#10763=AXIS2_PLACEMENT_3D ( 'NONE', #1039, #806, #2361 ) ;
#10770=ORIENTED_EDGE ( 'NONE', *, *, #144, .F. ) ;
#10771=ORIENTED_EDGE ( 'NONE', *, *, #20124, .F. ) ;
#10772=ORIENTED_EDGE ( 'NONE', *, *, #13560, .T. ) ;
#10781=CIRCLE ( 'NONE', #7968, 32.00000000000000000 ) ;
#10782=VECTOR ( 'NONE', #5542, 1000.000000000000000 ) ;
#10789=EDGE_CURVE ( 'NONE', #11651, #2871, #12796, .T. ) ;
#10791=ORIENTED_EDGE ( 'NONE', *, *, #12270, .T. ) ;
#10793=ORIENTED_EDGE ( 'NONE', *, *, #14080, .T. ) ;
#10794=CARTESIAN_POINT ( 'NONE',  ( 10.00000000000000000, -18.31866948046784316, 26.23788002993718038 ) ) ;
#10806=DIRECTION ( 'NONE',  ( -1.000000000000000000, 0.000000000000000000, 0.000000000000000000 ) ) ;
#10812=DIRECTION ( 'NONE',  ( 0.000000000000000000, 0.5877852522924689183, 0.8090169943749504489 ) ) ;
#10814=AXIS2_PLACEMENT_3D ( 'NONE', #13309, #4813, #16409 ) ;
#10820=ADVANCED_FACE ( 'NONE', ( #3428 ), #20342, .T. ) ;
#10821=VERTEX_POINT ( 'NONE', #10269 ) ;
#10823=VERTEX_POINT ( 'NONE', #16798 ) ;
#10825=EDGE_CURVE ( 'NONE', #1350, #19412, #19512, .T. ) ;
#10833=DIRECTION ( 'NONE',  ( 0.000000000000000000, -1.000000000000000000, 0.000000000000000000 ) ) ;
#10836=CYLINDRICAL_SURFACE ( 'NONE', #16470, 27.49900000000000233 ) ;
#10841=ORIENTED_EDGE ( 'NONE', *, *, #14032, .F. ) ;
#10842=DIRECTION ( 'NONE',  ( -1.000000000000000000, -0.000000000000000000, -0.000000000000000000 ) ) ;
#10843=AXIS2_PLACEMENT_3D ( 'NONE', #5965, #12367, #21537 ) ;
#10857=LINE ( 'NONE', #7142, #7748 ) ;
#10858=VECTOR ( 'NONE', #17147, 1000.000000000000000 ) ;
#10864=CIRCLE ( 'NONE', #1696, 11.99999999999999822 ) ;
#10867=EDGE_CURVE ( 'NONE', #20371, #14005, #104, .T. ) ;
#10877=FACE_OUTER_BOUND ( 'NONE', #12294, .T. ) ;
#10884=VERTEX_POINT ( 'NONE', #5202 ) ;
#10885=EDGE_LOOP ( 'NONE', ( #5896, #20858, #2894, #19661 ) ) ;
#10895=AXIS2_PLACEMENT_3D ( 'NONE', #9465, #2516, #16224 ) ;
#10900=EDGE_CURVE ( 'NONE', #1295, #19418, #8510, .T. ) ;
#10902=DIRECTION ( 'NONE',  ( -1.000000000000000000, -0.000000000000000000, -0.000000000000000000 ) ) ;
#10909=ORIENTED_EDGE ( 'NONE', *, *, #597, .T. ) ;
#10916=CARTESIAN_POINT ( 'NONE',  ( 0.000000000000000000, 19.29292659244005392, 25.53004080487768590 ) ) ;
#10918=DIRECTION ( 'NONE',  ( 0.000000000000000000, 0.8660254037844363761, 0.5000000000000039968 ) ) ;
#10925=LINE ( 'NONE', #20871, #14733 ) ;
#10941=AXIS2_PLACEMENT_3D ( 'NONE', #11835, #11623, #16927 ) ;
#10942=CARTESIAN_POINT ( 'NONE',  ( 10.00000000000000000, 0.000000000000000000, 0.000000000000000000 ) ) ;
#10947=CARTESIAN_POINT ( 'NONE',  ( 10.00000000000000000, 0.000000000000000000, 0.000000000000000000 ) ) ;
#10948=CARTESIAN_POINT ( 'NONE',  ( 10.00000000000000000, 0.000000000000000000, 0.000000000000000000 ) ) ;
#10972=DIRECTION ( 'NONE',  ( -1.000000000000000000, 0.000000000000000000, 0.000000000000000000 ) ) ;
#10974=CIRCLE ( 'NONE', #18035, 32.00000000000000000 ) ;
#10984=CARTESIAN_POINT ( 'NONE',  ( 10.00000000000000000, 28.00896854772012645, -15.47571261340895532 ) ) ;
#10985=VERTEX_POINT ( 'NONE', #19210 ) ;
#10989=EDGE_CURVE ( 'NONE', #14528, #18773, #18455, .T. ) ;
#10997=CARTESIAN_POINT ( 'NONE',  ( 10.00000000000000000, -26.69209308833503513, -6.612652082459592684 ) ) ;
#11006=DIRECTION ( 'NONE',  ( -1.000000000000000000, -0.000000000000000000, 0.000000000000000000 ) ) ;
#11017=VERTEX_POINT ( 'NONE', #12363 ) ;
#11032=EDGE_CURVE ( 'NONE', #15418, #18906, #3965, .T. ) ;
#11033=ORIENTED_EDGE ( 'NONE', *, *, #12584, .F. ) ;
#11036=AXIS2_PLACEMENT_3D ( 'NONE', #20762, #18779, #5517 ) ;
#11038=ADVANCED_FACE ( 'NONE', ( #2308 ), #9040, .T. ) ;
#11041=DIRECTION ( 'NONE',  ( -1.000000000000000000, -0.000000000000000000, -0.000000000000000000 ) ) ;
#11045=CARTESIAN_POINT ( 'NONE',  ( 10.00000000000000000, -12.90282758292962662, -25.06465718894790484 ) ) ;
#11052=CARTESIAN_POINT ( 'NONE',  ( 10.00000000000000000, 24.73395913766480447, -12.01774797440553044 ) ) ;
#11056=CARTESIAN_POINT ( 'NONE',  ( 10.00000000000000000, 27.48365448817206769, 0.9185515634842894572 ) ) ;
#11059=ADVANCED_FACE ( 'NONE', ( #20979 ), #21092, .T. ) ;
#11065=AXIS2_PLACEMENT_3D ( 'NONE', #17420, #13993, #8588 ) ;
#11068=ORIENTED_EDGE ( 'NONE', *, *, #3168, .F. ) ;
#11072=DIRECTION ( 'NONE',  ( 0.000000000000000000, 0.4067366430757948237, 0.9135454576426033091 ) ) ;
#11077=DIRECTION ( 'NONE',  ( -1.000000000000000000, 0.000000000000000000, 0.000000000000000000 ) ) ;
#11079=DIRECTION ( 'NONE',  ( -1.000000000000000000, -0.000000000000000000, 0.000000000000000000 ) ) ;
#11091=ORIENTED_EDGE ( 'NONE', *, *, #10867, .F. ) ;
#11092=EDGE_CURVE ( 'NONE', #20880, #21758, #117, .T. ) ;
#11102=CIRCLE ( 'NONE', #20632, 11.99999999999999645 ) ;
#11103=ORIENTED_EDGE ( 'NONE', *, *, #15907, .F. ) ;
#11106=ORIENTED_EDGE ( 'NONE', *, *, #5159, .F. ) ;
#11109=CIRCLE ( 'NONE', #21689, 11.99999999999999822 ) ;
#11121=DIRECTION ( 'NONE',  ( -1.000000000000000000, -0.000000000000000000, -0.000000000000000000 ) ) ;
#11122=ORIENTED_EDGE ( 'NONE', *, *, #9889, .F. ) ;
#11124=VECTOR ( 'NONE', #16513, 1000.000000000000000 ) ;
#11125=CIRCLE ( 'NONE', #878, 11.99999999999999822 ) ;
#11131=DIRECTION ( 'NONE',  ( -1.000000000000000000, -0.000000000000000000, -0.000000000000000000 ) ) ;
#11132=ORIENTED_EDGE ( 'NONE', *, *, #1722, .F. ) ;
#11133=CARTESIAN_POINT ( 'NONE',  ( 0.000000000000000000, -31.88200538760795766, 2.745493118646878727 ) ) ;
#11142=CYLINDRICAL_SURFACE ( 'NONE', #3292, 32.00000000000000000 ) ;
#11144=VECTOR ( 'NONE', #7128, 1000.000000000000000 ) ;
#11147=FACE_OUTER_BOUND ( 'NONE', #19503, .T. ) ;
#11156=ORIENTED_EDGE ( 'NONE', *, *, #254, .F. ) ;
#11164=DIRECTION ( 'NONE',  ( 0.000000000000000000, 0.000000000000000000, 1.000000000000000000 ) ) ;
#11165=EDGE_CURVE ( 'NONE', #14878, #14805, #19426, .T. ) ;
#11166=CIRCLE ( 'NONE', #13645, 11.99999999999999822 ) ;
#11168=CIRCLE ( 'NONE', #7300, 11.99999999999999822 ) ;
#11170=DIRECTION ( 'NONE',  ( 0.000000000000000000, 0.000000000000000000, 1.000000000000000000 ) ) ;
#11175=EDGE_LOOP ( 'NONE', ( #14929, #3492, #21289, #12586 ) ) ;
#11178=FACE_OUTER_BOUND ( 'NONE', #10306, .T. ) ;
#11179=ORIENTED_EDGE ( 'NONE', *, *, #17493, .F. ) ;
#11181=CARTESIAN_POINT ( 'NONE',  ( 0.000000000000000000, 0.000000000000000000, 0.000000000000000000 ) ) ;
#11184=AXIS2_PLACEMENT_3D ( 'NONE', #6758, #10050, #20223 ) ;
#11188=DIRECTION ( 'NONE',  ( 0.000000000000000000, 0.7431448254773953543, -0.6691306063588570163 ) ) ;
#11189=DIRECTION ( 'NONE',  ( 0.000000000000000000, 0.000000000000000000, 1.000000000000000000 ) ) ;
#11195=DIRECTION ( 'NONE',  ( -1.000000000000000000, 0.000000000000000000, 0.000000000000000000 ) ) ;
#11197=CARTESIAN_POINT ( 'NONE',  ( 10.00000000000000000, 28.15804365424195765, 1.358152127006451826 ) ) ;
#11198=CIRCLE ( 'NONE', #1676, 27.49900000000000233 ) ;
#11200=ORIENTED_EDGE ( 'NONE', *, *, #811, .T. ) ;
#11201=VECTOR ( 'NONE', #10248, 1000.000000000000000 ) ;
#11203=LINE ( 'NONE', #14518, #21028 ) ;
#11209=EDGE_CURVE ( 'NONE', #4988, #21757, #8563, .T. ) ;
#11217=LINE ( 'NONE', #16192, #1342 ) ;
#11220=EDGE_CURVE ( 'NONE', #7792, #142, #10694, .T. ) ;
#11232=VERTEX_POINT ( 'NONE', #18947 ) ;
#11235=DIRECTION ( 'NONE',  ( 0.000000000000000000, 0.000000000000000000, 1.000000000000000000 ) ) ;
#11236=EDGE_CURVE ( 'NONE', #3628, #8974, #2937, .T. ) ;
#11237=ORIENTED_EDGE ( 'NONE', *, *, #7628, .T. ) ;
#11252=AXIS2_PLACEMENT_3D ( 'NONE', #12671, #16099, #4174 ) ;
#11256=DIRECTION ( 'NONE',  ( 0.000000000000000000, 0.000000000000000000, 1.000000000000000000 ) ) ;
#11260=DIRECTION ( 'NONE',  ( -1.000000000000000000, 0.000000000000000000, -0.000000000000000000 ) ) ;
#11263=ORIENTED_EDGE ( 'NONE', *, *, #18830, .T. ) ;
#11265=VERTEX_POINT ( 'NONE', #10541 ) ;
#11266=VECTOR ( 'NONE', #6608, 1000.000000000000000 ) ;
#11268=CIRCLE ( 'NONE', #21512, 11.99999999999999822 ) ;
#11274=VERTEX_POINT ( 'NONE', #1720 ) ;
#11283=CARTESIAN_POINT ( 'NONE',  ( 10.00000000000000000, 0.000000000000000000, 0.000000000000000000 ) ) ;
#11293=VERTEX_POINT ( 'NONE', #10431 ) ;
#11296=CARTESIAN_POINT ( 'NONE',  ( 10.00000000000000000, 27.07404830566976983, -4.815694066514164540 ) ) ;
#11297=ORIENTED_EDGE ( 'NONE', *, *, #6637, .F. ) ;
#11298=ORIENTED_EDGE ( 'NONE', *, *, #14032, .T. ) ;
#11300=CARTESIAN_POINT ( 'NONE',  ( 10.00000000000000000, 17.70753755129037188, 21.03896658273978559 ) ) ;
#11313=DIRECTION ( 'NONE',  ( 0.000000000000000000, -0.5877852522924797984, 0.8090169943749426773 ) ) ;
#11318=( GEOMETRIC_REPRESENTATION_CONTEXT ( 3 ) GLOBAL_UNCERTAINTY_ASSIGNED_CONTEXT ( ( #14969 ) ) GLOBAL_UNIT_ASSIGNED_CONTEXT ( ( #17738, #16286, #18179 ) ) REPRESENTATION_CONTEXT ( 'NONE', 'WORKASPACE' ) );
#11323=LINE ( 'NONE', #6265, #5091 ) ;
#11327=CARTESIAN_POINT ( 'NONE',  ( 10.00000000000000000, 27.26034713664097353, 4.817140289263753594 ) ) ;
#11336=CARTESIAN_POINT ( 'NONE',  ( 10.00000000000000888, 0.000000000000000000, 0.000000000000000000 ) ) ;
#11343=VERTEX_POINT ( 'NONE', #7666 ) ;
#11345=CARTESIAN_POINT ( 'NONE',  ( 0.000000000000000000, 0.000000000000000000, 0.000000000000000000 ) ) ;
#11347=FACE_OUTER_BOUND ( 'NONE', #14954, .T. ) ;
#11356=CIRCLE ( 'NONE', #15232, 27.49900000000000233 ) ;
#11359=CARTESIAN_POINT ( 'NONE',  ( 10.00000000000000000, -24.17932380791704716, -20.96092317127029503 ) ) ;
#11365=ORIENTED_EDGE ( 'NONE', *, *, #21072, .F. ) ;
#11369=EDGE_LOOP ( 'NONE', ( #1348, #17384, #5135, #9533 ) ) ;
#11372=VERTEX_POINT ( 'NONE', #2574 ) ;
#11374=CARTESIAN_POINT ( 'NONE',  ( 0.000000000000000000, 0.000000000000000000, 0.000000000000000000 ) ) ;
#11375=AXIS2_PLACEMENT_3D ( 'NONE', #17673, #6184, #12688 ) ;
#11377=DIRECTION ( 'NONE',  ( 0.000000000000000000, 0.000000000000000000, 1.000000000000000000 ) ) ;
#11378=DIRECTION ( 'NONE',  ( 0.000000000000000000, 0.000000000000000000, 1.000000000000000000 ) ) ;
#11379=DIRECTION ( 'NONE',  ( -1.000000000000000000, 0.000000000000000000, -0.000000000000000000 ) ) ;
#11380=EDGE_CURVE ( 'NONE', #13798, #20540, #4376, .T. ) ;
#11387=CARTESIAN_POINT ( 'NONE',  ( 0.000000000000000000, 0.000000000000000000, 0.000000000000000000 ) ) ;
#11391=AXIS2_PLACEMENT_3D ( 'NONE', #21811, #6703, #13416 ) ;
#11395=AXIS2_PLACEMENT_3D ( 'NONE', #14148, #14254, #21006 ) ;
#11401=DIRECTION ( 'NONE',  ( -1.000000000000000000, 0.000000000000000000, 0.000000000000000000 ) ) ;
#11403=LINE ( 'NONE', #7877, #19202 ) ;
#11407=DIRECTION ( 'NONE',  ( 0.000000000000000000, 0.000000000000000000, 1.000000000000000000 ) ) ;
#11410=LINE ( 'NONE', #18161, #8287 ) ;
#11417=CIRCLE ( 'NONE', #18491, 32.00000000000000000 ) ;
#11419=DIRECTION ( 'NONE',  ( 0.000000000000000000, 0.000000000000000000, 1.000000000000000000 ) ) ;
#11424=VERTEX_POINT ( 'NONE', #7350 ) ;
#11426=VERTEX_POINT ( 'NONE', #5793 ) ;
#11428=EDGE_LOOP ( 'NONE', ( #16508, #13240, #19123, #17575 ) ) ;
#11438=CARTESIAN_POINT ( 'NONE',  ( -10.00000000000000000, 0.000000000000000000, 0.000000000000000000 ) ) ;
#11443=CIRCLE ( 'NONE', #1913, 32.00000000000000000 ) ;
#11446=EDGE_LOOP ( 'NONE', ( #17731, #10183, #20354, #16948 ) ) ;
#11450=AXIS2_PLACEMENT_3D ( 'NONE', #19007, #7084, #3753 ) ;
#11452=CIRCLE ( 'NONE', #912, 27.49900000000000588 ) ;
#11456=VECTOR ( 'NONE', #18622, 1000.000000000000000 ) ;
#11457=ORIENTED_EDGE ( 'NONE', *, *, #10298, .F. ) ;
#11459=DIRECTION ( 'NONE',  ( 0.000000000000000000, 1.000000000000000000, -0.000000000000000000 ) ) ;
#11465=DIRECTION ( 'NONE',  ( 0.000000000000000000, 0.000000000000000000, 1.000000000000000000 ) ) ;
#11466=DIRECTION ( 'NONE',  ( 1.000000000000000000, 0.000000000000000000, 0.000000000000000000 ) ) ;
#11476=CARTESIAN_POINT ( 'NONE',  ( 0.000000000000000000, -17.83210509884626660, -21.83428559348779530 ) ) ;
#11479=ORIENTED_EDGE ( 'NONE', *, *, #11165, .F. ) ;
#11484=ORIENTED_EDGE ( 'NONE', *, *, #10580, .T. ) ;
#11496=EDGE_CURVE ( 'NONE', #9954, #1185, #7203, .T. ) ;
#11498=CARTESIAN_POINT ( 'NONE',  ( 10.00000000000000000, -26.27606311335958011, 10.21217444509402661 ) ) ;
#11503=EDGE_CURVE ( 'NONE', #16515, #9022, #12955, .T. ) ;
#11506=CIRCLE ( 'NONE', #5178, 11.99999999999999822 ) ;
#11513=ORIENTED_EDGE ( 'NONE', *, *, #9969, .F. ) ;
#11522=CIRCLE ( 'NONE', #4821, 11.99999999999999822 ) ;
#11541=CARTESIAN_POINT ( 'NONE',  ( 10.00000000000000000, -26.27606311335958011, 10.21217444509402661 ) ) ;
#11543=VERTEX_POINT ( 'NONE', #20035 ) ;
#11544=VERTEX_POINT ( 'NONE', #16385 ) ;
#11546=EDGE_LOOP ( 'NONE', ( #19584, #14472, #16160, #12053 ) ) ;
#11548=DIRECTION ( 'NONE',  ( 0.000000000000000000, 0.5877852522924743583, -0.8090169943749465631 ) ) ;
#11558=CIRCLE ( 'NONE', #1333, 12.00000000000000178 ) ;
#11560=FACE_OUTER_BOUND ( 'NONE', #7009, .T. ) ;
#11562=LINE ( 'NONE', #6276, #1760 ) ;
#11568=CARTESIAN_POINT ( 'NONE',  ( 5.000000000000000888, 6.063030049135493371, -31.42037024962118608 ) ) ;
#11570=CARTESIAN_POINT ( 'NONE',  ( 10.00000000000000000, -14.53731623274912366, -23.34226719384920656 ) ) ;
#11575=VERTEX_POINT ( 'NONE', #18163 ) ;
#11576=ORIENTED_EDGE ( 'NONE', *, *, #16307, .F. ) ;
#11583=DIRECTION ( 'NONE',  ( 0.000000000000000000, -0.9510565162951503115, -0.3090169943749573878 ) ) ;
#11585=AXIS2_PLACEMENT_3D ( 'NONE', #9626, #8205, #19700 ) ;
#11588=DIRECTION ( 'NONE',  ( 0.000000000000000000, -0.8660254037844431485, 0.4999999999999919509 ) ) ;
#11590=CARTESIAN_POINT ( 'NONE',  ( 5.000000000000000000, -24.17932380791704716, -20.96092317127029503 ) ) ;
#11598=EDGE_CURVE ( 'NONE', #11575, #17610, #3661, .T. ) ;
#11603=CIRCLE ( 'NONE', #4536, 32.00000000000000000 ) ;
#11604=VERTEX_POINT ( 'NONE', #8109 ) ;
#11610=DIRECTION ( 'NONE',  ( -1.000000000000000000, -0.000000000000000000, 0.000000000000000000 ) ) ;
#11623=DIRECTION ( 'NONE',  ( 1.000000000000000000, 0.000000000000000000, 0.000000000000000000 ) ) ;
#11632=CARTESIAN_POINT ( 'NONE',  ( 5.000000000000000000, -28.00896854771981737, -15.47571261340952020 ) ) ;
#11638=CARTESIAN_POINT ( 'NONE',  ( 10.00000000000000000, 19.85071254963777676, 20.01672328094538145 ) ) ;
#11644=ADVANCED_FACE ( 'NONE', ( #18599 ), #10195, .T. ) ;
#11647=ADVANCED_FACE ( 'NONE', ( #15162 ), #9962, .T. ) ;
#11650=CARTESIAN_POINT ( 'NONE',  ( 0.000000000000000000, -27.40684453873955562, -16.51862198942037097 ) ) ;
#11651=VERTEX_POINT ( 'NONE', #21795 ) ;
#11652=DIRECTION ( 'NONE',  ( 0.000000000000000000, 0.7431448254773909134, 0.6691306063588619013 ) ) ;
#11653=VERTEX_POINT ( 'NONE', #20477 ) ;
#11657=EDGE_CURVE ( 'NONE', #4799, #5374, #1189, .T. ) ;
#11660=DIRECTION ( 'NONE',  ( 0.000000000000000000, 0.000000000000000000, 1.000000000000000000 ) ) ;
#11661=CARTESIAN_POINT ( 'NONE',  ( 5.000000000000000888, 13.56333590714014825, 28.98337314858439839 ) ) ;
#11671=EDGE_CURVE ( 'NONE', #8420, #11651, #8261, .T. ) ;
#11673=EDGE_CURVE ( 'NONE', #10646, #5499, #8955, .T. ) ;
#11684=DIRECTION ( 'NONE',  ( 0.000000000000000000, 0.000000000000000000, 1.000000000000000000 ) ) ;
#11687=DIRECTION ( 'NONE',  ( -1.000000000000000000, 0.000000000000000000, -0.000000000000000000 ) ) ;
#11689=FACE_OUTER_BOUND ( 'NONE', #5810, .T. ) ;
#11692=DIRECTION ( 'NONE',  ( 0.000000000000000000, 0.000000000000000000, 1.000000000000000000 ) ) ;
#11704=ORIENTED_EDGE ( 'NONE', *, *, #6376, .T. ) ;
#11705=ORIENTED_EDGE ( 'NONE', *, *, #2464, .T. ) ;
#11707=ORIENTED_EDGE ( 'NONE', *, *, #14983, .T. ) ;
#11713=CARTESIAN_POINT ( 'NONE',  ( 10.00000000000000000, -26.69209308833512395, 6.612652082459228531 ) ) ;
#11717=ORIENTED_EDGE ( 'NONE', *, *, #21665, .F. ) ;
#11720=VERTEX_POINT ( 'NONE', #3567 ) ;
#11722=ORIENTED_EDGE ( 'NONE', *, *, #15518, .F. ) ;
#11731=CARTESIAN_POINT ( 'NONE',  ( 0.000000000000000000, -28.00896854771981737, -15.47571261340952020 ) ) ;
#11736=CARTESIAN_POINT ( 'NONE',  ( 10.00000000000000000, 23.57863763525720202, 15.45211464167672588 ) ) ;
#11739=VECTOR ( 'NONE', #17454, 1000.000000000000000 ) ;
#11744=CIRCLE ( 'NONE', #12787, 32.00000000000000000 ) ;
#11746=DIRECTION ( 'NONE',  ( -1.000000000000000000, 0.000000000000000000, 0.000000000000000000 ) ) ;
#11751=EDGE_LOOP ( 'NONE', ( #4436, #4141, #6877, #21666 ) ) ;
#11766=CARTESIAN_POINT ( 'NONE',  ( 0.000000000000000000, 0.000000000000000000, 0.000000000000000000 ) ) ;
#11771=ORIENTED_EDGE ( 'NONE', *, *, #5859, .F. ) ;
#11772=CARTESIAN_POINT ( 'NONE',  ( 0.000000000000000000, 0.000000000000000000, 0.000000000000000000 ) ) ;
#11775=FACE_OUTER_BOUND ( 'NONE', #5872, .T. ) ;
#11778=DIRECTION ( 'NONE',  ( 0.000000000000000000, 0.000000000000000000, 1.000000000000000000 ) ) ;
#11783=PLANE ( 'NONE',  #15911 ) ;
#11784=EDGE_CURVE ( 'NONE', #1543, #11604, #4095, .T. ) ;
#11788=VERTEX_POINT ( 'NONE', #14048 ) ;
#11794=DIRECTION ( 'NONE',  ( 0.000000000000000000, -0.2079116908177469081, -0.9781476007338082423 ) ) ;
#11807=AXIS2_PLACEMENT_3D ( 'NONE', #2711, #14643, #4595 ) ;
#11808=ORIENTED_EDGE ( 'NONE', *, *, #8035, .T. ) ;
#11819=CARTESIAN_POINT ( 'NONE',  ( 0.000000000000000000, 7.409634587003466777, -27.19958299168149907 ) ) ;
#11825=AXIS2_PLACEMENT_3D ( 'NONE', #5407, #8926, #21787 ) ;
#11832=CIRCLE ( 'NONE', #2663, 32.00000000000000000 ) ;
#11834=AXIS2_PLACEMENT_3D ( 'NONE', #9523, #16272, #9625 ) ;
#11835=CARTESIAN_POINT ( 'NONE',  ( 0.000000000000000000, -28.15804365424196121, -1.358152127006266197 ) ) ;
#11840=DIRECTION ( 'NONE',  ( 0.000000000000000000, 0.000000000000000000, 1.000000000000000000 ) ) ;
#11842=EDGE_CURVE ( 'NONE', #17498, #14985, #19263, .T. ) ;
#11843=CIRCLE ( 'NONE', #16415, 32.00000000000000000 ) ;
#11845=CIRCLE ( 'NONE', #1266, 12.00000000000000178 ) ;
#11851=ADVANCED_FACE ( 'NONE', ( #685 ), #5766, .T. ) ;
#11854=DIRECTION ( 'NONE',  ( 1.000000000000000000, 0.000000000000000000, 0.000000000000000000 ) ) ;
#11856=VECTOR ( 'NONE', #6097, 1000.000000000000000 ) ;
#11857=ORIENTED_EDGE ( 'NONE', *, *, #3645, .F. ) ;
#11858=FACE_OUTER_BOUND ( 'NONE', #13920, .T. ) ;
#11865=ORIENTED_EDGE ( 'NONE', *, *, #21072, .T. ) ;
#11869=VERTEX_POINT ( 'NONE', #778 ) ;
#11871=CARTESIAN_POINT ( 'NONE',  ( 10.00000000000000000, -21.98203405400967014, 17.64965094506536403 ) ) ;
#11879=VECTOR ( 'NONE', #8460, 1000.000000000000000 ) ;
#11880=AXIS2_PLACEMENT_3D ( 'NONE', #18987, #17224, #3620 ) ;
#11883=ADVANCED_FACE ( 'NONE', ( #19350 ), #4217, .T. ) ;
#11888=DIRECTION ( 'NONE',  ( -1.000000000000000000, -0.000000000000000000, 0.000000000000000000 ) ) ;
#11895=EDGE_CURVE ( 'NONE', #19418, #21758, #9018, .T. ) ;
#11896=CIRCLE ( 'NONE', #17547, 32.00000000000000000 ) ;
#11899=FACE_OUTER_BOUND ( 'NONE', #4585, .T. ) ;
#11901=ORIENTED_EDGE ( 'NONE', *, *, #21081, .T. ) ;
#11902=CARTESIAN_POINT ( 'NONE',  ( 10.00000000000000000, -27.26034713664092379, -7.182859710736426706 ) ) ;
#11904=CARTESIAN_POINT ( 'NONE',  ( 10.00000000000000000, 0.000000000000000000, 0.000000000000000000 ) ) ;
#11905=CARTESIAN_POINT ( 'NONE',  ( -140.0000507999999968, 4.000000000000000000, 0.000000000000000000 ) ) ;
#11907=DIRECTION ( 'NONE',  ( -1.000000000000000000, 0.000000000000000000, 0.000000000000000000 ) ) ;
#11908=EDGE_CURVE ( 'NONE', #15667, #5499, #1009, .T. ) ;
#11909=CARTESIAN_POINT ( 'NONE',  ( 5.000000000000000000, -18.31866948046784671, 26.23788002993718393 ) ) ;
#11914=CARTESIAN_POINT ( 'NONE',  ( -140.0000507999999968, 6.123233995736766282E-16, 5.000000000000000000 ) ) ;
#11919=DIRECTION ( 'NONE',  ( 0.000000000000000000, 0.000000000000000000, 1.000000000000000000 ) ) ;
#11921=DIRECTION ( 'NONE',  ( -1.000000000000000000, 0.000000000000000000, 0.000000000000000000 ) ) ;
#11923=ORIENTED_EDGE ( 'NONE', *, *, #15759, .F. ) ;
#11927=SHAPE_REPRESENTATION ( 'spur gear_iso_ISO - Spur gear 2M 30T 20PA 10FW ---S30B10H150L6.0S1', ( #15567 ), #19439 ) ;
#11930=ADVANCED_FACE ( 'NONE', ( #3957 ), #14451, .T. ) ;
#11931=VERTEX_POINT ( 'NONE', #970 ) ;
#11933=CIRCLE ( 'NONE', #2749, 11.99999999999999822 ) ;
#11937=CYLINDRICAL_SURFACE ( 'NONE', #951, 11.99999999999999822 ) ;
#11938=DIRECTION ( 'NONE',  ( -1.000000000000000000, 0.000000000000000000, 0.000000000000000000 ) ) ;
#11947=VECTOR ( 'NONE', #12518, 1000.000000000000000 ) ;
#11950=EDGE_CURVE ( 'NONE', #13666, #13798, #20758, .T. ) ;
#11954=FACE_OUTER_BOUND ( 'NONE', #15037, .T. ) ;
#11955=VERTEX_POINT ( 'NONE', #12777 ) ;
#11969=DIRECTION ( 'NONE',  ( -1.000000000000000000, -0.000000000000000000, 0.000000000000000000 ) ) ;
#11978=CARTESIAN_POINT ( 'NONE',  ( 10.00000000000000000, 24.73395913766463750, 12.01774797440586084 ) ) ;
#11979=ORIENTED_EDGE ( 'NONE', *, *, #10150, .T. ) ;
#11980=ORIENTED_EDGE ( 'NONE', *, *, #12600, .T. ) ;
#11983=CARTESIAN_POINT ( 'NONE',  ( 0.000000000000000000, -19.85071254963763465, -20.01672328094552356 ) ) ;
#11987=DIRECTION ( 'NONE',  ( -1.000000000000000000, 0.000000000000000000, 0.000000000000000000 ) ) ;
#11989=AXIS2_PLACEMENT_3D ( 'NONE', #8330, #20376, #1701 ) ;
#11990=ORIENTED_EDGE ( 'NONE', *, *, #7093, .T. ) ;
#11999=DIRECTION ( 'NONE',  ( 0.000000000000000000, 0.000000000000000000, -1.000000000000000000 ) ) ;
#12000=ORIENTED_EDGE ( 'NONE', *, *, #19059, .T. ) ;
#12006=CIRCLE ( 'NONE', #18012, 11.99999999999999822 ) ;
#12009=CARTESIAN_POINT ( 'NONE',  ( 10.00000000000000000, 1.592605004253184964, -28.14575649959892445 ) ) ;
#12023=AXIS2_PLACEMENT_3D ( 'NONE', #13269, #18145, #20237 ) ;
#12026=EDGE_CURVE ( 'NONE', #7417, #1350, #1982, .T. ) ;
#12031=ORIENTED_EDGE ( 'NONE', *, *, #5792, .T. ) ;
#12036=CARTESIAN_POINT ( 'NONE',  ( 0.000000000000000000, 0.000000000000000000, 0.000000000000000000 ) ) ;
#12053=ORIENTED_EDGE ( 'NONE', *, *, #8124, .T. ) ;
#12054=EDGE_CURVE ( 'NONE', #16691, #1024, #855, .T. ) ;
#12058=CARTESIAN_POINT ( 'NONE',  ( 10.00000000000000000, 0.000000000000000000, 0.000000000000000000 ) ) ;
#12062=EDGE_CURVE ( 'NONE', #16531, #5649, #9354, .T. ) ;
#12063=EDGE_CURVE ( 'NONE', #10683, #4886, #525, .T. ) ;
#12064=DIRECTION ( 'NONE',  ( -1.000000000000000000, 0.000000000000000000, 0.000000000000000000 ) ) ;
#12069=DIRECTION ( 'NONE',  ( -1.000000000000000000, 0.000000000000000000, -0.000000000000000000 ) ) ;
#12072=ORIENTED_EDGE ( 'NONE', *, *, #1722, .T. ) ;
#12077=VECTOR ( 'NONE', #13607, 1000.000000000000000 ) ;
#12082=VECTOR ( 'NONE', #8608, 1000.000000000000000 ) ;
#12094=VERTEX_POINT ( 'NONE', #1186 ) ;
#12106=FACE_OUTER_BOUND ( 'NONE', #15854, .T. ) ;
#12112=EDGE_CURVE ( 'NONE', #1041, #4641, #8156, .T. ) ;
#12114=LINE ( 'NONE', #13671, #9636 ) ;
#12125=ORIENTED_EDGE ( 'NONE', *, *, #6788, .T. ) ;
#12138=EDGE_CURVE ( 'NONE', #13033, #2027, #6292, .T. ) ;
#12140=FACE_OUTER_BOUND ( 'NONE', #9232, .T. ) ;
#12145=DIRECTION ( 'NONE',  ( -1.000000000000000000, 0.000000000000000000, -0.000000000000000000 ) ) ;
#12146=CARTESIAN_POINT ( 'NONE',  ( 10.00000000000000000, 23.57863763525720202, 15.45211464167672588 ) ) ;
#12148=ORIENTED_EDGE ( 'NONE', *, *, #10137, .F. ) ;
#12150=FACE_OUTER_BOUND ( 'NONE', #15950, .T. ) ;
#12160=VECTOR ( 'NONE', #706, 1000.000000000000000 ) ;
#12161=CARTESIAN_POINT ( 'NONE',  ( 10.00000000000000000, 0.000000000000000000, 0.000000000000000000 ) ) ;
#12166=CIRCLE ( 'NONE', #11825, 27.49900000000000233 ) ;
#12169=FACE_OUTER_BOUND ( 'NONE', #5012, .T. ) ;
#12175=ORIENTED_EDGE ( 'NONE', *, *, #21463, .F. ) ;
#12191=ORIENTED_EDGE ( 'NONE', *, *, #3645, .T. ) ;
#12207=ORIENTED_EDGE ( 'NONE', *, *, #17292, .F. ) ;
#12212=AXIS2_PLACEMENT_3D ( 'NONE', #21220, #9914, #11465 ) ;
#12215=DIRECTION ( 'NONE',  ( 1.000000000000000000, 0.000000000000000000, 0.000000000000000000 ) ) ;
#12219=EDGE_LOOP ( 'NONE', ( #20059, #16429, #18067, #5213 ) ) ;
#12221=CARTESIAN_POINT ( 'NONE',  ( 150.0000507999999968, 4.000000000000000000, -1.000000000000000000 ) ) ;
#12225=CIRCLE ( 'NONE', #11880, 11.99999999999999822 ) ;
#12229=CARTESIAN_POINT ( 'NONE',  ( 10.00000000000000000, 0.000000000000000000, 0.000000000000000000 ) ) ;
#12230=DIRECTION ( 'NONE',  ( -1.000000000000000000, 0.000000000000000000, 0.000000000000000000 ) ) ;
#12231=ORIENTED_EDGE ( 'NONE', *, *, #118, .F. ) ;
#12233=EDGE_CURVE ( 'NONE', #4620, #16625, #1639, .T. ) ;
#12255=CYLINDRICAL_SURFACE ( 'NONE', #15421, 11.99999999999999645 ) ;
#12256=CARTESIAN_POINT ( 'NONE',  ( 10.00000000000000000, -30.24235385705231138, -10.45944707835137955 ) ) ;
#12258=CYLINDRICAL_SURFACE ( 'NONE', #5879, 12.00000000000000000 ) ;
#12260=EDGE_CURVE ( 'NONE', #20991, #5507, #8336, .T. ) ;
#12266=AXIS2_PLACEMENT_3D ( 'NONE', #1805, #11969, #3572 ) ;
#12270=EDGE_CURVE ( 'NONE', #142, #15171, #16751, .T. ) ;
#12277=LINE ( 'NONE', #1798, #14390 ) ;
#12280=FACE_OUTER_BOUND ( 'NONE', #20183, .T. ) ;
#12282=VECTOR ( 'NONE', #12703, 1000.000000000000000 ) ;
#12285=AXIS2_PLACEMENT_3D ( 'NONE', #11181, #15835, #698 ) ;
#12287=CIRCLE ( 'NONE', #19706, 32.00000000000000000 ) ;
#12290=EDGE_CURVE ( 'NONE', #9822, #2850, #2683, .T. ) ;
#12293=CARTESIAN_POINT ( 'NONE',  ( 0.000000000000000000, -27.82509854686814066, 4.525913221811051379 ) ) ;
#12294=EDGE_LOOP ( 'NONE', ( #1905, #7654, #7494, #7255 ) ) ;
#12296=ORIENTED_EDGE ( 'NONE', *, *, #1888, .T. ) ;
#12300=ORIENTED_EDGE ( 'NONE', *, *, #12138, .F. ) ;
#12323=CARTESIAN_POINT ( 'NONE',  ( 150.0000507999999968, 0.000000000000000000, 1.000000000000000000 ) ) ;
#12325=ORIENTED_EDGE ( 'NONE', *, *, #17618, .T. ) ;
#12337=VECTOR ( 'NONE', #6899, 1000.000000000000000 ) ;
#12348=CARTESIAN_POINT ( 'NONE',  ( 10.00000000000000000, 0.000000000000000000, 0.000000000000000000 ) ) ;
#12352=AXIS2_PLACEMENT_3D ( 'NONE', #4885, #16692, #18472 ) ;
#12353=CARTESIAN_POINT ( 'NONE',  ( 10.00000000000000000, -9.366510754379051562, -25.85466064925435603 ) ) ;
#12358=ORIENTED_EDGE ( 'NONE', *, *, #20511, .T. ) ;
#12363=CARTESIAN_POINT ( 'NONE',  ( 10.00000000000000000, -27.07404830566967746, -4.815694066514710769 ) ) ;
#12367=DIRECTION ( 'NONE',  ( -1.000000000000000000, 0.000000000000000000, 0.000000000000000000 ) ) ;
#12377=LINE ( 'NONE', #19122, #9815 ) ;
#12378=EDGE_LOOP ( 'NONE', ( #240, #15713, #6799, #4562 ) ) ;
#12380=CYLINDRICAL_SURFACE ( 'NONE', #17022, 27.49900000000000233 ) ;
#12389=EDGE_CURVE ( 'NONE', #17888, #11293, #19230, .T. ) ;
#12391=CARTESIAN_POINT ( 'NONE',  ( 0.000000000000000000, 18.31866948046803145, -26.23788002993705248 ) ) ;
#12392=ORIENTED_EDGE ( 'NONE', *, *, #10900, .T. ) ;
#12405=CARTESIAN_POINT ( 'NONE',  ( 0.000000000000000000, -23.37352460145298139, 21.85585385440871775 ) ) ;
#12410=ORIENTED_EDGE ( 'NONE', *, *, #20124, .T. ) ;
#12417=CIRCLE ( 'NONE', #17372, 27.49900000000000233 ) ;
#12431=DIRECTION ( 'NONE',  ( -1.000000000000000000, -0.000000000000000000, 0.000000000000000000 ) ) ;
#12433=ADVANCED_FACE ( 'NONE', ( #5381 ), #20623, .T. ) ;
#12438=ORIENTED_EDGE ( 'NONE', *, *, #1886, .T. ) ;
#12442=DIRECTION ( 'NONE',  ( -1.000000000000000000, -0.000000000000000000, -0.000000000000000000 ) ) ;
#12447=LINE ( 'NONE', #19095, #4184 ) ;
#12449=ORIENTED_EDGE ( 'NONE', *, *, #4346, .T. ) ;
#12454=EDGE_CURVE ( 'NONE', #11232, #18476, #8305, .T. ) ;
#12458=AXIS2_PLACEMENT_3D ( 'NONE', #13014, #1084, #14669 ) ;
#12475=ORIENTED_EDGE ( 'NONE', *, *, #9867, .F. ) ;
#12485=CARTESIAN_POINT ( 'NONE',  ( 0.000000000000000000, 17.83210509884670714, -21.83428559348744002 ) ) ;
#12487=FACE_OUTER_BOUND ( 'NONE', #17661, .T. ) ;
#12488=AXIS2_PLACEMENT_3D ( 'NONE', #19372, #10532, #10423 ) ;
#12489=CARTESIAN_POINT ( 'NONE',  ( 10.00000000000000000, 0.000000000000000000, 0.000000000000000000 ) ) ;
#12490=DIRECTION ( 'NONE',  ( -1.000000000000000000, -0.000000000000000000, -0.000000000000000000 ) ) ;
#12498=CARTESIAN_POINT ( 'NONE',  ( 5.000000000000000888, -0.6021240089799216877, -31.99433460282945063 ) ) ;
#12501=EDGE_LOOP ( 'NONE', ( #10238, #17477, #14116, #12125 ) ) ;
#12502=AXIS2_PLACEMENT_3D ( 'NONE', #7079, #13805, #20546 ) ;
#12516=AXIS2_PLACEMENT_3D ( 'NONE', #7053, #10669, #514 ) ;
#12518=DIRECTION ( 'NONE',  ( -1.000000000000000000, 0.000000000000000000, -0.000000000000000000 ) ) ;
#12519=DIRECTION ( 'NONE',  ( 0.000000000000000000, 0.5877852522924689183, 0.8090169943749504489 ) ) ;
#12524=VERTEX_POINT ( 'NONE', #14316 ) ;
#12528=DIRECTION ( 'NONE',  ( 0.000000000000000000, 0.000000000000000000, 1.000000000000000000 ) ) ;
#12537=ORIENTED_EDGE ( 'NONE', *, *, #5847, .F. ) ;
#12539=EDGE_LOOP ( 'NONE', ( #7305, #1995, #7896, #996 ) ) ;
#12544=DIRECTION ( 'NONE',  ( -1.000000000000000000, -0.000000000000000000, -0.000000000000000000 ) ) ;
#12549=ADVANCED_FACE ( 'NONE', ( #5929 ), #736, .T. ) ;
#12551=ORIENTED_EDGE ( 'NONE', *, *, #18013, .T. ) ;
#12556=ORIENTED_EDGE ( 'NONE', *, *, #19060, .T. ) ;
#12573=CARTESIAN_POINT ( 'NONE',  ( 0.000000000000000000, -25.48117629651182270, -10.33947075754286793 ) ) ;
#12574=CYLINDRICAL_SURFACE ( 'NONE', #2228, 11.99999999999999645 ) ;
#12583=VECTOR ( 'NONE', #9172, 1000.000000000000000 ) ;
#12584=EDGE_CURVE ( 'NONE', #18503, #12821, #11125, .T. ) ;
#12585=CYLINDRICAL_SURFACE ( 'NONE', #16802, 12.00000000000000000 ) ;
#12586=ORIENTED_EDGE ( 'NONE', *, *, #10199, .T. ) ;
#12591=ORIENTED_EDGE ( 'NONE', *, *, #10989, .T. ) ;
#12596=DIRECTION ( 'NONE',  ( 0.000000000000000000, 0.000000000000000000, -1.000000000000000000 ) ) ;
#12598=CARTESIAN_POINT ( 'NONE',  ( 0.000000000000000000, 9.366510754379572035, -25.85466064925416774 ) ) ;
#12600=EDGE_CURVE ( 'NONE', #7213, #16952, #14428, .T. ) ;
#12618=ORIENTED_EDGE ( 'NONE', *, *, #8964, .F. ) ;
#12621=CARTESIAN_POINT ( 'NONE',  ( 0.000000000000000000, -9.366510754379051562, -25.85466064925435603 ) ) ;
#12626=AXIS2_PLACEMENT_3D ( 'NONE', #10083, #12069, #16832 ) ;
#12632=CARTESIAN_POINT ( 'NONE',  ( 0.000000000000000000, -30.61448696004458370, 9.314139153634124924 ) ) ;
#12636=ORIENTED_EDGE ( 'NONE', *, *, #16050, .F. ) ;
#12638=ORIENTED_EDGE ( 'NONE', *, *, #811, .F. ) ;
#12644=CIRCLE ( 'NONE', #17598, 32.00000000000000000 ) ;
#12646=ORIENTED_EDGE ( 'NONE', *, *, #16613, .T. ) ;
#12647=EDGE_LOOP ( 'NONE', ( #6532, #11990, #11237, #20966, #16517, #5096, #12296, #19440, #3547, #8131, #14405, #17966, #8071, #8825, #2925, #14195, #5529, #21829, #10265, #16343, #18883, #17229, #8763, #13073, #9983, #16390, #9459, #1702, #9137, #13859, #12591, #13100, #5040, #19881, #15768, #9976, #8515, #15471, #6339, #9647, #18724, #13624, #4677, #2491, #14081, #4226, #1814, #17818, #8684, #5019, #12410, #12031, #14658, #3771, #5700, #17763, #9005, #9762, #10558, #934, #9024, #11717, #4665, #4149, #11865, #20459, #28, #8582, #9056, #15698, #3193, #9464, #18877, #14871, #19628, #10356, #16653, #9908, #9375, #6050, #17680, #14041, #17225, #2064, #10234, #2213, #1859, #17443, #12325, #19435, #6669, #17612, #818, #18703, #14207, #16124, #17765, #14827, #3303, #1131, #6115, #1839, #8947, #2409, #15892, #14378, #7137, #17525, #4282, #4393, #10518, #19795, #4179, #703, #18376, #6936, #4986, #13242, #7734, #4565, #9694, #689, #12000, #15647, #19333 ) ) ;
#12652=CARTESIAN_POINT ( 'NONE',  ( 10.00000000000000000, -22.77465461094683974, 15.41136296218079238 ) ) ;
#12653=DIRECTION ( 'NONE',  ( 1.000000000000000000, 0.000000000000000000, 0.000000000000000000 ) ) ;
#12657=DIRECTION ( 'NONE',  ( 1.000000000000000000, 0.000000000000000000, 0.000000000000000000 ) ) ;
#12664=DIRECTION ( 'NONE',  ( 0.000000000000000000, 0.000000000000000000, 1.000000000000000000 ) ) ;
#12666=FACE_OUTER_BOUND ( 'NONE', #4750, .T. ) ;
#12669=CARTESIAN_POINT ( 'NONE',  ( 10.00000000000000000, -7.619321854369744074, 26.42235673590688094 ) ) ;
#12671=CARTESIAN_POINT ( 'NONE',  ( 0.000000000000000000, -27.26034713664092379, -7.182859710736426706 ) ) ;
#12676=VECTOR ( 'NONE', #8993, 1000.000000000000000 ) ;
#12682=DIRECTION ( 'NONE',  ( 0.000000000000000000, 0.000000000000000000, 1.000000000000000000 ) ) ;
#12683=DIRECTION ( 'NONE',  ( -1.000000000000000000, 0.000000000000000000, 0.000000000000000000 ) ) ;
#12688=DIRECTION ( 'NONE',  ( 0.000000000000000000, 0.000000000000000000, 1.000000000000000000 ) ) ;
#12690=DIRECTION ( 'NONE',  ( -1.000000000000000000, 0.000000000000000000, -0.000000000000000000 ) ) ;
#12691=CYLINDRICAL_SURFACE ( 'NONE', #3142, 32.00000000000000000 ) ;
#12694=AXIS2_PLACEMENT_3D ( 'NONE', #3264, #1935, #18738 ) ;
#12703=DIRECTION ( 'NONE',  ( -1.000000000000000000, 0.000000000000000000, 0.000000000000000000 ) ) ;
#12704=EDGE_LOOP ( 'NONE', ( #13129, #9512, #16425, #5080 ) ) ;
#12715=EDGE_CURVE ( 'NONE', #13000, #2742, #21709, .T. ) ;
#12721=CARTESIAN_POINT ( 'NONE',  ( 10.00000000000000000, 1.592605004252791279, 28.14575649959894932 ) ) ;
#12726=ORIENTED_EDGE ( 'NONE', *, *, #1198, .F. ) ;
#12737=CARTESIAN_POINT ( 'NONE',  ( 0.000000000000000000, 14.53731623274928708, 23.34226719384910709 ) ) ;
#12743=EDGE_CURVE ( 'NONE', #20936, #1592, #1285, .T. ) ;
#12744=VERTEX_POINT ( 'NONE', #13092 ) ;
#12746=ORIENTED_EDGE ( 'NONE', *, *, #11032, .F. ) ;
#12748=VECTOR ( 'NONE', #10432, 1000.000000000000000 ) ;
#12749=DIRECTION ( 'NONE',  ( 0.000000000000000000, 0.000000000000000000, 1.000000000000000000 ) ) ;
#12760=CARTESIAN_POINT ( 'NONE',  ( 5.000000000000000000, 12.46320060045762013, -29.47318494484016327 ) ) ;
#12761=DIRECTION ( 'NONE',  ( 0.000000000000000000, -0.4067366430757888285, -0.9135454576426059736 ) ) ;
#12762=LINE ( 'NONE', #7477, #15079 ) ;
#12763=VERTEX_POINT ( 'NONE', #9988 ) ;
#12766=CARTESIAN_POINT ( 'NONE',  ( 10.00000000000000000, -25.17124263951000529, -12.69364185792245081 ) ) ;
#12771=CARTESIAN_POINT ( 'NONE',  ( -10.00000000000000000, 0.000000000000000000, 0.000000000000000000 ) ) ;
#12777=CARTESIAN_POINT ( 'NONE',  ( 0.000000000000000000, -28.00896854772002342, 15.47571261340914539 ) ) ;
#12780=CIRCLE ( 'NONE', #16672, 12.00000000000000000 ) ;
#12785=CARTESIAN_POINT ( 'NONE',  ( 10.00000000000000000, -14.53731623274945406, 23.34226719384900761 ) ) ;
#12786=DIRECTION ( 'NONE',  ( -1.000000000000000000, -0.000000000000000000, -0.000000000000000000 ) ) ;
#12787=AXIS2_PLACEMENT_3D ( 'NONE', #20627, #15646, #10464 ) ;
#12792=VERTEX_POINT ( 'NONE', #18732 ) ;
#12796=CIRCLE ( 'NONE', #13499, 11.99999999999999822 ) ;
#12797=CIRCLE ( 'NONE', #10643, 27.49900000000000233 ) ;
#12800=AXIS2_PLACEMENT_3D ( 'NONE', #8223, #8126, #15066 ) ;
#12802=CARTESIAN_POINT ( 'NONE',  ( 10.00000000000000000, 0.000000000000000000, 0.000000000000000000 ) ) ;
#12806=DIRECTION ( 'NONE',  ( -1.000000000000000000, -0.000000000000000000, 0.000000000000000000 ) ) ;
#12807=CIRCLE ( 'NONE', #6133, 12.00000000000000000 ) ;
#12812=DIRECTION ( 'NONE',  ( -1.000000000000000000, -0.000000000000000000, -0.000000000000000000 ) ) ;
#12813=EDGE_CURVE ( 'NONE', #9285, #19310, #7611, .T. ) ;
#12814=CARTESIAN_POINT ( 'NONE',  ( 10.00000000000000000, 0.000000000000000000, 0.000000000000000000 ) ) ;
#12816=ORIENTED_EDGE ( 'NONE', *, *, #13405, .F. ) ;
#12817=CIRCLE ( 'NONE', #10000, 11.99999999999999822 ) ;
#12819=FACE_OUTER_BOUND ( 'NONE', #19218, .T. ) ;
#12821=VERTEX_POINT ( 'NONE', #15186 ) ;
#12822=LINE ( 'NONE', #19572, #10174 ) ;
#12826=ORIENTED_EDGE ( 'NONE', *, *, #15165, .F. ) ;
#12840=DIRECTION ( 'NONE',  ( 0.000000000000000000, -0.9510565162951565288, 0.3090169943749382919 ) ) ;
#12847=DIRECTION ( 'NONE',  ( 0.000000000000000000, -0.4067366430757888285, -0.9135454576426059736 ) ) ;
#12850=EDGE_CURVE ( 'NONE', #1024, #17734, #17850, .T. ) ;
#12859=CYLINDRICAL_SURFACE ( 'NONE', #20457, 32.00000000000000000 ) ;
#12871=EDGE_CURVE ( 'NONE', #21761, #13692, #13962, .T. ) ;
#12875=CARTESIAN_POINT ( 'NONE',  ( 0.000000000000000000, 0.000000000000000000, 0.000000000000000000 ) ) ;
#12881=CARTESIAN_POINT ( 'NONE',  ( 10.00000000000000000, 30.61448696004452330, 9.314139153634327428 ) ) ;
#12883=AXIS2_PLACEMENT_3D ( 'NONE', #17220, #3517, #8816 ) ;
#12888=CIRCLE ( 'NONE', #19232, 12.00000000000000000 ) ;
#12890=CARTESIAN_POINT ( 'NONE',  ( 0.000000000000000000, -13.56333590714035253, 28.98337314858430602 ) ) ;
#12894=ORIENTED_EDGE ( 'NONE', *, *, #18928, .F. ) ;
#12896=CIRCLE ( 'NONE', #18560, 11.99999999999999822 ) ;
#12899=CYLINDRICAL_SURFACE ( 'NONE', #5972, 27.49900000000000233 ) ;
#12905=VECTOR ( 'NONE', #21600, 1000.000000000000000 ) ;
#12906=AXIS2_PLACEMENT_3D ( 'NONE', #15820, #15708, #7210 ) ;
#12911=DIRECTION ( 'NONE',  ( 0.000000000000000000, -0.9945218953682722907, -0.1045284632676635739 ) ) ;
#12919=ORIENTED_EDGE ( 'NONE', *, *, #14582, .F. ) ;
#12930=CARTESIAN_POINT ( 'NONE',  ( 0.000000000000000000, 3.786343810537573074, 27.23708136986053674 ) ) ;
#12942=ORIENTED_EDGE ( 'NONE', *, *, #8486, .F. ) ;
#12943=EDGE_LOOP ( 'NONE', ( #14137, #17879, #16959, #17992 ) ) ;
#12955=LINE ( 'NONE', #18276, #10709 ) ;
#12964=AXIS2_PLACEMENT_3D ( 'NONE', #16991, #8590, #13341 ) ;
#12976=AXIS2_PLACEMENT_3D ( 'NONE', #19250, #16151, #5665 ) ;
#12977=EDGE_LOOP ( 'NONE', ( #8656, #13985, #12392, #18615 ) ) ;
#12979=DIRECTION ( 'NONE',  ( -1.000000000000000000, 0.000000000000000000, 0.000000000000000000 ) ) ;
#12985=CARTESIAN_POINT ( 'NONE',  ( 10.00000000000000000, 4.000000000000000000, 0.000000000000000000 ) ) ;
#12989=CARTESIAN_POINT ( 'NONE',  ( 0.000000000000000000, -12.94633825542249994, -24.26081875733348170 ) ) ;
#12992=DIRECTION ( 'NONE',  ( 0.000000000000000000, 0.000000000000000000, 1.000000000000000000 ) ) ;
#13000=VERTEX_POINT ( 'NONE', #12405 ) ;
#13008=DIRECTION ( 'NONE',  ( 1.000000000000000000, 0.000000000000000000, -0.000000000000000000 ) ) ;
#13009=EDGE_CURVE ( 'NONE', #18240, #11426, #233, .T. ) ;
#13014=CARTESIAN_POINT ( 'NONE',  ( 0.000000000000000000, 17.83210509884640871, 21.83428559348767806 ) ) ;
#13025=CYLINDRICAL_SURFACE ( 'NONE', #1232, 32.00000000000000000 ) ;
#13029=AXIS2_PLACEMENT_3D ( 'NONE', #5695, #18643, #3497 ) ;
#13030=ORIENTED_EDGE ( 'NONE', *, *, #20691, .F. ) ;
#13031=AXIS2_PLACEMENT_3D ( 'NONE', #3496, #20184, #10232 ) ;
#13032=AXIS2_PLACEMENT_3D ( 'NONE', #6842, #10466, #17218 ) ;
#13033=VERTEX_POINT ( 'NONE', #9197 ) ;
#13039=CARTESIAN_POINT ( 'NONE',  ( 0.000000000000000000, 7.240962358591984227, -31.16999300804307538 ) ) ;
#13043=AXIS2_PLACEMENT_3D ( 'NONE', #6487, #21180, #12992 ) ;
#13048=ORIENTED_EDGE ( 'NONE', *, *, #21029, .T. ) ;
#13049=VERTEX_POINT ( 'NONE', #14511 ) ;
#13055=ORIENTED_EDGE ( 'NONE', *, *, #7423, .F. ) ;
#13067=DIRECTION ( 'NONE',  ( 0.000000000000000000, 0.000000000000000000, -1.000000000000000000 ) ) ;
#13073=ORIENTED_EDGE ( 'NONE', *, *, #808, .F. ) ;
#13079=PRESENTATION_STYLE_ASSIGNMENT (( #7898 ) ) ;
#13086=CARTESIAN_POINT ( 'NONE',  ( 0.000000000000000000, 15.25521607131206459, 23.70650506194175478 ) ) ;
#13088=MANIFOLD_SOLID_BREP ( 'Keyway', #15352 ) ;
#13090=CARTESIAN_POINT ( 'NONE',  ( 0.000000000000000000, 0.000000000000000000, 0.000000000000000000 ) ) ;
#13092=CARTESIAN_POINT ( 'NONE',  ( 10.00000000000000000, 3.786343810537937227, -27.23708136986048700 ) ) ;
#13093=DIRECTION ( 'NONE',  ( -1.000000000000000000, -0.000000000000000000, -0.000000000000000000 ) ) ;
#13100=ORIENTED_EDGE ( 'NONE', *, *, #1428, .T. ) ;
#13107=ORIENTED_EDGE ( 'NONE', *, *, #20321, .F. ) ;
#13114=ORIENTED_EDGE ( 'NONE', *, *, #17021, .F. ) ;
#13118=CARTESIAN_POINT ( 'NONE',  ( 10.00000000000000000, -28.00896854771981026, -15.47571261340951132 ) ) ;
#13129=ORIENTED_EDGE ( 'NONE', *, *, #9150, .F. ) ;
#13132=CIRCLE ( 'NONE', #2901, 27.49900000000000233 ) ;
#13141=AXIS2_PLACEMENT_3D ( 'NONE', #10249, #8813, #15438 ) ;
#13143=CARTESIAN_POINT ( 'NONE',  ( 10.00000000000000000, 0.000000000000000000, 0.000000000000000000 ) ) ;
#13153=AXIS2_PLACEMENT_3D ( 'NONE', #10418, #8766, #21350 ) ;
#13156=CARTESIAN_POINT ( 'NONE',  ( 0.000000000000000000, 13.56333590714014825, 28.98337314858439839 ) ) ;
#13168=SURFACE_STYLE_FILL_AREA ( #4671 ) ;
#13177=AXIS2_PLACEMENT_3D ( 'NONE', #4574, #21580, #7999 ) ;
#13187=VERTEX_POINT ( 'NONE', #19810 ) ;
#13188=CARTESIAN_POINT ( 'NONE',  ( 10.00000000000000000, -12.46320060045702682, -29.47318494484041196 ) ) ;
#13193=LINE ( 'NONE', #12985, #6645 ) ;
#13197=CARTESIAN_POINT ( 'NONE',  ( 5.000000000000000000, -19.29292659243987629, -25.53004080487782090 ) ) ;
#13205=ORIENTED_EDGE ( 'NONE', *, *, #20228, .F. ) ;
#13211=DIRECTION ( 'NONE',  ( -1.000000000000000000, -0.000000000000000000, 0.000000000000000000 ) ) ;
#13219=VECTOR ( 'NONE', #9568, 1000.000000000000000 ) ;
#13220=ORIENTED_EDGE ( 'NONE', *, *, #15167, .F. ) ;
#13238=VECTOR ( 'NONE', #1310, 1000.000000000000000 ) ;
#13239=CARTESIAN_POINT ( 'NONE',  ( 0.000000000000000000, 0.000000000000000000, 0.000000000000000000 ) ) ;
#13240=ORIENTED_EDGE ( 'NONE', *, *, #1678, .F. ) ;
#13242=ORIENTED_EDGE ( 'NONE', *, *, #11380, .T. ) ;
#13254=ADVANCED_FACE ( 'NONE', ( #15161 ), #16824, .T. ) ;
#13255=DIRECTION ( 'NONE',  ( 0.000000000000000000, 0.000000000000000000, 1.000000000000000000 ) ) ;
#13258=DIRECTION ( 'NONE',  ( 0.000000000000000000, -6.982962677686266711E-15, 1.000000000000000000 ) ) ;
#13259=CARTESIAN_POINT ( 'NONE',  ( 10.00000000000000000, 7.619321854369562885, 26.42235673590693423 ) ) ;
#13267=ORIENTED_EDGE ( 'NONE', *, *, #12454, .T. ) ;
#13268=ORIENTED_EDGE ( 'NONE', *, *, #14089, .T. ) ;
#13269=CARTESIAN_POINT ( 'NONE',  ( 0.000000000000000000, 28.15804365424197186, -1.358152127006073684 ) ) ;
#13274=EDGE_CURVE ( 'NONE', #18351, #13474, #11506, .T. ) ;
#13275=DIRECTION ( 'NONE',  ( -1.000000000000000000, 0.000000000000000000, -0.000000000000000000 ) ) ;
#13283=CARTESIAN_POINT ( 'NONE',  ( 0.000000000000000000, 31.75612719289746266, -3.943144139962234451 ) ) ;
#13288=LINE ( 'NONE', #20036, #20680 ) ;
#13291=VECTOR ( 'NONE', #4650, 1000.000000000000000 ) ;
#13293=CIRCLE ( 'NONE', #16103, 32.00000000000000000 ) ;
#13296=CARTESIAN_POINT ( 'NONE',  ( 5.000000000000000888, -30.24235385705245349, 10.45944707835097454 ) ) ;
#13302=EDGE_LOOP ( 'NONE', ( #1564, #9880, #1279, #8095 ) ) ;
#13303=ORIENTED_EDGE ( 'NONE', *, *, #1217, .T. ) ;
#13306=VERTEX_POINT ( 'NONE', #8434 ) ;
#13309=CARTESIAN_POINT ( 'NONE',  ( 0.000000000000000000, 0.000000000000000000, 0.000000000000000000 ) ) ;
#13310=CIRCLE ( 'NONE', #6614, 11.99999999999999822 ) ;
#13313=CIRCLE ( 'NONE', #8743, 11.99999999999999645 ) ;
#13317=DIRECTION ( 'NONE',  ( 0.000000000000000000, 0.000000000000000000, 1.000000000000000000 ) ) ;
#13319=ORIENTED_EDGE ( 'NONE', *, *, #11236, .F. ) ;
#13320=FACE_OUTER_BOUND ( 'NONE', #5841, .T. ) ;
#13333=ORIENTED_EDGE ( 'NONE', *, *, #13915, .T. ) ;
#13341=DIRECTION ( 'NONE',  ( 0.000000000000000000, 0.9945218953682729568, 0.1045284632676570791 ) ) ;
#13347=CARTESIAN_POINT ( 'NONE',  ( 10.00000000000000000, -19.85071254963791176, 20.01672328094525000 ) ) ;
#13373=CIRCLE ( 'NONE', #5264, 5.000000000000000000 ) ;
#13380=ORIENTED_EDGE ( 'NONE', *, *, #18128, .F. ) ;
#13381=EDGE_CURVE ( 'NONE', #13692, #18297, #14699, .T. ) ;
#13382=DIRECTION ( 'NONE',  ( 0.000000000000000000, -0.8660254037844432595, 0.4999999999999920064 ) ) ;
#13388=AXIS2_PLACEMENT_3D ( 'NONE', #1571, #18271, #13396 ) ;
#13396=DIRECTION ( 'NONE',  ( 0.000000000000000000, 0.000000000000000000, 1.000000000000000000 ) ) ;
#13405=EDGE_CURVE ( 'NONE', #667, #10646, #8702, .T. ) ;
#13411=EDGE_CURVE ( 'NONE', #4965, #16375, #3888, .T. ) ;
#13416=DIRECTION ( 'NONE',  ( 0.000000000000000000, 0.000000000000000000, -1.000000000000000000 ) ) ;
#13421=EDGE_LOOP ( 'NONE', ( #16695, #18475, #7308, #121 ) ) ;
#13430=CARTESIAN_POINT ( 'NONE',  ( 10.00000000000000000, 27.48365448817206769, -0.9185515634842869037 ) ) ;
#13434=ORIENTED_EDGE ( 'NONE', *, *, #19216, .F. ) ;
#13438=ORIENTED_EDGE ( 'NONE', *, *, #12062, .F. ) ;
#13439=EDGE_CURVE ( 'NONE', #4886, #8622, #19240, .T. ) ;
#13443=CARTESIAN_POINT ( 'NONE',  ( 0.000000000000000000, 0.000000000000000000, 0.000000000000000000 ) ) ;
#13450=LINE ( 'NONE', #17100, #9077 ) ;
#13460=EDGE_LOOP ( 'NONE', ( #10674, #20019, #3842, #18213 ) ) ;
#13463=ORIENTED_EDGE ( 'NONE', *, *, #3013, .T. ) ;
#13467=CARTESIAN_POINT ( 'NONE',  ( 0.000000000000000000, 19.07277123396568896, -19.80970465344728737 ) ) ;
#13474=VERTEX_POINT ( 'NONE', #19452 ) ;
#13484=ORIENTED_EDGE ( 'NONE', *, *, #11496, .F. ) ;
#13485=ORIENTED_EDGE ( 'NONE', *, *, #5833, .F. ) ;
#13490=ADVANCED_FACE ( 'NONE', ( #12487 ), #10836, .T. ) ;
#13491=CIRCLE ( 'NONE', #15258, 27.49900000000000233 ) ;
#13493=CARTESIAN_POINT ( 'NONE',  ( 0.000000000000000000, 0.000000000000000000, 0.000000000000000000 ) ) ;
#13495=DIRECTION ( 'NONE',  ( -1.000000000000000000, -0.000000000000000000, 0.000000000000000000 ) ) ;
#13499=AXIS2_PLACEMENT_3D ( 'NONE', #18686, #9827, #3315 ) ;
#13513=VERTEX_POINT ( 'NONE', #1111 ) ;
#13523=AXIS2_PLACEMENT_3D ( 'NONE', #20305, #1842, #5170 ) ;
#13524=ORIENTED_EDGE ( 'NONE', *, *, #15981, .F. ) ;
#13529=CARTESIAN_POINT ( 'NONE',  ( 0.000000000000000000, 0.000000000000000000, 0.000000000000000000 ) ) ;
#13532=EDGE_CURVE ( 'NONE', #715, #19694, #11522, .T. ) ;
#13533=CARTESIAN_POINT ( 'NONE',  ( 10.00000000000000000, -12.94633825542249994, -24.26081875733348170 ) ) ;
#13537=DIRECTION ( 'NONE',  ( -1.000000000000000000, -0.000000000000000000, -0.000000000000000000 ) ) ;
#13539=DIRECTION ( 'NONE',  ( 0.000000000000000000, 0.8660254037844361541, 0.5000000000000041078 ) ) ;
#13545=CYLINDRICAL_SURFACE ( 'NONE', #8449, 11.99999999999999645 ) ;
#13549=AXIS2_PLACEMENT_3D ( 'NONE', #11766, #20170, #1397 ) ;
#13553=CYLINDRICAL_SURFACE ( 'NONE', #13523, 32.00000000000000000 ) ;
#13555=CARTESIAN_POINT ( 'NONE',  ( 10.00000000000000888, 3.673940397442060361E-16, -3.000000000000000444 ) ) ;
#13560=EDGE_CURVE ( 'NONE', #6732, #9001, #11168, .T. ) ;
#13564=EDGE_CURVE ( 'NONE', #1056, #14528, #16106, .T. ) ;
#13567=CARTESIAN_POINT ( 'NONE',  ( 10.00000000000000888, 2.828427124746190291, -1.000000000000000000 ) ) ;
#13581=CIRCLE ( 'NONE', #7231, 32.00000000000000000 ) ;
#13599=AXIS2_PLACEMENT_3D ( 'NONE', #2774, #7750, #11377 ) ;
#13607=DIRECTION ( 'NONE',  ( -1.000000000000000000, 0.000000000000000000, 0.000000000000000000 ) ) ;
#13610=ADVANCED_FACE ( 'NONE', ( #14814 ), #13703, .T. ) ;
#13611=AXIS2_PLACEMENT_3D ( 'NONE', #1726, #177, #6927 ) ;
#13624=ORIENTED_EDGE ( 'NONE', *, *, #2444, .F. ) ;
#13625=AXIS2_PLACEMENT_3D ( 'NONE', #9943, #5208, #15240 ) ;
#13629=ORIENTED_EDGE ( 'NONE', *, *, #716, .F. ) ;
#13633=CARTESIAN_POINT ( 'NONE',  ( 10.00000000000000000, -30.24235385705245349, 10.45944707835097098 ) ) ;
#13641=DIRECTION ( 'NONE',  ( -1.000000000000000000, -0.000000000000000000, -0.000000000000000000 ) ) ;
#13645=AXIS2_PLACEMENT_3D ( 'NONE', #8495, #1645, #20103 ) ;
#13655=CARTESIAN_POINT ( 'NONE',  ( 0.000000000000000000, -24.17932380791732427, 20.96092317126997884 ) ) ;
#13666=VERTEX_POINT ( 'NONE', #18462 ) ;
#13667=CYLINDRICAL_SURFACE ( 'NONE', #20104, 32.00000000000000000 ) ;
#13669=FACE_OUTER_BOUND ( 'NONE', #2837, .T. ) ;
#13671=CARTESIAN_POINT ( 'NONE',  ( 5.000000000000000888, -6.063030049135288202, 31.42037024962122871 ) ) ;
#13672=DIRECTION ( 'NONE',  ( 0.000000000000000000, 0.000000000000000000, 1.000000000000000000 ) ) ;
#13675=DIRECTION ( 'NONE',  ( 0.000000000000000000, 0.000000000000000000, 1.000000000000000000 ) ) ;
#13681=CARTESIAN_POINT ( 'NONE',  ( 0.000000000000000000, 28.00896854772012645, -15.47571261340896065 ) ) ;
#13685=VERTEX_POINT ( 'NONE', #227 ) ;
#13686=CYLINDRICAL_SURFACE ( 'NONE', #13710, 11.99999999999999822 ) ;
#13689=EDGE_LOOP ( 'NONE', ( #8500, #16872, #7189, #9265 ) ) ;
#13690=ADVANCED_FACE ( 'NONE', ( #20343 ), #11937, .T. ) ;
#13692=VERTEX_POINT ( 'NONE', #11713 ) ;
#13703=CYLINDRICAL_SURFACE ( 'NONE', #11184, 11.99999999999999822 ) ;
#13704=FACE_OUTER_BOUND ( 'NONE', #20885, .T. ) ;
#13707=EDGE_LOOP ( 'NONE', ( #16058, #1504, #20263, #263 ) ) ;
#13710=AXIS2_PLACEMENT_3D ( 'NONE', #5620, #7163, #20753 ) ;
#13711=ORIENTED_EDGE ( 'NONE', *, *, #5326, .T. ) ;
#13712=AXIS2_PLACEMENT_3D ( 'NONE', #20007, #1223, #11164 ) ;
#13720=VERTEX_POINT ( 'NONE', #10599 ) ;
#13722=DIRECTION ( 'NONE',  ( -1.000000000000000000, 0.000000000000000000, 0.000000000000000000 ) ) ;
#13723=AXIS2_PLACEMENT_3D ( 'NONE', #1082, #14124, #6177 ) ;
#13732=DIRECTION ( 'NONE',  ( -1.000000000000000000, -0.000000000000000000, -0.000000000000000000 ) ) ;
#13736=CARTESIAN_POINT ( 'NONE',  ( 10.00000000000000000, 0.000000000000000000, 0.000000000000000000 ) ) ;
#13740=CIRCLE ( 'NONE', #15859, 12.00000000000000000 ) ;
#13742=PRODUCT_DEFINITION_SHAPE ( 'NONE', 'NONE',  #5916 ) ;
#13750=CARTESIAN_POINT ( 'NONE',  ( 10.00000000000000000, 0.000000000000000000, 0.000000000000000000 ) ) ;
#13765=ORIENTED_EDGE ( 'NONE', *, *, #16081, .T. ) ;
#13774=EDGE_LOOP ( 'NONE', ( #7658, #9637, #12475, #12826 ) ) ;
#13783=DIRECTION ( 'NONE',  ( -1.000000000000000000, -0.000000000000000000, 0.000000000000000000 ) ) ;
#13785=CARTESIAN_POINT ( 'NONE',  ( 10.00000000000000000, 27.40684453873966575, 16.51862198942017557 ) ) ;
#13792=CARTESIAN_POINT ( 'NONE',  ( 10.00000000000000000, 0.000000000000000000, 0.000000000000000000 ) ) ;
#13798=VERTEX_POINT ( 'NONE', #759 ) ;
#13805=DIRECTION ( 'NONE',  ( -1.000000000000000000, -0.000000000000000000, 0.000000000000000000 ) ) ;
#13806=CARTESIAN_POINT ( 'NONE',  ( 0.000000000000000000, -17.70753755129051754, 21.03896658273966480 ) ) ;
#13807=CARTESIAN_POINT ( 'NONE',  ( 150.0000507999999968, 3.673940397442060361E-16, -3.000000000000000444 ) ) ;
#13817=CARTESIAN_POINT ( 'NONE',  ( 10.00000000000000000, 4.294029059349855793, 27.86182539015968018 ) ) ;
#13837=VECTOR ( 'NONE', #8555, 1000.000000000000000 ) ;
#13838=DIRECTION ( 'NONE',  ( -1.000000000000000000, 0.000000000000000000, 0.000000000000000000 ) ) ;
#13839=CYLINDRICAL_SURFACE ( 'NONE', #14106, 27.49900000000000233 ) ;
#13841=DIRECTION ( 'NONE',  ( 0.000000000000000000, 0.8660254037844361541, 0.5000000000000041078 ) ) ;
#13845=AXIS2_PLACEMENT_3D ( 'NONE', #11045, #12806, #21115 ) ;
#13859=ORIENTED_EDGE ( 'NONE', *, *, #13564, .T. ) ;
#13861=AXIS2_PLACEMENT_3D ( 'NONE', #3861, #20450, #225 ) ;
#13864=ORIENTED_EDGE ( 'NONE', *, *, #9080, .T. ) ;
#13870=ORIENTED_EDGE ( 'NONE', *, *, #6556, .F. ) ;
#13874=VERTEX_POINT ( 'NONE', #12785 ) ;
#13879=CARTESIAN_POINT ( 'NONE',  ( 0.000000000000000000, 27.07404830566976983, -4.815694066514164540 ) ) ;
#13885=LINE ( 'NONE', #2392, #16938 ) ;
#13891=AXIS2_PLACEMENT_3D ( 'NONE', #16084, #2831, #12761 ) ;
#13894=CARTESIAN_POINT ( 'NONE',  ( 0.000000000000000000, -30.24235385705231849, -10.45944707835137777 ) ) ;
#13897=AXIS2_PLACEMENT_3D ( 'NONE', #20922, #5577, #17722 ) ;
#13899=AXIS2_PLACEMENT_3D ( 'NONE', #6374, #12979, #6148 ) ;
#13900=ORIENTED_EDGE ( 'NONE', *, *, #4346, .F. ) ;
#13904=LINE ( 'NONE', #13807, #20570 ) ;
#13911=ADVANCED_FACE ( 'NONE', ( #19652 ), #21304, .T. ) ;
#13915=EDGE_CURVE ( 'NONE', #5097, #9782, #2750, .T. ) ;
#13919=ORIENTED_EDGE ( 'NONE', *, *, #5461, .F. ) ;
#13920=EDGE_LOOP ( 'NONE', ( #18746, #8360, #18587, #9725 ) ) ;
#13929=EDGE_CURVE ( 'NONE', #21583, #8568, #13313, .T. ) ;
#13935=DIRECTION ( 'NONE',  ( -1.000000000000000000, 0.000000000000000000, -0.000000000000000000 ) ) ;
#13936=DIRECTION ( 'NONE',  ( -1.000000000000000000, -0.000000000000000000, 0.000000000000000000 ) ) ;
#13950=VERTEX_POINT ( 'NONE', #8057 ) ;
#13958=ORIENTED_EDGE ( 'NONE', *, *, #10536, .T. ) ;
#13959=EDGE_CURVE ( 'NONE', #8974, #15746, #3076, .T. ) ;
#13960=CARTESIAN_POINT ( 'NONE',  ( 10.00000000000000000, 27.82509854686817263, -4.525913221810857756 ) ) ;
#13961=DIRECTION ( 'NONE',  ( -1.000000000000000000, 0.000000000000000000, 0.000000000000000000 ) ) ;
#13962=CIRCLE ( 'NONE', #10426, 27.49900000000000233 ) ;
#13963=ADVANCED_FACE ( 'NONE', ( #19765 ), #21200, .T. ) ;
#13974=ORIENTED_EDGE ( 'NONE', *, *, #10402, .T. ) ;
#13976=( GEOMETRIC_REPRESENTATION_CONTEXT ( 3 ) GLOBAL_UNCERTAINTY_ASSIGNED_CONTEXT ( ( #16299 ) ) GLOBAL_UNIT_ASSIGNED_CONTEXT ( ( #16383, #16706, #17945 ) ) REPRESENTATION_CONTEXT ( 'NONE', 'WORKASPACE' ) );
#13983=VERTEX_POINT ( 'NONE', #18007 ) ;
#13985=ORIENTED_EDGE ( 'NONE', *, *, #2200, .T. ) ;
#13992=AXIS2_PLACEMENT_3D ( 'NONE', #16024, #12812, #10730 ) ;
#13993=DIRECTION ( 'NONE',  ( -1.000000000000000000, 0.000000000000000000, 0.000000000000000000 ) ) ;
#14005=VERTEX_POINT ( 'NONE', #4627 ) ;
#14008=ORIENTED_EDGE ( 'NONE', *, *, #3818, .F. ) ;
#14013=ORIENTED_EDGE ( 'NONE', *, *, #6784, .T. ) ;
#14016=LINE ( 'NONE', #7080, #10678 ) ;
#14022=CIRCLE ( 'NONE', #16851, 27.49900000000000233 ) ;
#14023=FACE_OUTER_BOUND ( 'NONE', #1330, .T. ) ;
#14025=EDGE_LOOP ( 'NONE', ( #127, #21617, #6446, #16599, #20356, #14166 ) ) ;
#14032=EDGE_CURVE ( 'NONE', #13474, #15205, #17913, .T. ) ;
#14033=CIRCLE ( 'NONE', #12626, 27.49900000000000233 ) ;
#14041=ORIENTED_EDGE ( 'NONE', *, *, #15231, .F. ) ;
#14043=CYLINDRICAL_SURFACE ( 'NONE', #18081, 11.99999999999999822 ) ;
#14045=FACE_OUTER_BOUND ( 'NONE', #13421, .T. ) ;
#14046=CARTESIAN_POINT ( 'NONE',  ( 10.00000000000000000, -30.61448696004445580, -9.314139153634537038 ) ) ;
#14047=CARTESIAN_POINT ( 'NONE',  ( 10.00000000000000000, -21.98203405400967014, 17.64965094506536403 ) ) ;
#14048=CARTESIAN_POINT ( 'NONE',  ( 0.000000000000000000, 6.063030049135491595, -31.42037024962118608 ) ) ;
#14052=VECTOR ( 'NONE', #2216, 1000.000000000000000 ) ;
#14055=ORIENTED_EDGE ( 'NONE', *, *, #11598, .T. ) ;
#14058=CYLINDRICAL_SURFACE ( 'NONE', #2765, 11.99999999999999822 ) ;
#14063=VERTEX_POINT ( 'NONE', #13785 ) ;
#14073=AXIS2_PLACEMENT_3D ( 'NONE', #10053, #16917, #230 ) ;
#14075=DIRECTION ( 'NONE',  ( 1.000000000000000000, -0.000000000000000000, -0.000000000000000000 ) ) ;
#14080=EDGE_CURVE ( 'NONE', #874, #19022, #8489, .T. ) ;
#14081=ORIENTED_EDGE ( 'NONE', *, *, #1930, .T. ) ;
#14083=DIRECTION ( 'NONE',  ( 0.000000000000000000, -0.8660254037844432595, 0.4999999999999918399 ) ) ;
#14087=CIRCLE ( 'NONE', #21850, 11.99999999999999822 ) ;
#14089=EDGE_CURVE ( 'NONE', #10823, #4316, #13450, .T. ) ;
#14090=CYLINDRICAL_SURFACE ( 'NONE', #21435, 27.49900000000000233 ) ;
#14091=VERTEX_POINT ( 'NONE', #6839 ) ;
#14092=DIRECTION ( 'NONE',  ( 0.000000000000000000, -0.9510565162951502005, -0.3090169943749575543 ) ) ;
#14093=CYLINDRICAL_SURFACE ( 'NONE', #13029, 5.000000000000000000 ) ;
#14105=CARTESIAN_POINT ( 'NONE',  ( 0.000000000000000000, 9.992993448021948666, -26.36019881529875519 ) ) ;
#14106=AXIS2_PLACEMENT_3D ( 'NONE', #13736, #17277, #9081 ) ;
#14113=DIRECTION ( 'NONE',  ( -1.000000000000000000, -0.000000000000000000, -0.000000000000000000 ) ) ;
#14115=DIRECTION ( 'NONE',  ( -1.000000000000000000, -0.000000000000000000, 0.000000000000000000 ) ) ;
#14116=ORIENTED_EDGE ( 'NONE', *, *, #9047, .T. ) ;
#14120=EDGE_LOOP ( 'NONE', ( #5562, #18620, #223, #20351 ) ) ;
#14122=DIRECTION ( 'NONE',  ( -1.000000000000000000, 0.000000000000000000, 0.000000000000000000 ) ) ;
#14124=DIRECTION ( 'NONE',  ( -1.000000000000000000, 0.000000000000000000, -0.000000000000000000 ) ) ;
#14125=CARTESIAN_POINT ( 'NONE',  ( 10.00000000000000000, -27.48365448817207479, 0.9185515634840949462 ) ) ;
#14128=DIRECTION ( 'NONE',  ( -1.000000000000000000, -0.000000000000000000, -0.000000000000000000 ) ) ;
#14133=DIRECTION ( 'NONE',  ( -1.000000000000000000, 0.000000000000000000, 0.000000000000000000 ) ) ;
#14137=ORIENTED_EDGE ( 'NONE', *, *, #20947, .T. ) ;
#14148=CARTESIAN_POINT ( 'NONE',  ( 10.00000000000000000, 21.98203405400978383, -17.64965094506522192 ) ) ;
#14155=CARTESIAN_POINT ( 'NONE',  ( 10.00000000000000000, 22.77465461094674026, 15.41136296218094159 ) ) ;
#14159=ORIENTED_EDGE ( 'NONE', *, *, #11220, .F. ) ;
#14165=ORIENTED_EDGE ( 'NONE', *, *, #9493, .F. ) ;
#14166=ORIENTED_EDGE ( 'NONE', *, *, #1322, .F. ) ;
#14178=EDGE_CURVE ( 'NONE', #15448, #9457, #11558, .T. ) ;
#14179=EDGE_CURVE ( 'NONE', #9611, #16266, #14022, .T. ) ;
#14180=EDGE_CURVE ( 'NONE', #15608, #1543, #21156, .T. ) ;
#14187=DIRECTION ( 'NONE',  ( -1.000000000000000000, -0.000000000000000000, 0.000000000000000000 ) ) ;
#14189=DIRECTION ( 'NONE',  ( 0.000000000000000000, 0.000000000000000000, 1.000000000000000000 ) ) ;
#14195=ORIENTED_EDGE ( 'NONE', *, *, #5710, .F. ) ;
#14207=ORIENTED_EDGE ( 'NONE', *, *, #11784, .T. ) ;
#14214=VERTEX_POINT ( 'NONE', #2577 ) ;
#14218=CYLINDRICAL_SURFACE ( 'NONE', #15473, 32.00000000000000000 ) ;
#14227=AXIS2_PLACEMENT_3D ( 'NONE', #5854, #865, #21506 ) ;
#14230=ADVANCED_FACE ( 'NONE', ( #18869 ), #3726, .T. ) ;
#14239=VECTOR ( 'NONE', #2717, 1000.000000000000000 ) ;
#14241=AXIS2_PLACEMENT_3D ( 'NONE', #5442, #13495, #10078 ) ;
#14254=DIRECTION ( 'NONE',  ( -1.000000000000000000, 0.000000000000000000, -0.000000000000000000 ) ) ;
#14258=CARTESIAN_POINT ( 'NONE',  ( 0.000000000000000000, 26.69209308833517014, -6.612652082459055336 ) ) ;
#14260=ORIENTED_EDGE ( 'NONE', *, *, #19059, .F. ) ;
#14275=ORIENTED_EDGE ( 'NONE', *, *, #20748, .T. ) ;
#14289=AXIS2_PLACEMENT_3D ( 'NONE', #361, #3989, #5877 ) ;
#14290=EDGE_LOOP ( 'NONE', ( #7187, #594, #13107, #18706 ) ) ;
#14292=DIRECTION ( 'NONE',  ( -1.000000000000000000, 0.000000000000000000, 0.000000000000000000 ) ) ;
#14295=DIRECTION ( 'NONE',  ( 0.000000000000000000, 0.000000000000000000, -1.000000000000000000 ) ) ;
#14296=ORIENTED_EDGE ( 'NONE', *, *, #16648, .F. ) ;
#14308=EDGE_LOOP ( 'NONE', ( #3279, #7787, #15356, #18885 ) ) ;
#14309=EDGE_CURVE ( 'NONE', #20292, #17498, #16149, .T. ) ;
#14315=DIRECTION ( 'NONE',  ( 0.000000000000000000, 0.000000000000000000, -1.000000000000000000 ) ) ;
#14316=CARTESIAN_POINT ( 'NONE',  ( 10.00000000000000000, 0.6021240089805636186, -31.99433460282944708 ) ) ;
#14318=AXIS2_PLACEMENT_3D ( 'NONE', #1576, #18165, #8209 ) ;
#14326=AXIS2_PLACEMENT_3D ( 'NONE', #10948, #21327, #14589 ) ;
#14327=CARTESIAN_POINT ( 'NONE',  ( 10.00000000000000000, 7.619321854369911051, -26.42235673590683476 ) ) ;
#14331=DIRECTION ( 'NONE',  ( -1.000000000000000000, 0.000000000000000000, 0.000000000000000000 ) ) ;
#14334=EDGE_LOOP ( 'NONE', ( #14496, #16838, #19234, #6528 ) ) ;
#14336=EDGE_LOOP ( 'NONE', ( #14367, #1070, #19116, #20403 ) ) ;
#14339=DIRECTION ( 'NONE',  ( -1.000000000000000000, 0.000000000000000000, 0.000000000000000000 ) ) ;
#14342=AXIS2_PLACEMENT_3D ( 'NONE', #12229, #20847, #13672 ) ;
#14354=CIRCLE ( 'NONE', #3769, 27.49900000000000233 ) ;
#14357=ORIENTED_EDGE ( 'NONE', *, *, #13274, .T. ) ;
#14358=ORIENTED_EDGE ( 'NONE', *, *, #1322, .T. ) ;
#14367=ORIENTED_EDGE ( 'NONE', *, *, #14989, .F. ) ;
#14371=CYLINDRICAL_SURFACE ( 'NONE', #13845, 11.99999999999999822 ) ;
#14374=DIRECTION ( 'NONE',  ( -1.000000000000000000, 0.000000000000000000, -0.000000000000000000 ) ) ;
#14375=DIRECTION ( 'NONE',  ( 0.000000000000000000, -0.4067366430758070361, 0.9135454576425978690 ) ) ;
#14376=CARTESIAN_POINT ( 'NONE',  ( 10.00000000000000000, -28.15804365424196121, 10.64184787299373269 ) ) ;
#14377=CYLINDRICAL_SURFACE ( 'NONE', #10177, 11.99999999999999645 ) ;
#14378=ORIENTED_EDGE ( 'NONE', *, *, #17163, .T. ) ;
#14381=AXIS2_PLACEMENT_3D ( 'NONE', #20422, #7144, #5281 ) ;
#14384=CARTESIAN_POINT ( 'NONE',  ( 10.00000000000000000, 1.959304526718168571, -27.42911093658673138 ) ) ;
#14388=ORIENTED_EDGE ( 'NONE', *, *, #20544, .T. ) ;
#14390=VECTOR ( 'NONE', #8432, 1000.000000000000000 ) ;
#14393=ORIENTED_EDGE ( 'NONE', *, *, #8288, .T. ) ;
#14394=CARTESIAN_POINT ( 'NONE',  ( -10.00000000000000000, 0.000000000000000000, 0.000000000000000000 ) ) ;
#14395=DIRECTION ( 'NONE',  ( -1.000000000000000000, 0.000000000000000000, -0.000000000000000000 ) ) ;
#14403=CARTESIAN_POINT ( 'NONE',  ( 10.00000000000000000, 9.366510754379572035, -25.85466064925416774 ) ) ;
#14405=ORIENTED_EDGE ( 'NONE', *, *, #1236, .T. ) ;
#14406=DIRECTION ( 'NONE',  ( 0.000000000000000000, 0.8660254037844363761, 0.5000000000000039968 ) ) ;
#14412=CIRCLE ( 'NONE', #13712, 32.00000000000000000 ) ;
#14428=LINE ( 'NONE', #12760, #18551 ) ;
#14429=CIRCLE ( 'NONE', #17260, 32.00000000000000000 ) ;
#14430=LINE ( 'NONE', #21176, #130 ) ;
#14436=CARTESIAN_POINT ( 'NONE',  ( 10.00000000000000000, 0.000000000000000000, 0.000000000000000000 ) ) ;
#14437=CYLINDRICAL_SURFACE ( 'NONE', #19592, 27.49900000000000233 ) ;
#14442=ORIENTED_EDGE ( 'NONE', *, *, #13381, .T. ) ;
#14449=ORIENTED_EDGE ( 'NONE', *, *, #6004, .F. ) ;
#14451=CYLINDRICAL_SURFACE ( 'NONE', #16791, 11.99999999999999822 ) ;
#14454=EDGE_CURVE ( 'NONE', #16474, #1041, #21582, .T. ) ;
#14457=DIRECTION ( 'NONE',  ( -1.000000000000000000, 0.000000000000000000, -0.000000000000000000 ) ) ;
#14460=DIRECTION ( 'NONE',  ( -1.000000000000000000, -0.000000000000000000, 0.000000000000000000 ) ) ;
#14472=ORIENTED_EDGE ( 'NONE', *, *, #9895, .F. ) ;
#14487=DIRECTION ( 'NONE',  ( -1.000000000000000000, 0.000000000000000000, 0.000000000000000000 ) ) ;
#14490=CYLINDRICAL_SURFACE ( 'NONE', #13992, 32.00000000000000000 ) ;
#14491=LINE ( 'NONE', #17804, #2416 ) ;
#14492=ORIENTED_EDGE ( 'NONE', *, *, #939, .F. ) ;
#14496=ORIENTED_EDGE ( 'NONE', *, *, #12850, .F. ) ;
#14500=LINE ( 'NONE', #16036, #897 ) ;
#14502=ORIENTED_EDGE ( 'NONE', *, *, #3110, .F. ) ;
#14503=CARTESIAN_POINT ( 'NONE',  ( 0.000000000000000000, 17.70753755129037188, 21.03896658273978559 ) ) ;
#14510=LINE ( 'NONE', #16047, #6299 ) ;
#14511=CARTESIAN_POINT ( 'NONE',  ( 10.00000000000000000, -19.29292659243987629, -25.53004080487781735 ) ) ;
#14516=CARTESIAN_POINT ( 'NONE',  ( 10.00000000000000000, 0.000000000000000000, 0.000000000000000000 ) ) ;
#14518=CARTESIAN_POINT ( 'NONE',  ( 5.000000000000000000, -12.46320060045703038, -29.47318494484041196 ) ) ;
#14519=VERTEX_POINT ( 'NONE', #3569 ) ;
#14527=ORIENTED_EDGE ( 'NONE', *, *, #11657, .F. ) ;
#14528=VERTEX_POINT ( 'NONE', #10297 ) ;
#14547=DIRECTION ( 'NONE',  ( 1.000000000000000000, 0.000000000000000000, 0.000000000000000000 ) ) ;
#14551=ORIENTED_EDGE ( 'NONE', *, *, #2867, .T. ) ;
#14555=FACE_OUTER_BOUND ( 'NONE', #1729, .T. ) ;
#14563=EDGE_CURVE ( 'NONE', #21750, #8568, #10504, .T. ) ;
#14570=ORIENTED_EDGE ( 'NONE', *, *, #17576, .F. ) ;
#14578=ADVANCED_FACE ( 'NONE', ( #8640 ), #10623, .T. ) ;
#14582=EDGE_CURVE ( 'NONE', #19694, #20559, #2398, .T. ) ;
#14584=ADVANCED_FACE ( 'NONE', ( #37 ), #3458, .T. ) ;
#14589=DIRECTION ( 'NONE',  ( 0.000000000000000000, 0.000000000000000000, 1.000000000000000000 ) ) ;
#14590=CARTESIAN_POINT ( 'NONE',  ( 10.00000000000000000, 25.48117629651189375, 10.33947075754270095 ) ) ;
#14611=DIRECTION ( 'NONE',  ( -1.000000000000000000, -0.000000000000000000, 0.000000000000000000 ) ) ;
#14612=LINE ( 'NONE', #21355, #19753 ) ;
#14613=EDGE_CURVE ( 'NONE', #9954, #1233, #14491, .T. ) ;
#14622=ORIENTED_EDGE ( 'NONE', *, *, #118, .T. ) ;
#14626=ORIENTED_EDGE ( 'NONE', *, *, #9969, .T. ) ;
#14630=EDGE_CURVE ( 'NONE', #428, #16396, #11603, .T. ) ;
#14631=CYLINDRICAL_SURFACE ( 'NONE', #19737, 11.99999999999999822 ) ;
#14633=EDGE_CURVE ( 'NONE', #6341, #11343, #15710, .T. ) ;
#14634=AXIS2_PLACEMENT_3D ( 'NONE', #18688, #3540, #10272 ) ;
#14635=VERTEX_POINT ( 'NONE', #11052 ) ;
#14639=DIRECTION ( 'NONE',  ( -1.000000000000000000, 0.000000000000000000, -0.000000000000000000 ) ) ;
#14643=DIRECTION ( 'NONE',  ( -1.000000000000000000, -0.000000000000000000, 0.000000000000000000 ) ) ;
#14654=AXIS2_PLACEMENT_3D ( 'NONE', #18290, #16618, #11313 ) ;
#14656=CARTESIAN_POINT ( 'NONE',  ( 0.000000000000000000, -19.07277123396528040, -19.80970465344767817 ) ) ;
#14658=ORIENTED_EDGE ( 'NONE', *, *, #15165, .T. ) ;
#14665=DIRECTION ( 'NONE',  ( -1.000000000000000000, 0.000000000000000000, 0.000000000000000000 ) ) ;
#14669=DIRECTION ( 'NONE',  ( 0.000000000000000000, 0.000000000000000000, -1.000000000000000000 ) ) ;
#14670=AXIS2_PLACEMENT_3D ( 'NONE', #15193, #7531, #17494 ) ;
#14684=ORIENTED_EDGE ( 'NONE', *, *, #2843, .F. ) ;
#14693=DIRECTION ( 'NONE',  ( 0.000000000000000000, 0.4067366430758010409, -0.9135454576426005335 ) ) ;
#14699=CIRCLE ( 'NONE', #19646, 11.99999999999999822 ) ;
#14701=CARTESIAN_POINT ( 'NONE',  ( 0.000000000000000000, 27.48365448817206769, 0.9185515634842894572 ) ) ;
#14705=EDGE_CURVE ( 'NONE', #12763, #15688, #12287, .T. ) ;
#14719=DIRECTION ( 'NONE',  ( -1.000000000000000000, -0.000000000000000000, 0.000000000000000000 ) ) ;
#14722=DIRECTION ( 'NONE',  ( -1.000000000000000000, 0.000000000000000000, 0.000000000000000000 ) ) ;
#14723=FACE_OUTER_BOUND ( 'NONE', #18725, .T. ) ;
#14724=ADVANCED_FACE ( 'NONE', ( #2452 ), #14377, .T. ) ;
#14727=SURFACE_SIDE_STYLE ('',( #13168 ) ) ;
#14728=DIRECTION ( 'NONE',  ( 1.000000000000000000, 0.000000000000000000, 0.000000000000000000 ) ) ;
#14731=DIRECTION ( 'NONE',  ( -1.000000000000000000, -0.000000000000000000, 0.000000000000000000 ) ) ;
#14733=VECTOR ( 'NONE', #17675, 1000.000000000000000 ) ;
#14734=CIRCLE ( 'NONE', #21779, 27.49900000000000233 ) ;
#14738=ORIENTED_EDGE ( 'NONE', *, *, #10282, .T. ) ;
#14739=EDGE_CURVE ( 'NONE', #12821, #19022, #12644, .T. ) ;
#14757=DIRECTION ( 'NONE',  ( 0.000000000000000000, 0.000000000000000000, 1.000000000000000000 ) ) ;
#14760=EDGE_CURVE ( 'NONE', #17965, #9285, #9505, .T. ) ;
#14761=FACE_OUTER_BOUND ( 'NONE', #18432, .T. ) ;
#14766=ORIENTED_EDGE ( 'NONE', *, *, #16740, .T. ) ;
#14770=CARTESIAN_POINT ( 'NONE',  ( 0.000000000000000000, 13.56333590714055326, -28.98337314858420299 ) ) ;
#14781=DIRECTION ( 'NONE',  ( -1.000000000000000000, -0.000000000000000000, 0.000000000000000000 ) ) ;
#14785=VERTEX_POINT ( 'NONE', #14701 ) ;
#14786=DIRECTION ( 'NONE',  ( 1.000000000000000000, 0.000000000000000000, 0.000000000000000000 ) ) ;
#14799=CYLINDRICAL_SURFACE ( 'NONE', #15692, 11.99999999999999822 ) ;
#14802=ORIENTED_EDGE ( 'NONE', *, *, #9428, .F. ) ;
#14805=VERTEX_POINT ( 'NONE', #12930 ) ;
#14807=ORIENTED_EDGE ( 'NONE', *, *, #2550, .T. ) ;
#14813=DIRECTION ( 'NONE',  ( 0.000000000000000000, 0.5877852522924742473, -0.8090169943749466741 ) ) ;
#14814=FACE_OUTER_BOUND ( 'NONE', #16400, .T. ) ;
#14816=CYLINDRICAL_SURFACE ( 'NONE', #18603, 11.99999999999999822 ) ;
#14820=CYLINDRICAL_SURFACE ( 'NONE', #19990, 32.00000000000000000 ) ;
#14827=ORIENTED_EDGE ( 'NONE', *, *, #13929, .F. ) ;
#14839=DIRECTION ( 'NONE',  ( -1.000000000000000000, -0.000000000000000000, 0.000000000000000000 ) ) ;
#14842=ORIENTED_EDGE ( 'NONE', *, *, #4622, .F. ) ;
#14844=ORIENTED_EDGE ( 'NONE', *, *, #21396, .T. ) ;
#14849=AXIS2_PLACEMENT_3D ( 'NONE', #11438, #9892, #19950 ) ;
#14852=SHAPE_REPRESENTATION_RELATIONSHIP ( 'NONE' , 'NONE' ,  #11927, #7762 ) ;
#14871=ORIENTED_EDGE ( 'NONE', *, *, #7136, .F. ) ;
#14878=VERTEX_POINT ( 'NONE', #18464 ) ;
#14880=CARTESIAN_POINT ( 'NONE',  ( 0.000000000000000000, 0.000000000000000000, 0.000000000000000000 ) ) ;
#14885=ORIENTED_EDGE ( 'NONE', *, *, #16071, .T. ) ;
#14887=EDGE_CURVE ( 'NONE', #21758, #17790, #20226, .T. ) ;
#14895=CARTESIAN_POINT ( 'NONE',  ( 10.00000000000000000, -17.83210509884655792, 21.83428559348755371 ) ) ;
#14896=CARTESIAN_POINT ( 'NONE',  ( 10.00000000000000000, 27.07404830566976983, -4.815694066514164540 ) ) ;
#14899=DIRECTION ( 'NONE',  ( -1.000000000000000000, -0.000000000000000000, -0.000000000000000000 ) ) ;
#14900=CARTESIAN_POINT ( 'NONE',  ( 0.000000000000000000, 0.000000000000000000, 0.000000000000000000 ) ) ;
#14903=ORIENTED_EDGE ( 'NONE', *, *, #18415, .T. ) ;
#14913=DIRECTION ( 'NONE',  ( -0.000000000000000000, 0.000000000000000000, 1.000000000000000000 ) ) ;
#14915=CARTESIAN_POINT ( 'NONE',  ( 10.00000000000000000, 19.85071254963777676, 20.01672328094538145 ) ) ;
#14922=DIRECTION ( 'NONE',  ( 0.000000000000000000, -0.2079116908177666145, 0.9781476007338040235 ) ) ;
#14929=ORIENTED_EDGE ( 'NONE', *, *, #7446, .T. ) ;
#14933=CARTESIAN_POINT ( 'NONE',  ( 5.000000000000000888, 30.61448696004464409, -9.314139153633925972 ) ) ;
#14937=CARTESIAN_POINT ( 'NONE',  ( 10.00000000000000000, -9.992993448021772807, 26.36019881529882980 ) ) ;
#14945=ORIENTED_EDGE ( 'NONE', *, *, #14180, .T. ) ;
#14953=CIRCLE ( 'NONE', #13899, 11.99999999999999822 ) ;
#14954=EDGE_LOOP ( 'NONE', ( #14449, #14388, #18995, #16812 ) ) ;
#14956=ORIENTED_EDGE ( 'NONE', *, *, #12290, .F. ) ;
#14960=EDGE_CURVE ( 'NONE', #20936, #14091, #7382, .T. ) ;
#14963=CARTESIAN_POINT ( 'NONE',  ( 10.00000000000000000, -12.94633825542249994, -24.26081875733348170 ) ) ;
#14964=PLANE ( 'NONE',  #10814 ) ;
#14966=CARTESIAN_POINT ( 'NONE',  ( 10.00000000000000000, 13.56333590714014825, 28.98337314858439484 ) ) ;
#14969=UNCERTAINTY_MEASURE_WITH_UNIT (LENGTH_MEASURE( 1.000000000000000082E-05 ), #17738, 'distance_accuracy_value', 'NONE');
#14983=EDGE_CURVE ( 'NONE', #8691, #6248, #10194, .T. ) ;
#14985=VERTEX_POINT ( 'NONE', #12256 ) ;
#14989=EDGE_CURVE ( 'NONE', #19418, #15166, #17269, .T. ) ;
#14998=LINE ( 'NONE', #10460, #4701 ) ;
#15001=AXIS2_PLACEMENT_3D ( 'NONE', #18314, #1611, #6390 ) ;
#15008=CARTESIAN_POINT ( 'NONE',  ( 10.00000000000000000, -25.48117629651182270, -10.33947075754286793 ) ) ;
#15010=DIRECTION ( 'NONE',  ( 1.000000000000000000, -0.000000000000000000, -0.000000000000000000 ) ) ;
#15014=ADVANCED_FACE ( 'NONE', ( #7405 ), #12691, .T. ) ;
#15015=ORIENTED_EDGE ( 'NONE', *, *, #7270, .F. ) ;
#15019=ORIENTED_EDGE ( 'NONE', *, *, #4464, .T. ) ;
#15036=CARTESIAN_POINT ( 'NONE',  ( 0.000000000000000000, 31.88200538760793634, 2.745493118647102548 ) ) ;
#15037=EDGE_LOOP ( 'NONE', ( #7392, #14956, #15393, #14055 ) ) ;
#15041=ORIENTED_EDGE ( 'NONE', *, *, #10116, .F. ) ;
#15047=ORIENTED_EDGE ( 'NONE', *, *, #14630, .T. ) ;
#15060=DIRECTION ( 'NONE',  ( -1.000000000000000000, -0.000000000000000000, 0.000000000000000000 ) ) ;
#15066=DIRECTION ( 'NONE',  ( 0.000000000000000000, 0.000000000000000000, 1.000000000000000000 ) ) ;
#15067=ORIENTED_EDGE ( 'NONE', *, *, #10580, .F. ) ;
#15068=ORIENTED_EDGE ( 'NONE', *, *, #3409, .F. ) ;
#15077=CARTESIAN_POINT ( 'NONE',  ( 10.00000000000000000, -26.27606311335944511, -10.21217444509438188 ) ) ;
#15079=VECTOR ( 'NONE', #4160, 1000.000000000000000 ) ;
#15080=EDGE_CURVE ( 'NONE', #3591, #10715, #20077, .T. ) ;
#15084=EDGE_LOOP ( 'NONE', ( #18644, #12942, #11479, #9728 ) ) ;
#15087=ORIENTED_EDGE ( 'NONE', *, *, #16344, .T. ) ;
#15101=CARTESIAN_POINT ( 'NONE',  ( 10.00000000000000000, 21.98203405400978383, -17.64965094506522192 ) ) ;
#15102=DIRECTION ( 'NONE',  ( -1.000000000000000000, -0.000000000000000000, 0.000000000000000000 ) ) ;
#15110=CIRCLE ( 'NONE', #12285, 27.49900000000000588 ) ;
#15113=DIRECTION ( 'NONE',  ( -1.000000000000000000, -0.000000000000000000, -0.000000000000000000 ) ) ;
#15122=EDGE_LOOP ( 'NONE', ( #14738, #221, #11263, #6443, #19066, #21239 ) ) ;
#15123=AXIS2_PLACEMENT_3D ( 'NONE', #3951, #20539, #532 ) ;
#15153=DIRECTION ( 'NONE',  ( -1.000000000000000000, 0.000000000000000000, 0.000000000000000000 ) ) ;
#15154=ORIENTED_EDGE ( 'NONE', *, *, #19852, .T. ) ;
#15157=DIRECTION ( 'NONE',  ( 0.000000000000000000, 0.000000000000000000, 1.000000000000000000 ) ) ;
#15161=FACE_OUTER_BOUND ( 'NONE', #20585, .T. ) ;
#15162=FACE_OUTER_BOUND ( 'NONE', #19779, .T. ) ;
#15165=EDGE_CURVE ( 'NONE', #14214, #21189, #17616, .T. ) ;
#15166=VERTEX_POINT ( 'NONE', #18341 ) ;
#15167=EDGE_CURVE ( 'NONE', #7466, #15171, #4848, .T. ) ;
#15168=VECTOR ( 'NONE', #17050, 1000.000000000000000 ) ;
#15169=DIRECTION ( 'NONE',  ( 0.000000000000000000, 0.000000000000000000, 1.000000000000000000 ) ) ;
#15171=VERTEX_POINT ( 'NONE', #11359 ) ;
#15185=DIRECTION ( 'NONE',  ( 0.000000000000000000, 0.000000000000000000, 1.000000000000000000 ) ) ;
#15186=CARTESIAN_POINT ( 'NONE',  ( 10.00000000000000000, -19.29292659244022445, 25.53004080487755445 ) ) ;
#15187=VECTOR ( 'NONE', #6289, 1000.000000000000000 ) ;
#15193=CARTESIAN_POINT ( 'NONE',  ( 150.0000507999999968, 0.000000000000000000, 0.000000000000000000 ) ) ;
#15194=ORIENTED_EDGE ( 'NONE', *, *, #18800, .T. ) ;
#15198=CIRCLE ( 'NONE', #1787, 12.00000000000000000 ) ;
#15202=FACE_OUTER_BOUND ( 'NONE', #8303, .T. ) ;
#15205=VERTEX_POINT ( 'NONE', #17898 ) ;
#15226=ORIENTED_EDGE ( 'NONE', *, *, #16027, .T. ) ;
#15230=DIRECTION ( 'NONE',  ( 0.000000000000000000, -0.7431448254773862505, -0.6691306063588668973 ) ) ;
#15231=EDGE_CURVE ( 'NONE', #9187, #7466, #7034, .T. ) ;
#15232=AXIS2_PLACEMENT_3D ( 'NONE', #16656, #15102, #5174 ) ;
#15233=CARTESIAN_POINT ( 'NONE',  ( 10.00000000000000000, 21.69483248597422076, 16.89761061231787309 ) ) ;
#15236=CARTESIAN_POINT ( 'NONE',  ( 0.000000000000000000, -22.77465461094683974, 15.41136296218079238 ) ) ;
#15237=EDGE_CURVE ( 'NONE', #7417, #14214, #4732, .T. ) ;
#15240=DIRECTION ( 'NONE',  ( 0.000000000000000000, 0.4067366430757948237, 0.9135454576426033091 ) ) ;
#15241=AXIS2_PLACEMENT_3D ( 'NONE', #2873, #9381, #12596 ) ;
#15246=ORIENTED_EDGE ( 'NONE', *, *, #11092, .F. ) ;
#15247=EDGE_CURVE ( 'NONE', #7775, #3621, #17982, .T. ) ;
#15253=AXIS2_PLACEMENT_3D ( 'NONE', #3515, #19985, #11588 ) ;
#15254=LINE ( 'NONE', #11632, #21105 ) ;
#15258=AXIS2_PLACEMENT_3D ( 'NONE', #5409, #15463, #19106 ) ;
#15263=CYLINDRICAL_SURFACE ( 'NONE', #16435, 27.49900000000000233 ) ;
#15267=CIRCLE ( 'NONE', #7859, 32.00000000000000000 ) ;
#15272=CARTESIAN_POINT ( 'NONE',  ( 10.00000000000000000, 12.94633825542266869, 24.26081875733338933 ) ) ;
#15277=AXIS2_PLACEMENT_3D ( 'NONE', #17183, #3808, #61 ) ;
#15288=CARTESIAN_POINT ( 'NONE',  ( -140.0000507999999968, 3.673940397442060361E-16, -3.000000000000000444 ) ) ;
#15295=ORIENTED_EDGE ( 'NONE', *, *, #8030, .F. ) ;
#15306=FACE_OUTER_BOUND ( 'NONE', #11428, .T. ) ;
#15311=EDGE_LOOP ( 'NONE', ( #8952, #19518, #11156, #9053 ) ) ;
#15316=DIRECTION ( 'NONE',  ( -1.000000000000000000, -0.000000000000000000, 0.000000000000000000 ) ) ;
#15318=DIRECTION ( 'NONE',  ( 0.000000000000000000, 0.000000000000000000, 1.000000000000000000 ) ) ;
#15320=AXIS2_PLACEMENT_3D ( 'NONE', #14394, #2801, #2681 ) ;
#15325=AXIS2_PLACEMENT_3D ( 'NONE', #17456, #15789, #8932 ) ;
#15344=AXIS2_PLACEMENT_3D ( 'NONE', #6453, #11079, #11407 ) ;
#15352=CLOSED_SHELL ( 'NONE', ( #19446, #19475, #13254, #5974, #10657, #3237, #3799, #16797, #5868, #9821, #4984, #19568, #810, #1069, #6421, #10027, #19045, #17347, #4220, #8918, #11038, #17146, #17892, #2551, #696, #18392, #17984, #3289, #2047, #16257, #7262, #5112, #719, #15681, #7978, #14584, #15014, #1938, #3922, #8226, #1326, #6708, #2118, #3519, #3113, #14230, #7090, #5597, #7730, #11059, #5311, #12433, #4996, #21074, #793, #4107, #8014, #2073, #9329, #18123, #16890, #8262, #5539, #4842, #5048, #13490, #20701, #8758, #15832, #11644, #15736, #7433, #14578, #5688, #2289, #16300, #5586, #10820, #2833, #18566, #20713, #18646, #13690, #4920, #10304, #3658, #1619, #20255, #10544, #18640, #17433, #16239, #16585, #20668, #2164, #12549, #19430, #5299, #7809, #13963, #11930, #11851, #16608, #17048, #13911, #175, #4477, #19190, #15379, #9868, #2202, #18967, #14724, #5412, #13610, #18518, #18272, #7687, #18017, #8621, #11647, #21332, #17330, #5420, #21480, #11883, #8541, #18459, #10516, #17894, #17295, #19495, #671, #21784, #16933, #20783 ) ) ;
#15354=CARTESIAN_POINT ( 'NONE',  ( 10.00000000000000000, -15.25521607131222268, 23.70650506194164464 ) ) ;
#15356=ORIENTED_EDGE ( 'NONE', *, *, #10270, .T. ) ;
#15359=AXIS2_PLACEMENT_3D ( 'NONE', #8461, #18838, #16965 ) ;
#15363=ORIENTED_EDGE ( 'NONE', *, *, #16344, .F. ) ;
#15365=CARTESIAN_POINT ( 'NONE',  ( 5.000000000000000888, -31.88200538760795766, 2.745493118646880504 ) ) ;
#15369=DIRECTION ( 'NONE',  ( 0.000000000000000000, 0.000000000000000000, 1.000000000000000000 ) ) ;
#15373=AXIS2_PLACEMENT_3D ( 'NONE', #5113, #5440, #363 ) ;
#15375=DIRECTION ( 'NONE',  ( 0.000000000000000000, 0.000000000000000000, 1.000000000000000000 ) ) ;
#15379=ADVANCED_FACE ( 'NONE', ( #3616 ), #5068, .T. ) ;
#15392=ORIENTED_EDGE ( 'NONE', *, *, #14705, .F. ) ;
#15393=ORIENTED_EDGE ( 'NONE', *, *, #3556, .F. ) ;
#15405=CIRCLE ( 'NONE', #2006, 11.99999999999999822 ) ;
#15410=LINE ( 'NONE', #17074, #3180 ) ;
#15412=DIRECTION ( 'NONE',  ( 1.000000000000000000, 0.000000000000000000, -0.000000000000000000 ) ) ;
#15416=FACE_OUTER_BOUND ( 'NONE', #11546, .T. ) ;
#15418=VERTEX_POINT ( 'NONE', #8593 ) ;
#15421=AXIS2_PLACEMENT_3D ( 'NONE', #19008, #20225, #5089 ) ;
#15423=ORIENTED_EDGE ( 'NONE', *, *, #11671, .F. ) ;
#15436=CYLINDRICAL_SURFACE ( 'NONE', #14342, 27.49900000000000233 ) ;
#15438=DIRECTION ( 'NONE',  ( 0.000000000000000000, 0.000000000000000000, 1.000000000000000000 ) ) ;
#15448=VERTEX_POINT ( 'NONE', #19409 ) ;
#15454=CARTESIAN_POINT ( 'NONE',  ( 0.000000000000000000, 26.27606311335965827, -10.21217444509384364 ) ) ;
#15458=DIRECTION ( 'NONE',  ( 0.000000000000000000, -0.4067366430757888285, -0.9135454576426059736 ) ) ;
#15459=CARTESIAN_POINT ( 'NONE',  ( 0.000000000000000000, 0.000000000000000000, -5.000000000000000000 ) ) ;
#15463=DIRECTION ( 'NONE',  ( -1.000000000000000000, 0.000000000000000000, 0.000000000000000000 ) ) ;
#15471=ORIENTED_EDGE ( 'NONE', *, *, #21203, .F. ) ;
#15473=AXIS2_PLACEMENT_3D ( 'NONE', #12771, #11131, #5947 ) ;
#15484=DIRECTION ( 'NONE',  ( 0.000000000000000000, 0.000000000000000000, 1.000000000000000000 ) ) ;
#15497=CIRCLE ( 'NONE', #5983, 32.00000000000000000 ) ;
#15502=AXIS2_PLACEMENT_3D ( 'NONE', #7362, #12215, #11999 ) ;
#15508=DIRECTION ( 'NONE',  ( 0.000000000000000000, 0.000000000000000000, 1.000000000000000000 ) ) ;
#15514=DIRECTION ( 'NONE',  ( -1.000000000000000000, 0.000000000000000000, 0.000000000000000000 ) ) ;
#15518=EDGE_CURVE ( 'NONE', #16668, #11869, #11268, .T. ) ;
#15519=DIRECTION ( 'NONE',  ( -1.000000000000000000, 0.000000000000000000, 0.000000000000000000 ) ) ;
#15529=DIRECTION ( 'NONE',  ( -1.000000000000000000, -0.000000000000000000, 0.000000000000000000 ) ) ;
#15540=ORIENTED_EDGE ( 'NONE', *, *, #2990, .T. ) ;
#15542=EDGE_CURVE ( 'NONE', #4811, #15448, #18981, .T. ) ;
#15548=FACE_OUTER_BOUND ( 'NONE', #18843, .T. ) ;
#15561=ORIENTED_EDGE ( 'NONE', *, *, #14960, .T. ) ;
#15562=ORIENTED_EDGE ( 'NONE', *, *, #1528, .T. ) ;
#15564=EDGE_CURVE ( 'NONE', #9611, #3591, #13885, .T. ) ;
#15567=AXIS2_PLACEMENT_3D ( 'NONE', #21837, #20187, #17085 ) ;
#15574=CARTESIAN_POINT ( 'NONE',  ( 5.000000000000000000, 24.17932380791719282, 20.96092317127012805 ) ) ;
#15578=FACE_OUTER_BOUND ( 'NONE', #10477, .T. ) ;
#15579=VERTEX_POINT ( 'NONE', #19511 ) ;
#15592=DIRECTION ( 'NONE',  ( 0.000000000000000000, 0.000000000000000000, -1.000000000000000000 ) ) ;
#15596=DIRECTION ( 'NONE',  ( -1.000000000000000000, 0.000000000000000000, 0.000000000000000000 ) ) ;
#15602=DIRECTION ( 'NONE',  ( 0.000000000000000000, -1.000000000000000000, 0.000000000000000000 ) ) ;
#15608=VERTEX_POINT ( 'NONE', #8031 ) ;
#15612=AXIS2_PLACEMENT_3D ( 'NONE', #226, #11610, #13255 ) ;
#15625=CYLINDRICAL_SURFACE ( 'NONE', #20389, 27.49900000000000233 ) ;
#15628=AXIS2_PLACEMENT_3D ( 'NONE', #2855, #4183, #10918 ) ;
#15632=EDGE_CURVE ( 'NONE', #19849, #10985, #11562, .T. ) ;
#15635=ORIENTED_EDGE ( 'NONE', *, *, #17759, .T. ) ;
#15640=CIRCLE ( 'NONE', #8584, 11.99999999999999822 ) ;
#15643=CARTESIAN_POINT ( 'NONE',  ( 10.00000000000000000, -4.294029059349679045, -27.86182539015970505 ) ) ;
#15646=DIRECTION ( 'NONE',  ( -1.000000000000000000, -0.000000000000000000, -0.000000000000000000 ) ) ;
#15647=ORIENTED_EDGE ( 'NONE', *, *, #6275, .F. ) ;
#15651=EDGE_CURVE ( 'NONE', #6083, #11017, #359, .T. ) ;
#15665=CARTESIAN_POINT ( 'NONE',  ( 150.0000507999999968, 0.000000000000000000, 3.000000000000000444 ) ) ;
#15667=VERTEX_POINT ( 'NONE', #6051 ) ;
#15669=CARTESIAN_POINT ( 'NONE',  ( 10.00000000000000000, 0.000000000000000000, 0.000000000000000000 ) ) ;
#15670=CARTESIAN_POINT ( 'NONE',  ( 5.000000000000000888, -31.75612719289738095, -3.943144139962873940 ) ) ;
#15681=ADVANCED_FACE ( 'NONE', ( #4703 ), #954, .T. ) ;
#15684=DIRECTION ( 'NONE',  ( -1.000000000000000000, 0.000000000000000000, 0.000000000000000000 ) ) ;
#15685=ORIENTED_EDGE ( 'NONE', *, *, #17493, .T. ) ;
#15688=VERTEX_POINT ( 'NONE', #4603 ) ;
#15689=DIRECTION ( 'NONE',  ( 1.000000000000000000, 0.000000000000000000, 0.000000000000000000 ) ) ;
#15692=AXIS2_PLACEMENT_3D ( 'NONE', #9691, #6417, #9922 ) ;
#15696=VECTOR ( 'NONE', #18188, 1000.000000000000000 ) ;
#15698=ORIENTED_EDGE ( 'NONE', *, *, #7826, .F. ) ;
#15702=LINE ( 'NONE', #20679, #448 ) ;
#15703=CYLINDRICAL_SURFACE ( 'NONE', #1601, 27.49900000000000233 ) ;
#15708=DIRECTION ( 'NONE',  ( -1.000000000000000000, 0.000000000000000000, 0.000000000000000000 ) ) ;
#15709=CARTESIAN_POINT ( 'NONE',  ( 10.00000000000000000, 26.27606311335951617, 10.21217444509420424 ) ) ;
#15710=LINE ( 'NONE', #21011, #2080 ) ;
#15713=ORIENTED_EDGE ( 'NONE', *, *, #2138, .T. ) ;
#15719=DIRECTION ( 'NONE',  ( 0.000000000000000000, 0.000000000000000000, -1.000000000000000000 ) ) ;
#15723=ORIENTED_EDGE ( 'NONE', *, *, #14179, .F. ) ;
#15726=ORIENTED_EDGE ( 'NONE', *, *, #4003, .T. ) ;
#15736=ADVANCED_FACE ( 'NONE', ( #16970 ), #21715, .T. ) ;
#15746=VERTEX_POINT ( 'NONE', #3375 ) ;
#15748=FACE_OUTER_BOUND ( 'NONE', #12219, .T. ) ;
#15753=VERTEX_POINT ( 'NONE', #13430 ) ;
#15757=DIRECTION ( 'NONE',  ( 0.000000000000000000, 0.000000000000000000, 1.000000000000000000 ) ) ;
#15759=EDGE_CURVE ( 'NONE', #12763, #5686, #15410, .T. ) ;
#15765=CARTESIAN_POINT ( 'NONE',  ( 5.000000000000000888, 30.24235385705252099, -10.45944707835077558 ) ) ;
#15766=DIRECTION ( 'NONE',  ( -1.000000000000000000, 0.000000000000000000, 0.000000000000000000 ) ) ;
#15768=ORIENTED_EDGE ( 'NONE', *, *, #18128, .T. ) ;
#15773=DIRECTION ( 'NONE',  ( 0.000000000000000000, 0.9510565162951544194, -0.3090169943749449533 ) ) ;
#15775=ORIENTED_EDGE ( 'NONE', *, *, #4622, .T. ) ;
#15786=CARTESIAN_POINT ( 'NONE',  ( -10.00000000000000000, 0.000000000000000000, 0.000000000000000000 ) ) ;
#15789=DIRECTION ( 'NONE',  ( -1.000000000000000000, -0.000000000000000000, 0.000000000000000000 ) ) ;
#15794=CYLINDRICAL_SURFACE ( 'NONE', #20347, 27.49900000000000233 ) ;
#15801=CIRCLE ( 'NONE', #2394, 11.99999999999999645 ) ;
#15802=ORIENTED_EDGE ( 'NONE', *, *, #7980, .F. ) ;
#15803=VECTOR ( 'NONE', #6365, 1000.000000000000000 ) ;
#15808=DIRECTION ( 'NONE',  ( 1.000000000000000000, -0.000000000000000000, 0.000000000000000000 ) ) ;
#15810=ORIENTED_EDGE ( 'NONE', *, *, #5191, .F. ) ;
#15817=CARTESIAN_POINT ( 'NONE',  ( 10.00000000000000000, 0.000000000000000000, 0.000000000000000000 ) ) ;
#15820=CARTESIAN_POINT ( 'NONE',  ( 0.000000000000000000, 0.000000000000000000, 0.000000000000000000 ) ) ;
#15827=ORIENTED_EDGE ( 'NONE', *, *, #4906, .F. ) ;
#15830=EDGE_CURVE ( 'NONE', #13720, #874, #560, .T. ) ;
#15832=ADVANCED_FACE ( 'NONE', ( #1498 ), #8240, .T. ) ;
#15835=DIRECTION ( 'NONE',  ( -1.000000000000000000, 0.000000000000000000, -0.000000000000000000 ) ) ;
#15836=ORIENTED_EDGE ( 'NONE', *, *, #21727, .T. ) ;
#15842=ORIENTED_EDGE ( 'NONE', *, *, #2138, .F. ) ;
#15844=AXIS2_PLACEMENT_3D ( 'NONE', #8715, #15010, #17332 ) ;
#15847=DIRECTION ( 'NONE',  ( -1.000000000000000000, -0.000000000000000000, 0.000000000000000000 ) ) ;
#15854=EDGE_LOOP ( 'NONE', ( #7629, #102, #4234, #7575 ) ) ;
#15856=CIRCLE ( 'NONE', #2443, 32.00000000000000000 ) ;
#15858=ORIENTED_EDGE ( 'NONE', *, *, #13929, .T. ) ;
#15859=AXIS2_PLACEMENT_3D ( 'NONE', #16862, #1730, #18639 ) ;
#15860=EDGE_CURVE ( 'NONE', #4990, #2536, #9014, .T. ) ;
#15863=CYLINDRICAL_SURFACE ( 'NONE', #9854, 27.49900000000000233 ) ;
#15870=ORIENTED_EDGE ( 'NONE', *, *, #8288, .F. ) ;
#15875=DIRECTION ( 'NONE',  ( 0.000000000000000000, 0.2079116908177599532, -0.9781476007338055778 ) ) ;
#15882=CARTESIAN_POINT ( 'NONE',  ( 10.00000000000000000, 26.27606311335965827, -10.21217444509384364 ) ) ;
#15883=DIRECTION ( 'NONE',  ( 0.000000000000000000, 0.000000000000000000, 1.000000000000000000 ) ) ;
#15887=ORIENTED_EDGE ( 'NONE', *, *, #9987, .F. ) ;
#15892=ORIENTED_EDGE ( 'NONE', *, *, #12850, .T. ) ;
#15893=DIRECTION ( 'NONE',  ( 0.000000000000000000, 0.000000000000000000, 1.000000000000000000 ) ) ;
#15906=VECTOR ( 'NONE', #62, 1000.000000000000000 ) ;
#15907=EDGE_CURVE ( 'NONE', #14635, #5699, #19272, .T. ) ;
#15911=AXIS2_PLACEMENT_3D ( 'NONE', #16869, #5371, #10007 ) ;
#15913=ORIENTED_EDGE ( 'NONE', *, *, #6236, .T. ) ;
#15914=CYLINDRICAL_SURFACE ( 'NONE', #9109, 11.99999999999999822 ) ;
#15922=CARTESIAN_POINT ( 'NONE',  ( 0.000000000000000000, 27.48365448817206769, -0.9185515634842869037 ) ) ;
#15923=DIRECTION ( 'NONE',  ( 0.000000000000000000, 0.000000000000000000, 1.000000000000000000 ) ) ;
#15931=CARTESIAN_POINT ( 'NONE',  ( 0.000000000000000000, -27.07404830566967746, -4.815694066514710769 ) ) ;
#15939=DIRECTION ( 'NONE',  ( 0.000000000000000000, 0.2079116908177532919, 0.9781476007338070211 ) ) ;
#15941=DIRECTION ( 'NONE',  ( 0.000000000000000000, 0.000000000000000000, -1.000000000000000000 ) ) ;
#15948=CARTESIAN_POINT ( 'NONE',  ( 10.00000000000000000, -27.48365448817206058, -0.9185515634844814148 ) ) ;
#15950=EDGE_LOOP ( 'NONE', ( #7798, #5455, #11200, #2295 ) ) ;
#15951=CARTESIAN_POINT ( 'NONE',  ( 10.00000000000000000, 0.000000000000000000, 0.000000000000000000 ) ) ;
#15955=EDGE_CURVE ( 'NONE', #10449, #17973, #11452, .T. ) ;
#15958=ORIENTED_EDGE ( 'NONE', *, *, #12871, .T. ) ;
#15960=ORIENTED_EDGE ( 'NONE', *, *, #5710, .T. ) ;
#15963=CARTESIAN_POINT ( 'NONE',  ( 10.00000000000000000, 0.000000000000000000, 0.000000000000000000 ) ) ;
#15971=CARTESIAN_POINT ( 'NONE',  ( 0.000000000000000000, 28.00896854771991329, 15.47571261340933546 ) ) ;
#15979=CYLINDRICAL_SURFACE ( 'NONE', #3429, 12.00000000000000000 ) ;
#15981=EDGE_CURVE ( 'NONE', #2536, #19281, #3380, .T. ) ;
#15985=ORIENTED_EDGE ( 'NONE', *, *, #10116, .T. ) ;
#15989=ORIENTED_EDGE ( 'NONE', *, *, #15651, .T. ) ;
#15991=AXIS2_PLACEMENT_3D ( 'NONE', #15786, #14128, #9247 ) ;
#15999=DIRECTION ( 'NONE',  ( -1.000000000000000000, -0.000000000000000000, 0.000000000000000000 ) ) ;
#16006=ORIENTED_EDGE ( 'NONE', *, *, #14454, .F. ) ;
#16009=ORIENTED_EDGE ( 'NONE', *, *, #18697, .F. ) ;
#16021=DIRECTION ( 'NONE',  ( 0.000000000000000000, 0.2079116908177532919, 0.9781476007338070211 ) ) ;
#16024=CARTESIAN_POINT ( 'NONE',  ( -10.00000000000000000, 0.000000000000000000, 0.000000000000000000 ) ) ;
#16027=EDGE_CURVE ( 'NONE', #16206, #16668, #18220, .T. ) ;
#16034=CYLINDRICAL_SURFACE ( 'NONE', #8838, 12.00000000000000000 ) ;
#16036=CARTESIAN_POINT ( 'NONE',  ( 10.00000000000000000, -7.619321854369379032, -26.42235673590698397 ) ) ;
#16041=VERTEX_POINT ( 'NONE', #9531 ) ;
#16043=DIRECTION ( 'NONE',  ( -1.000000000000000000, 0.000000000000000000, -0.000000000000000000 ) ) ;
#16045=CIRCLE ( 'NONE', #19227, 32.00000000000000000 ) ;
#16047=CARTESIAN_POINT ( 'NONE',  ( 5.000000000000000888, -31.75612719289743779, 3.943144139962448058 ) ) ;
#16050=EDGE_CURVE ( 'NONE', #17052, #16573, #16177, .T. ) ;
#16058=ORIENTED_EDGE ( 'NONE', *, *, #1528, .F. ) ;
#16059=AXIS2_PLACEMENT_3D ( 'NONE', #1740, #15316, #5173 ) ;
#16061=VERTEX_POINT ( 'NONE', #17841 ) ;
#16062=AXIS2_PLACEMENT_3D ( 'NONE', #10215, #8662, #5463 ) ;
#16063=CARTESIAN_POINT ( 'NONE',  ( 0.000000000000000000, -28.15804365424196121, 10.64184787299373269 ) ) ;
#16068=CIRCLE ( 'NONE', #4789, 11.99999999999999822 ) ;
#16071=EDGE_CURVE ( 'NONE', #13874, #13666, #10440, .T. ) ;
#16080=DIRECTION ( 'NONE',  ( 0.000000000000000000, 0.000000000000000000, -1.000000000000000000 ) ) ;
#16081=EDGE_CURVE ( 'NONE', #8553, #11931, #11203, .T. ) ;
#16084=CARTESIAN_POINT ( 'NONE',  ( 10.00000000000000000, 17.83210509884670714, -21.83428559348744002 ) ) ;
#16099=DIRECTION ( 'NONE',  ( 1.000000000000000000, 0.000000000000000000, 0.000000000000000000 ) ) ;
#16100=EDGE_CURVE ( 'NONE', #16815, #15166, #10722, .T. ) ;
#16103=AXIS2_PLACEMENT_3D ( 'NONE', #13239, #4853, #9693 ) ;
#16106=CIRCLE ( 'NONE', #6601, 27.49900000000000588 ) ;
#16109=DIRECTION ( 'NONE',  ( 1.000000000000000000, -0.000000000000000000, 0.000000000000000000 ) ) ;
#16111=DIRECTION ( 'NONE',  ( -1.000000000000000000, -0.000000000000000000, -0.000000000000000000 ) ) ;
#16124=ORIENTED_EDGE ( 'NONE', *, *, #1642, .T. ) ;
#16128=EDGE_CURVE ( 'NONE', #19694, #20854, #2441, .T. ) ;
#16141=CARTESIAN_POINT ( 'NONE',  ( 0.000000000000000000, 12.90282758292980247, 25.06465718894781247 ) ) ;
#16142=CARTESIAN_POINT ( 'NONE',  ( -10.00000000000000000, 0.000000000000000000, 0.000000000000000000 ) ) ;
#16143=DIRECTION ( 'NONE',  ( -1.000000000000000000, 0.000000000000000000, 0.000000000000000000 ) ) ;
#16145=DIRECTION ( 'NONE',  ( -1.000000000000000000, -0.000000000000000000, -0.000000000000000000 ) ) ;
#16146=AXIS2_PLACEMENT_3D ( 'NONE', #17745, #5703, #2595 ) ;
#16148=ORIENTED_EDGE ( 'NONE', *, *, #8529, .T. ) ;
#16149=CIRCLE ( 'NONE', #5233, 27.49900000000000588 ) ;
#16151=DIRECTION ( 'NONE',  ( -1.000000000000000000, -0.000000000000000000, 0.000000000000000000 ) ) ;
#16158=AXIS2_PLACEMENT_3D ( 'NONE', #8636, #20683, #5546 ) ;
#16160=ORIENTED_EDGE ( 'NONE', *, *, #15981, .T. ) ;
#16163=CARTESIAN_POINT ( 'NONE',  ( 10.00000000000000000, -23.57863763525731216, 15.45211464167656601 ) ) ;
#16167=CARTESIAN_POINT ( 'NONE',  ( 0.000000000000000000, -27.48365448817206058, -0.9185515634844814148 ) ) ;
#16170=CIRCLE ( 'NONE', #5248, 27.49900000000000233 ) ;
#16172=VECTOR ( 'NONE', #346, 1000.000000000000000 ) ;
#16177=LINE ( 'NONE', #924, #7268 ) ;
#16183=AXIS2_PLACEMENT_3D ( 'NONE', #18144, #1860, #3304 ) ;
#16192=CARTESIAN_POINT ( 'NONE',  ( 10.00000000000000000, 26.69209308833516658, -6.612652082459054448 ) ) ;
#16205=CARTESIAN_POINT ( 'NONE',  ( 10.00000000000000000, -12.90282758292996235, 25.06465718894773431 ) ) ;
#16206=VERTEX_POINT ( 'NONE', #4101 ) ;
#16212=EDGE_CURVE ( 'NONE', #16041, #16573, #2994, .T. ) ;
#16224=DIRECTION ( 'NONE',  ( 0.000000000000000000, 0.000000000000000000, 1.000000000000000000 ) ) ;
#16225=CARTESIAN_POINT ( 'NONE',  ( 0.000000000000000000, -1.959304526717989381, 27.42911093658674559 ) ) ;
#16237=ORIENTED_EDGE ( 'NONE', *, *, #2208, .F. ) ;
#16239=ADVANCED_FACE ( 'NONE', ( #18554 ), #18342, .T. ) ;
#16250=DIRECTION ( 'NONE',  ( 0.000000000000000000, 0.9510565162951523099, 0.3090169943749512815 ) ) ;
#16253=DIRECTION ( 'NONE',  ( -1.000000000000000000, 0.000000000000000000, 0.000000000000000000 ) ) ;
#16257=ADVANCED_FACE ( 'NONE', ( #20204 ), #13025, .T. ) ;
#16260=VERTEX_POINT ( 'NONE', #2966 ) ;
#16261=CARTESIAN_POINT ( 'NONE',  ( 10.00000000000000000, 3.786343810537937227, -27.23708136986048700 ) ) ;
#16264=DIRECTION ( 'NONE',  ( -1.000000000000000000, 0.000000000000000000, 0.000000000000000000 ) ) ;
#16266=VERTEX_POINT ( 'NONE', #3190 ) ;
#16271=CYLINDRICAL_SURFACE ( 'NONE', #6715, 12.00000000000000000 ) ;
#16272=DIRECTION ( 'NONE',  ( 1.000000000000000000, -0.000000000000000000, -0.000000000000000000 ) ) ;
#16279=ORIENTED_EDGE ( 'NONE', *, *, #21847, .F. ) ;
#16284=FACE_OUTER_BOUND ( 'NONE', #20308, .T. ) ;
#16286=( NAMED_UNIT ( * ) PLANE_ANGLE_UNIT ( ) SI_UNIT ( $, .RADIAN. ) );
#16291=ORIENTED_EDGE ( 'NONE', *, *, #5342, .F. ) ;
#16298=DIRECTION ( 'NONE',  ( -1.000000000000000000, -0.000000000000000000, -0.000000000000000000 ) ) ;
#16299=UNCERTAINTY_MEASURE_WITH_UNIT (LENGTH_MEASURE( 1.000000000000000082E-05 ), #16383, 'distance_accuracy_value', 'NONE');
#16300=ADVANCED_FACE ( 'NONE', ( #19871 ), #14799, .T. ) ;
#16301=PRODUCT_DEFINITION_FORMATION_WITH_SPECIFIED_SOURCE ( 'ANY', '', #8086, .NOT_KNOWN. ) ;
#16304=CIRCLE ( 'NONE', #15241, 11.99999999999999822 ) ;
#16306=VERTEX_POINT ( 'NONE', #19472 ) ;
#16307=EDGE_CURVE ( 'NONE', #3827, #16396, #21539, .T. ) ;
#16309=EDGE_LOOP ( 'NONE', ( #1779, #7951, #8631, #11808 ) ) ;
#16310=VECTOR ( 'NONE', #5355, 1000.000000000000000 ) ;
#16314=AXIS2_PLACEMENT_3D ( 'NONE', #206, #5290, #17101 ) ;
#16315=DIRECTION ( 'NONE',  ( 1.000000000000000000, 0.000000000000000000, 0.000000000000000000 ) ) ;
#16330=CARTESIAN_POINT ( 'NONE',  ( 0.000000000000000000, 0.000000000000000000, 0.000000000000000000 ) ) ;
#16333=CARTESIAN_POINT ( 'NONE',  ( 10.00000000000000000, 0.000000000000000000, 0.000000000000000000 ) ) ;
#16340=EDGE_CURVE ( 'NONE', #18743, #5507, #11102, .T. ) ;
#16343=ORIENTED_EDGE ( 'NONE', *, *, #11895, .F. ) ;
#16344=EDGE_CURVE ( 'NONE', #8622, #5258, #2632, .T. ) ;
#16349=CIRCLE ( 'NONE', #13891, 12.00000000000000178 ) ;
#16357=EDGE_CURVE ( 'NONE', #11720, #12094, #13581, .T. ) ;
#16371=ORIENTED_EDGE ( 'NONE', *, *, #4077, .F. ) ;
#16374=CARTESIAN_POINT ( 'NONE',  ( 10.00000000000000000, -27.07404830566967746, -4.815694066514710769 ) ) ;
#16375=VERTEX_POINT ( 'NONE', #20631 ) ;
#16383=( LENGTH_UNIT ( ) NAMED_UNIT ( * ) SI_UNIT ( .MILLI., .METRE. ) );
#16385=CARTESIAN_POINT ( 'NONE',  ( 10.00000000000000000, 23.37352460145283217, 21.85585385440887762 ) ) ;
#16390=ORIENTED_EDGE ( 'NONE', *, *, #21463, .T. ) ;
#16396=VERTEX_POINT ( 'NONE', #1970 ) ;
#16400=EDGE_LOOP ( 'NONE', ( #1915, #4385, #98, #586 ) ) ;
#16409=DIRECTION ( 'NONE',  ( 0.000000000000000000, 0.000000000000000000, -1.000000000000000000 ) ) ;
#16411=DIRECTION ( 'NONE',  ( 0.000000000000000000, 0.000000000000000000, 1.000000000000000000 ) ) ;
#16415=AXIS2_PLACEMENT_3D ( 'NONE', #21499, #8130, #18301 ) ;
#16418=DIRECTION ( 'NONE',  ( -1.000000000000000000, 0.000000000000000000, -0.000000000000000000 ) ) ;
#16423=DIRECTION ( 'NONE',  ( -1.000000000000000000, 0.000000000000000000, 0.000000000000000000 ) ) ;
#16425=ORIENTED_EDGE ( 'NONE', *, *, #20890, .T. ) ;
#16429=ORIENTED_EDGE ( 'NONE', *, *, #11503, .T. ) ;
#16431=ORIENTED_EDGE ( 'NONE', *, *, #20965, .F. ) ;
#16435=AXIS2_PLACEMENT_3D ( 'NONE', #5443, #2225, #15375 ) ;
#16441=DIRECTION ( 'NONE',  ( 0.000000000000000000, 0.000000000000000000, -1.000000000000000000 ) ) ;
#16446=DIRECTION ( 'NONE',  ( -1.000000000000000000, 0.000000000000000000, 0.000000000000000000 ) ) ;
#16450=CARTESIAN_POINT ( 'NONE',  ( -10.00000000000000000, 0.000000000000000000, 0.000000000000000000 ) ) ;
#16451=LINE ( 'NONE', #8064, #3414 ) ;
#16463=DIRECTION ( 'NONE',  ( -1.000000000000000000, -0.000000000000000000, 0.000000000000000000 ) ) ;
#16465=FACE_OUTER_BOUND ( 'NONE', #10885, .T. ) ;
#16469=CARTESIAN_POINT ( 'NONE',  ( 10.00000000000000000, -19.85071254963791176, 20.01672328094525000 ) ) ;
#16470=AXIS2_PLACEMENT_3D ( 'NONE', #10947, #14374, #5994 ) ;
#16474=VERTEX_POINT ( 'NONE', #13567 ) ;
#16491=EDGE_CURVE ( 'NONE', #17402, #21395, #17123, .T. ) ;
#16492=ORIENTED_EDGE ( 'NONE', *, *, #9493, .T. ) ;
#16498=LINE ( 'NONE', #1773, #163 ) ;
#16505=ORIENTED_EDGE ( 'NONE', *, *, #7093, .F. ) ;
#16508=ORIENTED_EDGE ( 'NONE', *, *, #20433, .T. ) ;
#16510=CARTESIAN_POINT ( 'NONE',  ( 10.00000000000000000, 19.85071254963803611, -20.01672328094512565 ) ) ;
#16513=DIRECTION ( 'NONE',  ( -1.000000000000000000, 0.000000000000000000, -0.000000000000000000 ) ) ;
#16515=VERTEX_POINT ( 'NONE', #11914 ) ;
#16517=ORIENTED_EDGE ( 'NONE', *, *, #20011, .T. ) ;
#16518=ORIENTED_EDGE ( 'NONE', *, *, #16937, .T. ) ;
#16519=CIRCLE ( 'NONE', #6303, 11.99999999999999822 ) ;
#16522=AXIS2_PLACEMENT_3D ( 'NONE', #10513, #17371, #8962 ) ;
#16527=DIRECTION ( 'NONE',  ( 0.000000000000000000, 0.000000000000000000, 1.000000000000000000 ) ) ;
#16531=VERTEX_POINT ( 'NONE', #2395 ) ;
#16536=VECTOR ( 'NONE', #1123, 1000.000000000000000 ) ;
#16550=AXIS2_PLACEMENT_3D ( 'NONE', #21394, #19734, #4600 ) ;
#16553=CARTESIAN_POINT ( 'NONE',  ( 10.00000000000000000, 21.69483248597444813, -16.89761061231758177 ) ) ;
#16561=CARTESIAN_POINT ( 'NONE',  ( 10.00000000000000000, -22.77465461094663368, -15.41136296218110147 ) ) ;
#16565=DIRECTION ( 'NONE',  ( 1.000000000000000000, 0.000000000000000000, 0.000000000000000000 ) ) ;
#16573=VERTEX_POINT ( 'NONE', #12881 ) ;
#16575=DIRECTION ( 'NONE',  ( -1.000000000000000000, -0.000000000000000000, 0.000000000000000000 ) ) ;
#16578=CARTESIAN_POINT ( 'NONE',  ( 10.00000000000000000, 0.000000000000000000, 0.000000000000000000 ) ) ;
#16585=ADVANCED_FACE ( 'NONE', ( #9340 ), #14437, .T. ) ;
#16586=ORIENTED_EDGE ( 'NONE', *, *, #16307, .T. ) ;
#16591=FACE_OUTER_BOUND ( 'NONE', #105, .T. ) ;
#16593=CIRCLE ( 'NONE', #10941, 11.99999999999999822 ) ;
#16599=ORIENTED_EDGE ( 'NONE', *, *, #7446, .F. ) ;
#16608=ADVANCED_FACE ( 'NONE', ( #21068 ), #4050, .T. ) ;
#16611=CIRCLE ( 'NONE', #7098, 11.99999999999999822 ) ;
#16613=EDGE_CURVE ( 'NONE', #10884, #715, #17488, .T. ) ;
#16618=DIRECTION ( 'NONE',  ( -1.000000000000000000, 0.000000000000000000, 0.000000000000000000 ) ) ;
#16625=VERTEX_POINT ( 'NONE', #14327 ) ;
#16646=DIRECTION ( 'NONE',  ( 0.000000000000000000, 0.000000000000000000, 1.000000000000000000 ) ) ;
#16648=EDGE_CURVE ( 'NONE', #15753, #9954, #18548, .T. ) ;
#16652=EDGE_CURVE ( 'NONE', #910, #16782, #20317, .T. ) ;
#16653=ORIENTED_EDGE ( 'NONE', *, *, #21373, .T. ) ;
#16656=CARTESIAN_POINT ( 'NONE',  ( 10.00000000000000000, 0.000000000000000000, 0.000000000000000000 ) ) ;
#16666=DIRECTION ( 'NONE',  ( 0.000000000000000000, 0.000000000000000000, 1.000000000000000000 ) ) ;
#16668=VERTEX_POINT ( 'NONE', #8243 ) ;
#16672=AXIS2_PLACEMENT_3D ( 'NONE', #14937, #21679, #20031 ) ;
#16676=ORIENTED_EDGE ( 'NONE', *, *, #6425, .T. ) ;
#16678=DIRECTION ( 'NONE',  ( -1.000000000000000000, 0.000000000000000000, -0.000000000000000000 ) ) ;
#16679=CIRCLE ( 'NONE', #7861, 32.00000000000000000 ) ;
#16681=FACE_OUTER_BOUND ( 'NONE', #8819, .T. ) ;
#16691=VERTEX_POINT ( 'NONE', #20071 ) ;
#16692=DIRECTION ( 'NONE',  ( -1.000000000000000000, -0.000000000000000000, -0.000000000000000000 ) ) ;
#16695=ORIENTED_EDGE ( 'NONE', *, *, #20011, .F. ) ;
#16697=DIRECTION ( 'NONE',  ( 1.000000000000000000, 0.000000000000000000, -0.000000000000000000 ) ) ;
#16702=CARTESIAN_POINT ( 'NONE',  ( 0.000000000000000000, 30.24235385705238244, 10.45944707835117882 ) ) ;
#16706=( NAMED_UNIT ( * ) PLANE_ANGLE_UNIT ( ) SI_UNIT ( $, .RADIAN. ) );
#16714=FACE_OUTER_BOUND ( 'NONE', #12539, .T. ) ;
#16724=CARTESIAN_POINT ( 'NONE',  ( 0.000000000000000000, 12.46320060045724354, 29.47318494484032669 ) ) ;
#16729=DIRECTION ( 'NONE',  ( -1.000000000000000000, -0.000000000000000000, -0.000000000000000000 ) ) ;
#16731=CARTESIAN_POINT ( 'NONE',  ( -10.00000000000000000, 0.000000000000000000, 0.000000000000000000 ) ) ;
#16734=DIRECTION ( 'NONE',  ( -1.000000000000000000, -0.000000000000000000, 0.000000000000000000 ) ) ;
#16737=ORIENTED_EDGE ( 'NONE', *, *, #3767, .T. ) ;
#16740=EDGE_CURVE ( 'NONE', #16266, #289, #2644, .T. ) ;
#16744=CARTESIAN_POINT ( 'NONE',  ( 5.000000000000000000, -24.17932380791732427, 20.96092317126997884 ) ) ;
#16749=CARTESIAN_POINT ( 'NONE',  ( 0.000000000000000000, 7.240962358591573889, 31.16999300804317130 ) ) ;
#16750=ORIENTED_EDGE ( 'NONE', *, *, #4906, .T. ) ;
#16751=CIRCLE ( 'NONE', #7234, 32.00000000000000000 ) ;
#16756=ORIENTED_EDGE ( 'NONE', *, *, #7676, .T. ) ;
#16764=EDGE_CURVE ( 'NONE', #12792, #7793, #17137, .T. ) ;
#16765=DIRECTION ( 'NONE',  ( -1.000000000000000000, 0.000000000000000000, -0.000000000000000000 ) ) ;
#16780=ORIENTED_EDGE ( 'NONE', *, *, #5042, .F. ) ;
#16782=VERTEX_POINT ( 'NONE', #14770 ) ;
#16791=AXIS2_PLACEMENT_3D ( 'NONE', #17554, #17664, #15893 ) ;
#16794=ORIENTED_EDGE ( 'NONE', *, *, #15651, .F. ) ;
#16797=ADVANCED_FACE ( 'NONE', ( #3055 ), #10733, .F. ) ;
#16798=CARTESIAN_POINT ( 'NONE',  ( 10.00000000000000000, 1.959304526717801975, 27.42911093658675981 ) ) ;
#16802=AXIS2_PLACEMENT_3D ( 'NONE', #21425, #7832, #4411 ) ;
#16804=EDGE_CURVE ( 'NONE', #13666, #10884, #1978, .T. ) ;
#16806=DIRECTION ( 'NONE',  ( 0.000000000000000000, 0.000000000000000000, 1.000000000000000000 ) ) ;
#16811=CARTESIAN_POINT ( 'NONE',  ( 10.00000000000000000, -4.294029059350045863, 27.86182539015965176 ) ) ;
#16812=ORIENTED_EDGE ( 'NONE', *, *, #18830, .F. ) ;
#16815=VERTEX_POINT ( 'NONE', #14155 ) ;
#16821=CYLINDRICAL_SURFACE ( 'NONE', #781, 12.00000000000000000 ) ;
#16824=CYLINDRICAL_SURFACE ( 'NONE', #15373, 11.99999999999999822 ) ;
#16832=DIRECTION ( 'NONE',  ( 0.000000000000000000, 0.8660254037844398178, -0.4999999999999980016 ) ) ;
#16838=ORIENTED_EDGE ( 'NONE', *, *, #12054, .F. ) ;
#16843=CARTESIAN_POINT ( 'NONE',  ( 10.00000000000000000, -3.786343810537759147, 27.23708136986050832 ) ) ;
#16851=AXIS2_PLACEMENT_3D ( 'NONE', #14516, #7887, #12519 ) ;
#16855=DIRECTION ( 'NONE',  ( 0.000000000000000000, 0.000000000000000000, 1.000000000000000000 ) ) ;
#16858=ORIENTED_EDGE ( 'NONE', *, *, #4354, .F. ) ;
#16861=AXIS2_PLACEMENT_3D ( 'NONE', #3332, #13275, #11840 ) ;
#16862=CARTESIAN_POINT ( 'NONE',  ( 0.000000000000000000, -21.98203405400942856, -17.64965094506566246 ) ) ;
#16867=ORIENTED_EDGE ( 'NONE', *, *, #2550, .F. ) ;
#16869=CARTESIAN_POINT ( 'NONE',  ( 150.0000507999999968, 4.000000000000000000, 1.000000000000000000 ) ) ;
#16872=ORIENTED_EDGE ( 'NONE', *, *, #7577, .F. ) ;
#16875=VECTOR ( 'NONE', #10293, 1000.000000000000000 ) ;
#16890=ADVANCED_FACE ( 'NONE', ( #11775 ), #5773, .T. ) ;
#16894=DIRECTION ( 'NONE',  ( -1.000000000000000000, -0.000000000000000000, -0.000000000000000000 ) ) ;
#16895=ORIENTED_EDGE ( 'NONE', *, *, #12715, .F. ) ;
#16896=EDGE_CURVE ( 'NONE', #20213, #7466, #21025, .T. ) ;
#16910=LINE ( 'NONE', #1868, #12082 ) ;
#16911=DIRECTION ( 'NONE',  ( 0.000000000000000000, 0.7431448254773953543, -0.6691306063588570163 ) ) ;
#16917=DIRECTION ( 'NONE',  ( -1.000000000000000000, 0.000000000000000000, -0.000000000000000000 ) ) ;
#16919=AXIS2_PLACEMENT_3D ( 'NONE', #18744, #17197, #20611 ) ;
#16924=EDGE_CURVE ( 'NONE', #11424, #2463, #19608, .T. ) ;
#16927=DIRECTION ( 'NONE',  ( 0.000000000000000000, 0.000000000000000000, -1.000000000000000000 ) ) ;
#16929=DIRECTION ( 'NONE',  ( -1.000000000000000000, 0.000000000000000000, 0.000000000000000000 ) ) ;
#16933=ADVANCED_FACE ( 'NONE', ( #1936 ), #18633, .T. ) ;
#16936=VECTOR ( 'NONE', #10201, 1000.000000000000000 ) ;
#16937=EDGE_CURVE ( 'NONE', #20292, #18743, #285, .T. ) ;
#16938=VECTOR ( 'NONE', #9131, 1000.000000000000000 ) ;
#16945=CARTESIAN_POINT ( 'NONE',  ( 10.00000000000000000, 0.000000000000000000, 0.000000000000000000 ) ) ;
#16946=DIRECTION ( 'NONE',  ( 0.000000000000000000, 0.000000000000000000, 1.000000000000000000 ) ) ;
#16948=ORIENTED_EDGE ( 'NONE', *, *, #1108, .T. ) ;
#16949=VECTOR ( 'NONE', #21563, 1000.000000000000000 ) ;
#16952=VERTEX_POINT ( 'NONE', #19458 ) ;
#16954=ORIENTED_EDGE ( 'NONE', *, *, #17292, .T. ) ;
#16959=ORIENTED_EDGE ( 'NONE', *, *, #19896, .T. ) ;
#16963=CYLINDRICAL_SURFACE ( 'NONE', #5105, 32.00000000000000000 ) ;
#16965=DIRECTION ( 'NONE',  ( 0.000000000000000000, 0.000000000000000000, -1.000000000000000000 ) ) ;
#16966=LINE ( 'NONE', #1927, #8610 ) ;
#16970=FACE_OUTER_BOUND ( 'NONE', #8504, .T. ) ;
#16971=DIRECTION ( 'NONE',  ( -1.000000000000000000, 0.000000000000000000, 0.000000000000000000 ) ) ;
#16977=CARTESIAN_POINT ( 'NONE',  ( 0.000000000000000000, 0.6021240089805670603, -31.99433460282943997 ) ) ;
#16980=ORIENTED_EDGE ( 'NONE', *, *, #4077, .T. ) ;
#16991=CARTESIAN_POINT ( 'NONE',  ( 10.00000000000000000, 0.000000000000000000, 0.000000000000000000 ) ) ;
#16992=CYLINDRICAL_SURFACE ( 'NONE', #5046, 11.99999999999999822 ) ;
#16997=DIRECTION ( 'NONE',  ( 0.000000000000000000, 0.000000000000000000, 1.000000000000000000 ) ) ;
#17001=LINE ( 'NONE', #16261, #16536 ) ;
#17002=VERTEX_POINT ( 'NONE', #11056 ) ;
#17010=EDGE_CURVE ( 'NONE', #13187, #4811, #1613, .T. ) ;
#17012=CARTESIAN_POINT ( 'NONE',  ( 10.00000000000000000, -28.15804365424196121, -1.358152127006266197 ) ) ;
#17013=VECTOR ( 'NONE', #11692, 1000.000000000000000 ) ;
#17021=EDGE_CURVE ( 'NONE', #19331, #13000, #10781, .T. ) ;
#17022=AXIS2_PLACEMENT_3D ( 'NONE', #12058, #13722, #19125 ) ;
#17036=DIRECTION ( 'NONE',  ( 0.000000000000000000, -0.7431448254773861395, -0.6691306063588672304 ) ) ;
#17038=VECTOR ( 'NONE', #1660, 1000.000000000000000 ) ;
#17041=CARTESIAN_POINT ( 'NONE',  ( 10.00000000000000000, -15.25521607131222268, 23.70650506194164464 ) ) ;
#17045=AXIS2_PLACEMENT_3D ( 'NONE', #20222, #1663, #10 ) ;
#17048=ADVANCED_FACE ( 'NONE', ( #12819 ), #9603, .T. ) ;
#17050=DIRECTION ( 'NONE',  ( -1.000000000000000000, 0.000000000000000000, 0.000000000000000000 ) ) ;
#17051=AXIS2_PLACEMENT_3D ( 'NONE', #1518, #10134, #6512 ) ;
#17052=VERTEX_POINT ( 'NONE', #2666 ) ;
#17059=CYLINDRICAL_SURFACE ( 'NONE', #12800, 27.49900000000000233 ) ;
#17072=CIRCLE ( 'NONE', #6501, 32.00000000000000000 ) ;
#17074=CARTESIAN_POINT ( 'NONE',  ( 5.000000000000000888, 7.240962358591984227, -31.16999300804307538 ) ) ;
#17076=CARTESIAN_POINT ( 'NONE',  ( 150.0000507999999968, 4.000000000000000000, -1.000000000000000000 ) ) ;
#17079=DIRECTION ( 'NONE',  ( -1.000000000000000000, 0.000000000000000000, -0.000000000000000000 ) ) ;
#17085=DIRECTION ( 'NONE',  ( 1.000000000000000000, 0.000000000000000000, 0.000000000000000000 ) ) ;
#17087=ORIENTED_EDGE ( 'NONE', *, *, #16027, .F. ) ;
#17092=DIRECTION ( 'NONE',  ( -1.000000000000000000, -0.000000000000000000, -0.000000000000000000 ) ) ;
#17098=VECTOR ( 'NONE', #18941, 1000.000000000000000 ) ;
#17100=CARTESIAN_POINT ( 'NONE',  ( 10.00000000000000000, 1.959304526717801975, 27.42911093658675981 ) ) ;
#17101=DIRECTION ( 'NONE',  ( 0.000000000000000000, 0.9945218953682737340, -0.1045284632676503622 ) ) ;
#17107=DIRECTION ( 'NONE',  ( -1.000000000000000000, 0.000000000000000000, 0.000000000000000000 ) ) ;
#17108=CIRCLE ( 'NONE', #4409, 11.99999999999999822 ) ;
#17120=ORIENTED_EDGE ( 'NONE', *, *, #3013, .F. ) ;
#17121=DIRECTION ( 'NONE',  ( -1.000000000000000000, -0.000000000000000000, 0.000000000000000000 ) ) ;
#17123=CIRCLE ( 'NONE', #12883, 12.00000000000000000 ) ;
#17128=DIRECTION ( 'NONE',  ( -1.000000000000000000, 0.000000000000000000, -0.000000000000000000 ) ) ;
#17131=DIRECTION ( 'NONE',  ( 0.000000000000000000, 0.2079116908177599532, -0.9781476007338055778 ) ) ;
#17134=CARTESIAN_POINT ( 'NONE',  ( 0.000000000000000000, 23.37352460145313771, -21.85585385440855788 ) ) ;
#17135=EDGE_CURVE ( 'NONE', #17002, #14785, #16, .T. ) ;
#17137=CIRCLE ( 'NONE', #18201, 12.00000000000000000 ) ;
#17146=ADVANCED_FACE ( 'NONE', ( #10055 ), #14820, .T. ) ;
#17147=DIRECTION ( 'NONE',  ( -1.000000000000000000, -0.000000000000000000, 0.000000000000000000 ) ) ;
#17152=DIRECTION ( 'NONE',  ( 0.000000000000000000, 0.000000000000000000, 1.000000000000000000 ) ) ;
#17160=AXIS2_PLACEMENT_3D ( 'NONE', #2297, #2408, #10691 ) ;
#17161=ORIENTED_EDGE ( 'NONE', *, *, #16357, .T. ) ;
#17163=EDGE_CURVE ( 'NONE', #17734, #11955, #10458, .T. ) ;
#17164=EDGE_CURVE ( 'NONE', #21218, #11543, #1290, .T. ) ;
#17169=DIRECTION ( 'NONE',  ( 0.000000000000000000, 0.000000000000000000, 1.000000000000000000 ) ) ;
#17175=ORIENTED_EDGE ( 'NONE', *, *, #4229, .T. ) ;
#17180=CARTESIAN_POINT ( 'NONE',  ( 0.000000000000000000, 27.26034713664097353, -7.182859710736244629 ) ) ;
#17183=CARTESIAN_POINT ( 'NONE',  ( 10.00000000000000000, 0.000000000000000000, 0.000000000000000000 ) ) ;
#17190=AXIS2_PLACEMENT_3D ( 'NONE', #17895, #16446, #4402 ) ;
#17192=ORIENTED_EDGE ( 'NONE', *, *, #19018, .F. ) ;
#17194=ORIENTED_EDGE ( 'NONE', *, *, #10385, .T. ) ;
#17197=DIRECTION ( 'NONE',  ( -1.000000000000000000, 0.000000000000000000, 0.000000000000000000 ) ) ;
#17203=DIRECTION ( 'NONE',  ( 0.000000000000000000, 0.000000000000000000, 1.000000000000000000 ) ) ;
#17212=CARTESIAN_POINT ( 'NONE',  ( 10.00000000000000000, 27.82509854686811224, 4.525913221811229903 ) ) ;
#17216=ORIENTED_EDGE ( 'NONE', *, *, #207, .F. ) ;
#17218=DIRECTION ( 'NONE',  ( 0.000000000000000000, 0.000000000000000000, 1.000000000000000000 ) ) ;
#17219=CIRCLE ( 'NONE', #18637, 27.49900000000000233 ) ;
#17220=CARTESIAN_POINT ( 'NONE',  ( 0.000000000000000000, 1.592605004252791279, 28.14575649959894932 ) ) ;
#17224=DIRECTION ( 'NONE',  ( 1.000000000000000000, 0.000000000000000000, 0.000000000000000000 ) ) ;
#17225=ORIENTED_EDGE ( 'NONE', *, *, #5961, .T. ) ;
#17229=ORIENTED_EDGE ( 'NONE', *, *, #8506, .T. ) ;
#17230=ORIENTED_EDGE ( 'NONE', *, *, #973, .F. ) ;
#17236=DIRECTION ( 'NONE',  ( 1.000000000000000000, -0.000000000000000000, -0.000000000000000000 ) ) ;
#17241=DIRECTION ( 'NONE',  ( 0.000000000000000000, 0.000000000000000000, 1.000000000000000000 ) ) ;
#17245=VERTEX_POINT ( 'NONE', #15036 ) ;
#17249=CIRCLE ( 'NONE', #16183, 27.49900000000000588 ) ;
#17250=ORIENTED_EDGE ( 'NONE', *, *, #5, .T. ) ;
#17260=AXIS2_PLACEMENT_3D ( 'NONE', #4492, #16298, #1170 ) ;
#17264=CYLINDRICAL_SURFACE ( 'NONE', #546, 11.99999999999999822 ) ;
#17269=CIRCLE ( 'NONE', #14073, 27.49900000000000233 ) ;
#17275=CARTESIAN_POINT ( 'NONE',  ( 10.00000000000000000, -9.992993448021772807, 26.36019881529882980 ) ) ;
#17277=DIRECTION ( 'NONE',  ( -1.000000000000000000, 0.000000000000000000, -0.000000000000000000 ) ) ;
#17286=VERTEX_POINT ( 'NONE', #17134 ) ;
#17287=ORIENTED_EDGE ( 'NONE', *, *, #12233, .T. ) ;
#17290=CARTESIAN_POINT ( 'NONE',  ( 150.0000507999999968, 2.828427124746190291, 1.000000000000000000 ) ) ;
#17291=DIRECTION ( 'NONE',  ( -1.000000000000000000, 0.000000000000000000, 0.000000000000000000 ) ) ;
#17292=EDGE_CURVE ( 'NONE', #20559, #13983, #231, .T. ) ;
#17295=ADVANCED_FACE ( 'NONE', ( #557 ), #12258, .T. ) ;
#17303=ORIENTED_EDGE ( 'NONE', *, *, #21619, .F. ) ;
#17307=DIRECTION ( 'NONE',  ( -1.000000000000000000, 0.000000000000000000, -0.000000000000000000 ) ) ;
#17318=CARTESIAN_POINT ( 'NONE',  ( 10.00000000000000000, -17.83210509884626660, -21.83428559348779530 ) ) ;
#17321=DIRECTION ( 'NONE',  ( 0.000000000000000000, 0.000000000000000000, 1.000000000000000000 ) ) ;
#17330=ADVANCED_FACE ( 'NONE', ( #12150 ), #15794, .T. ) ;
#17332=DIRECTION ( 'NONE',  ( 0.000000000000000000, 0.000000000000000000, 1.000000000000000000 ) ) ;
#17336=ORIENTED_EDGE ( 'NONE', *, *, #6673, .T. ) ;
#17347=ADVANCED_FACE ( 'NONE', ( #15578 ), #7185, .T. ) ;
#17350=DIRECTION ( 'NONE',  ( 0.000000000000000000, 0.4067366430757948237, 0.9135454576426033091 ) ) ;
#17354=ORIENTED_EDGE ( 'NONE', *, *, #3089, .F. ) ;
#17356=ORIENTED_EDGE ( 'NONE', *, *, #4206, .F. ) ;
#17358=DIRECTION ( 'NONE',  ( 0.000000000000000000, 0.000000000000000000, -1.000000000000000000 ) ) ;
#17362=CARTESIAN_POINT ( 'NONE',  ( 5.000000000000000000, 28.00896854771991329, 15.47571261340933724 ) ) ;
#17370=FACE_OUTER_BOUND ( 'NONE', #8603, .T. ) ;
#17371=DIRECTION ( 'NONE',  ( -1.000000000000000000, 0.000000000000000000, 0.000000000000000000 ) ) ;
#17372=AXIS2_PLACEMENT_3D ( 'NONE', #11374, #19784, #14693 ) ;
#17382=FACE_OUTER_BOUND ( 'NONE', #19842, .T. ) ;
#17384=ORIENTED_EDGE ( 'NONE', *, *, #21369, .F. ) ;
#17402=VERTEX_POINT ( 'NONE', #1203 ) ;
#17406=DIRECTION ( 'NONE',  ( 0.000000000000000000, 0.4067366430758008744, -0.9135454576426006446 ) ) ;
#17413=ORIENTED_EDGE ( 'NONE', *, *, #17949, .F. ) ;
#17420=CARTESIAN_POINT ( 'NONE',  ( 0.000000000000000000, 9.992993448021589842, 26.36019881529889020 ) ) ;
#17426=VECTOR ( 'NONE', #2165, 1000.000000000000000 ) ;
#17429=CARTESIAN_POINT ( 'NONE',  ( 10.00000000000000000, 0.000000000000000000, 0.000000000000000000 ) ) ;
#17433=ADVANCED_FACE ( 'NONE', ( #2424 ), #12585, .T. ) ;
#17434=CARTESIAN_POINT ( 'NONE',  ( 0.000000000000000000, 0.000000000000000000, 0.000000000000000000 ) ) ;
#17443=ORIENTED_EDGE ( 'NONE', *, *, #20020, .T. ) ;
#17446=ORIENTED_EDGE ( 'NONE', *, *, #13009, .F. ) ;
#17454=DIRECTION ( 'NONE',  ( -1.000000000000000000, -0.000000000000000000, 0.000000000000000000 ) ) ;
#17456=CARTESIAN_POINT ( 'NONE',  ( 0.000000000000000000, -9.992993448021419312, -26.36019881529895770 ) ) ;
#17477=ORIENTED_EDGE ( 'NONE', *, *, #13915, .F. ) ;
#17487=CIRCLE ( 'NONE', #10763, 11.99999999999999822 ) ;
#17488=CIRCLE ( 'NONE', #4073, 32.00000000000000000 ) ;
#17493=EDGE_CURVE ( 'NONE', #12744, #21233, #5188, .T. ) ;
#17494=DIRECTION ( 'NONE',  ( 0.000000000000000000, 0.000000000000000000, 1.000000000000000000 ) ) ;
#17498=VERTEX_POINT ( 'NONE', #15008 ) ;
#17525=ORIENTED_EDGE ( 'NONE', *, *, #21081, .F. ) ;
#17530=ORIENTED_EDGE ( 'NONE', *, *, #8506, .F. ) ;
#17533=CARTESIAN_POINT ( 'NONE',  ( 10.00000000000000000, 21.98203405400955290, 17.64965094506551324 ) ) ;
#17547=AXIS2_PLACEMENT_3D ( 'NONE', #3521, #3946, #5183 ) ;
#17553=VERTEX_POINT ( 'NONE', #18446 ) ;
#17554=CARTESIAN_POINT ( 'NONE',  ( 10.00000000000000000, -28.15804365424196121, -1.358152127006266197 ) ) ;
#17558=FACE_OUTER_BOUND ( 'NONE', #2186, .T. ) ;
#17560=VECTOR ( 'NONE', #9220, 1000.000000000000000 ) ;
#17566=EDGE_CURVE ( 'NONE', #7709, #17245, #21753, .T. ) ;
#17567=AXIS2_PLACEMENT_3D ( 'NONE', #1144, #7667, #17834 ) ;
#17573=ORIENTED_EDGE ( 'NONE', *, *, #19637, .F. ) ;
#17575=ORIENTED_EDGE ( 'NONE', *, *, #12584, .T. ) ;
#17576=EDGE_CURVE ( 'NONE', #3283, #13187, #11166, .T. ) ;
#17598=AXIS2_PLACEMENT_3D ( 'NONE', #19455, #4314, #7758 ) ;
#17599=CARTESIAN_POINT ( 'NONE',  ( 0.000000000000000000, 0.000000000000000000, 0.000000000000000000 ) ) ;
#17603=EDGE_LOOP ( 'NONE', ( #6529, #3236, #1208, #6825 ) ) ;
#17610=VERTEX_POINT ( 'NONE', #3299 ) ;
#17612=ORIENTED_EDGE ( 'NONE', *, *, #17164, .T. ) ;
#17614=DIRECTION ( 'NONE',  ( 0.000000000000000000, 0.000000000000000000, 1.000000000000000000 ) ) ;
#17615=VECTOR ( 'NONE', #5837, 1000.000000000000000 ) ;
#17616=CIRCLE ( 'NONE', #21831, 32.00000000000000000 ) ;
#17617=DIRECTION ( 'NONE',  ( 0.000000000000000000, 0.000000000000000000, 1.000000000000000000 ) ) ;
#17618=EDGE_CURVE ( 'NONE', #18973, #13033, #13293, .T. ) ;
#17619=DIRECTION ( 'NONE',  ( -1.000000000000000000, -0.000000000000000000, -0.000000000000000000 ) ) ;
#17629=AXIS2_PLACEMENT_3D ( 'NONE', #7895, #21048, #19166 ) ;
#17636=CARTESIAN_POINT ( 'NONE',  ( 0.000000000000000000, -30.24235385705245349, 10.45944707835097098 ) ) ;
#17640=EDGE_LOOP ( 'NONE', ( #4483, #11704, #19660, #1599 ) ) ;
#17653=DIRECTION ( 'NONE',  ( 0.000000000000000000, 0.000000000000000000, -1.000000000000000000 ) ) ;
#17661=EDGE_LOOP ( 'NONE', ( #10771, #3148, #337, #17708 ) ) ;
#17662=EDGE_CURVE ( 'NONE', #11869, #5926, #16451, .T. ) ;
#17664=DIRECTION ( 'NONE',  ( -1.000000000000000000, 0.000000000000000000, 0.000000000000000000 ) ) ;
#17665=ORIENTED_EDGE ( 'NONE', *, *, #5685, .F. ) ;
#17666=FACE_OUTER_BOUND ( 'NONE', #6982, .T. ) ;
#17668=CARTESIAN_POINT ( 'NONE',  ( -10.00000000000000000, 0.000000000000000000, 0.000000000000000000 ) ) ;
#17673=CARTESIAN_POINT ( 'NONE',  ( 10.00000000000000888, 0.000000000000000000, 0.000000000000000000 ) ) ;
#17675=DIRECTION ( 'NONE',  ( -1.000000000000000000, 0.000000000000000000, 0.000000000000000000 ) ) ;
#17680=ORIENTED_EDGE ( 'NONE', *, *, #16896, .T. ) ;
#17683=EDGE_CURVE ( 'NONE', #18295, #19585, #12225, .T. ) ;
#17708=ORIENTED_EDGE ( 'NONE', *, *, #20801, .T. ) ;
#17714=ORIENTED_EDGE ( 'NONE', *, *, #20691, .T. ) ;
#17722=DIRECTION ( 'NONE',  ( 0.000000000000000000, 0.8660254037844361541, 0.5000000000000041078 ) ) ;
#17728=EDGE_CURVE ( 'NONE', #18476, #11575, #4137, .T. ) ;
#17731=ORIENTED_EDGE ( 'NONE', *, *, #9867, .T. ) ;
#17734=VERTEX_POINT ( 'NONE', #5616 ) ;
#17738=( LENGTH_UNIT ( ) NAMED_UNIT ( * ) SI_UNIT ( .MILLI., .METRE. ) );
#17739=ORIENTED_EDGE ( 'NONE', *, *, #14179, .T. ) ;
#17741=EDGE_CURVE ( 'NONE', #11543, #13950, #11896, .T. ) ;
#17745=CARTESIAN_POINT ( 'NONE',  ( 10.00000000000000000, 0.000000000000000000, 0.000000000000000000 ) ) ;
#17750=CARTESIAN_POINT ( 'NONE',  ( 10.00000000000000000, -7.409634587003275819, 27.19958299168154880 ) ) ;
#17756=DIRECTION ( 'NONE',  ( 0.000000000000000000, -0.7431448254773861395, -0.6691306063588671194 ) ) ;
#17759=EDGE_CURVE ( 'NONE', #13983, #18351, #5203, .T. ) ;
#17760=CARTESIAN_POINT ( 'NONE',  ( -10.00000000000000000, 0.000000000000000000, 0.000000000000000000 ) ) ;
#17763=ORIENTED_EDGE ( 'NONE', *, *, #16652, .T. ) ;
#17765=ORIENTED_EDGE ( 'NONE', *, *, #14563, .T. ) ;
#17766=AXIS2_PLACEMENT_3D ( 'NONE', #9916, #3074, #19763 ) ;
#17767=VERTEX_POINT ( 'NONE', #13681 ) ;
#17770=ORIENTED_EDGE ( 'NONE', *, *, #20890, .F. ) ;
#17790=VERTEX_POINT ( 'NONE', #10254 ) ;
#17804=CARTESIAN_POINT ( 'NONE',  ( 5.000000000000000000, 31.88200538760793634, -2.745493118647104325 ) ) ;
#17818=ORIENTED_EDGE ( 'NONE', *, *, #18018, .T. ) ;
#17819=CIRCLE ( 'NONE', #9335, 27.49900000000000944 ) ;
#17834=DIRECTION ( 'NONE',  ( 0.000000000000000000, 0.000000000000000000, 1.000000000000000000 ) ) ;
#17841=CARTESIAN_POINT ( 'NONE',  ( 10.00000000000000000, 28.00896854771991329, 15.47571261340933368 ) ) ;
#17845=CARTESIAN_POINT ( 'NONE',  ( 0.000000000000000000, -9.366510754379408610, 25.85466064925422458 ) ) ;
#17850=CIRCLE ( 'NONE', #1614, 27.49900000000000588 ) ;
#17860=FACE_OUTER_BOUND ( 'NONE', #3243, .T. ) ;
#17863=DIRECTION ( 'NONE',  ( 0.000000000000000000, 0.000000000000000000, 1.000000000000000000 ) ) ;
#17866=APPLICATION_CONTEXT ( 'automotive_design' ) ;
#17868=ORIENTED_EDGE ( 'NONE', *, *, #19630, .T. ) ;
#17869=STYLED_ITEM ( 'NONE', ( #18385 ), #13088 ) ;
#17870=DIRECTION ( 'NONE',  ( -1.000000000000000000, 0.000000000000000000, 0.000000000000000000 ) ) ;
#17878=DIRECTION ( 'NONE',  ( -1.000000000000000000, -0.000000000000000000, -0.000000000000000000 ) ) ;
#17879=ORIENTED_EDGE ( 'NONE', *, *, #20228, .T. ) ;
#17883=ORIENTED_EDGE ( 'NONE', *, *, #5024, .T. ) ;
#17884=ORIENTED_EDGE ( 'NONE', *, *, #4434, .T. ) ;
#17888=VERTEX_POINT ( 'NONE', #19635 ) ;
#17891=CARTESIAN_POINT ( 'NONE',  ( 10.00000000000000000, -12.46320060045743361, 29.47318494484024143 ) ) ;
#17892=ADVANCED_FACE ( 'NONE', ( #9231 ), #4498, .T. ) ;
#17894=ADVANCED_FACE ( 'NONE', ( #12666 ), #15979, .T. ) ;
#17895=CARTESIAN_POINT ( 'NONE',  ( 10.00000000000000000, 0.000000000000000000, 0.000000000000000000 ) ) ;
#17896=CYLINDRICAL_SURFACE ( 'NONE', #4678, 27.49900000000000233 ) ;
#17898=CARTESIAN_POINT ( 'NONE',  ( 10.00000000000000000, -1.959304526717989381, 27.42911093658674204 ) ) ;
#17900=AXIS2_PLACEMENT_3D ( 'NONE', #12348, #14113, #16997 ) ;
#17905=EDGE_LOOP ( 'NONE', ( #5430, #21754, #12636, #15802 ) ) ;
#17907=ORIENTED_EDGE ( 'NONE', *, *, #11209, .T. ) ;
#17913=CIRCLE ( 'NONE', #12964, 27.49900000000000233 ) ;
#17915=VECTOR ( 'NONE', #9336, 1000.000000000000000 ) ;
#17918=DIRECTION ( 'NONE',  ( 0.000000000000000000, 0.8660254037844398178, -0.4999999999999979461 ) ) ;
#17940=CARTESIAN_POINT ( 'NONE',  ( 10.00000000000000000, 24.73395913766463750, 12.01774797440586084 ) ) ;
#17944=CIRCLE ( 'NONE', #2781, 27.49900000000000233 ) ;
#17945=( NAMED_UNIT ( * ) SI_UNIT ( $, .STERADIAN. ) SOLID_ANGLE_UNIT ( ) );
#17949=EDGE_CURVE ( 'NONE', #12094, #15608, #6630, .T. ) ;
#17959=CIRCLE ( 'NONE', #21848, 27.49900000000000233 ) ;
#17965=VERTEX_POINT ( 'NONE', #5834 ) ;
#17966=ORIENTED_EDGE ( 'NONE', *, *, #16491, .F. ) ;
#17972=DIRECTION ( 'NONE',  ( -1.000000000000000000, -0.000000000000000000, -0.000000000000000000 ) ) ;
#17973=VERTEX_POINT ( 'NONE', #14656 ) ;
#17982=CIRCLE ( 'NONE', #5628, 27.49900000000000233 ) ;
#17984=ADVANCED_FACE ( 'NONE', ( #21611 ), #4709, .T. ) ;
#17992=ORIENTED_EDGE ( 'NONE', *, *, #7826, .T. ) ;
#17995=VERTEX_POINT ( 'NONE', #18204 ) ;
#18002=DIRECTION ( 'NONE',  ( 0.000000000000000000, 0.000000000000000000, 1.000000000000000000 ) ) ;
#18007=CARTESIAN_POINT ( 'NONE',  ( 10.00000000000000000, -7.240962358591787940, 31.16999300804311801 ) ) ;
#18012=AXIS2_PLACEMENT_3D ( 'NONE', #10737, #20806, #15719 ) ;
#18013=EDGE_CURVE ( 'NONE', #289, #19331, #9665, .T. ) ;
#18015=ORIENTED_EDGE ( 'NONE', *, *, #3118, .F. ) ;
#18017=ADVANCED_FACE ( 'NONE', ( #13320 ), #19961, .T. ) ;
#18018=EDGE_CURVE ( 'NONE', #16375, #4982, #13310, .T. ) ;
#18021=ORIENTED_EDGE ( 'NONE', *, *, #14630, .F. ) ;
#18035=AXIS2_PLACEMENT_3D ( 'NONE', #9906, #8362, #11684 ) ;
#18040=ORIENTED_EDGE ( 'NONE', *, *, #8274, .F. ) ;
#18041=DIRECTION ( 'NONE',  ( 0.000000000000000000, -0.4067366430758070361, 0.9135454576425978690 ) ) ;
#18060=ORIENTED_EDGE ( 'NONE', *, *, #21351, .T. ) ;
#18066=ORIENTED_EDGE ( 'NONE', *, *, #5847, .T. ) ;
#18067=ORIENTED_EDGE ( 'NONE', *, *, #10180, .T. ) ;
#18068=CARTESIAN_POINT ( 'NONE',  ( 10.00000000000000000, 15.25521607131206459, 23.70650506194175478 ) ) ;
#18081=AXIS2_PLACEMENT_3D ( 'NONE', #20787, #5655, #20887 ) ;
#18090=ORIENTED_EDGE ( 'NONE', *, *, #17618, .F. ) ;
#18102=CARTESIAN_POINT ( 'NONE',  ( 10.00000000000000000, -28.15804365424196121, 10.64184787299373269 ) ) ;
#18105=CARTESIAN_POINT ( 'NONE',  ( 0.000000000000000000, -24.17932380791704716, -20.96092317127029503 ) ) ;
#18116=CIRCLE ( 'NONE', #17051, 11.99999999999999822 ) ;
#18123=ADVANCED_FACE ( 'NONE', ( #18742 ), #15625, .T. ) ;
#18124=LINE ( 'NONE', #18239, #994 ) ;
#18128=EDGE_CURVE ( 'NONE', #14785, #3387, #14734, .T. ) ;
#18139=AXIS2_PLACEMENT_3D ( 'NONE', #13086, #7902, #19940 ) ;
#18144=CARTESIAN_POINT ( 'NONE',  ( 0.000000000000000000, 0.000000000000000000, 0.000000000000000000 ) ) ;
#18145=DIRECTION ( 'NONE',  ( -1.000000000000000000, 0.000000000000000000, -0.000000000000000000 ) ) ;
#18146=AXIS2_PLACEMENT_3D ( 'NONE', #8137, #13093, #16527 ) ;
#18147=ORIENTED_EDGE ( 'NONE', *, *, #15231, .T. ) ;
#18150=ORIENTED_EDGE ( 'NONE', *, *, #21847, .T. ) ;
#18152=AXIS2_PLACEMENT_3D ( 'NONE', #11904, #21845, #6734 ) ;
#18161=CARTESIAN_POINT ( 'NONE',  ( 10.00000000000000000, -1.959304526717989381, 27.42911093658674204 ) ) ;
#18163=CARTESIAN_POINT ( 'NONE',  ( 10.00000000000000000, -3.786343810537388332, -27.23708136986056161 ) ) ;
#18165=DIRECTION ( 'NONE',  ( -1.000000000000000000, 0.000000000000000000, 0.000000000000000000 ) ) ;
#18167=AXIS2_PLACEMENT_3D ( 'NONE', #7295, #3639, #2420 ) ;
#18171=CIRCLE ( 'NONE', #1931, 27.49900000000000233 ) ;
#18174=CARTESIAN_POINT ( 'NONE',  ( -10.00000000000000000, 0.000000000000000000, 0.000000000000000000 ) ) ;
#18179=( NAMED_UNIT ( * ) SI_UNIT ( $, .STERADIAN. ) SOLID_ANGLE_UNIT ( ) );
#18188=DIRECTION ( 'NONE',  ( -1.000000000000000000, -0.000000000000000000, 0.000000000000000000 ) ) ;
#18192=CIRCLE ( 'NONE', #18152, 27.49900000000000233 ) ;
#18200=VERTEX_POINT ( 'NONE', #5802 ) ;
#18201=AXIS2_PLACEMENT_3D ( 'NONE', #9553, #16418, #6489 ) ;
#18204=CARTESIAN_POINT ( 'NONE',  ( 0.000000000000000000, 0.000000000000000000, 32.00000000000000000 ) ) ;
#18207=CARTESIAN_POINT ( 'NONE',  ( 10.00000000000000000, -25.17124263951018293, 12.69364185792209909 ) ) ;
#18210=ORIENTED_EDGE ( 'NONE', *, *, #13564, .F. ) ;
#18213=ORIENTED_EDGE ( 'NONE', *, *, #14563, .F. ) ;
#18214=CARTESIAN_POINT ( 'NONE',  ( 0.000000000000000000, -9.992993448021772807, 26.36019881529882980 ) ) ;
#18216=CARTESIAN_POINT ( 'NONE',  ( 0.000000000000000000, 12.94633825542301153, -24.26081875733320814 ) ) ;
#18220=CIRCLE ( 'NONE', #4437, 32.00000000000000000 ) ;
#18229=DIRECTION ( 'NONE',  ( 1.000000000000000000, -0.000000000000000000, -0.000000000000000000 ) ) ;
#18237=ORIENTED_EDGE ( 'NONE', *, *, #18013, .F. ) ;
#18239=CARTESIAN_POINT ( 'NONE',  ( 10.00000000000000000, -1.959304526717615902, -27.42911093658677402 ) ) ;
#18240=VERTEX_POINT ( 'NONE', #10984 ) ;
#18241=CARTESIAN_POINT ( 'NONE',  ( 0.000000000000000000, 23.57863763525720202, 15.45211464167672588 ) ) ;
#18248=DIRECTION ( 'NONE',  ( -1.000000000000000000, 0.000000000000000000, 0.000000000000000000 ) ) ;
#18249=DIRECTION ( 'NONE',  ( 0.000000000000000000, 0.000000000000000000, 1.000000000000000000 ) ) ;
#18253=CARTESIAN_POINT ( 'NONE',  ( 10.00000000000000000, 25.17124263951009411, 12.69364185792227495 ) ) ;
#18261=DIRECTION ( 'NONE',  ( -1.000000000000000000, 0.000000000000000000, 0.000000000000000000 ) ) ;
#18263=AXIS2_PLACEMENT_3D ( 'NONE', #12766, #20853, #844 ) ;
#18270=DIRECTION ( 'NONE',  ( -1.000000000000000000, -0.000000000000000000, 0.000000000000000000 ) ) ;
#18271=DIRECTION ( 'NONE',  ( -1.000000000000000000, 0.000000000000000000, 0.000000000000000000 ) ) ;
#18272=ADVANCED_FACE ( 'NONE', ( #7356 ), #14090, .T. ) ;
#18276=CARTESIAN_POINT ( 'NONE',  ( -140.0000507999999968, 6.123233995736766282E-16, 5.000000000000000000 ) ) ;
#18289=EDGE_CURVE ( 'NONE', #11343, #10255, #18984, .T. ) ;
#18290=CARTESIAN_POINT ( 'NONE',  ( 0.000000000000000000, -27.82509854686807671, -4.525913221811426190 ) ) ;
#18295=VERTEX_POINT ( 'NONE', #16063 ) ;
#18296=DIRECTION ( 'NONE',  ( 0.000000000000000000, 0.000000000000000000, 1.000000000000000000 ) ) ;
#18297=VERTEX_POINT ( 'NONE', #7788 ) ;
#18301=DIRECTION ( 'NONE',  ( 0.000000000000000000, 0.000000000000000000, 1.000000000000000000 ) ) ;
#18304=CARTESIAN_POINT ( 'NONE',  ( 10.00000000000000000, -23.57863763525709189, -15.45211464167688753 ) ) ;
#18314=CARTESIAN_POINT ( 'NONE',  ( 10.00000000000000000, -12.90282758292996235, 25.06465718894773431 ) ) ;
#18315=CIRCLE ( 'NONE', #1028, 32.00000000000000000 ) ;
#18316=ORIENTED_EDGE ( 'NONE', *, *, #973, .T. ) ;
#18318=AXIS2_PLACEMENT_3D ( 'NONE', #19363, #8094, #18041 ) ;
#18320=DIRECTION ( 'NONE',  ( -1.000000000000000000, -0.000000000000000000, 0.000000000000000000 ) ) ;
#18322=FACE_OUTER_BOUND ( 'NONE', #3171, .T. ) ;
#18333=CARTESIAN_POINT ( 'NONE',  ( 0.000000000000000000, -18.31866948046784671, 26.23788002993718393 ) ) ;
#18341=CARTESIAN_POINT ( 'NONE',  ( 0.000000000000000000, 22.77465461094674026, 15.41136296218094159 ) ) ;
#18342=CYLINDRICAL_SURFACE ( 'NONE', #5118, 12.00000000000000000 ) ;
#18351=VERTEX_POINT ( 'NONE', #19712 ) ;
#18356=ORIENTED_EDGE ( 'NONE', *, *, #20972, .F. ) ;
#18370=ORIENTED_EDGE ( 'NONE', *, *, #1369, .T. ) ;
#18371=CARTESIAN_POINT ( 'NONE',  ( 10.00000000000000000, 7.619321854369911051, -26.42235673590683476 ) ) ;
#18376=ORIENTED_EDGE ( 'NONE', *, *, #15830, .T. ) ;
#18383=CARTESIAN_POINT ( 'NONE',  ( 5.000000000000000888, 18.31866948046766552, 26.23788002993730828 ) ) ;
#18385=PRESENTATION_STYLE_ASSIGNMENT (( #1574 ) ) ;
#18390=ORIENTED_EDGE ( 'NONE', *, *, #4734, .T. ) ;
#18392=ADVANCED_FACE ( 'NONE', ( #16714 ), #19928, .T. ) ;
#18404=ORIENTED_EDGE ( 'NONE', *, *, #15542, .F. ) ;
#18412=EDGE_CURVE ( 'NONE', #17610, #2850, #8329, .T. ) ;
#18415=EDGE_CURVE ( 'NONE', #16952, #4620, #11933, .T. ) ;
#18417=VERTEX_POINT ( 'NONE', #1377 ) ;
#18426=DIRECTION ( 'NONE',  ( -1.000000000000000000, 0.000000000000000000, 0.000000000000000000 ) ) ;
#18427=CARTESIAN_POINT ( 'NONE',  ( 10.00000000000000000, 0.000000000000000000, 0.000000000000000000 ) ) ;
#18432=EDGE_LOOP ( 'NONE', ( #19222, #8660, #17192, #4773 ) ) ;
#18435=DIRECTION ( 'NONE',  ( -1.000000000000000000, 0.000000000000000000, -0.000000000000000000 ) ) ;
#18446=CARTESIAN_POINT ( 'NONE',  ( 10.00000000000000000, 28.15804365424197186, 10.64184787299392454 ) ) ;
#18453=ORIENTED_EDGE ( 'NONE', *, *, #14613, .T. ) ;
#18455=CIRCLE ( 'NONE', #1519, 11.99999999999999822 ) ;
#18459=ADVANCED_FACE ( 'NONE', ( #20375 ), #2131, .T. ) ;
#18461=DIRECTION ( 'NONE',  ( -1.000000000000000000, 0.000000000000000000, -0.000000000000000000 ) ) ;
#18462=CARTESIAN_POINT ( 'NONE',  ( 10.00000000000000000, -12.94633825542284278, 24.26081875733330406 ) ) ;
#18463=DIRECTION ( 'NONE',  ( -1.000000000000000000, 0.000000000000000000, 0.000000000000000000 ) ) ;
#18464=CARTESIAN_POINT ( 'NONE',  ( 10.00000000000000000, 3.786343810537573518, 27.23708136986054029 ) ) ;
#18466=CARTESIAN_POINT ( 'NONE',  ( 10.00000000000000000, 27.48365448817206769, 0.9185515634842894572 ) ) ;
#18470=CIRCLE ( 'NONE', #11391, 11.99999999999999645 ) ;
#18472=DIRECTION ( 'NONE',  ( 0.000000000000000000, 0.000000000000000000, 1.000000000000000000 ) ) ;
#18475=ORIENTED_EDGE ( 'NONE', *, *, #14089, .F. ) ;
#18476=VERTEX_POINT ( 'NONE', #6898 ) ;
#18486=DIRECTION ( 'NONE',  ( -1.000000000000000000, 0.000000000000000000, -0.000000000000000000 ) ) ;
#18487=DIRECTION ( 'NONE',  ( 0.000000000000000000, -0.9945218953682721796, -0.1045284632676636571 ) ) ;
#18491=AXIS2_PLACEMENT_3D ( 'NONE', #1064, #19507, #17863 ) ;
#18495=LINE ( 'NONE', #15272, #12337 ) ;
#18503=VERTEX_POINT ( 'NONE', #18929 ) ;
#18511=CARTESIAN_POINT ( 'NONE',  ( 10.00000000000000000, 18.31866948046803145, -26.23788002993704893 ) ) ;
#18515=DIRECTION ( 'NONE',  ( -1.000000000000000000, -0.000000000000000000, -0.000000000000000000 ) ) ;
#18518=ADVANCED_FACE ( 'NONE', ( #5234 ), #5124, .T. ) ;
#18520=AXIS2_PLACEMENT_3D ( 'NONE', #4666, #16043, #11188 ) ;
#18527=CIRCLE ( 'NONE', #14634, 32.00000000000000000 ) ;
#18529=DIRECTION ( 'NONE',  ( 0.000000000000000000, 0.9510565162951521989, 0.3090169943749513926 ) ) ;
#18530=ORIENTED_EDGE ( 'NONE', *, *, #5159, .T. ) ;
#18533=EDGE_CURVE ( 'NONE', #4965, #16206, #19001, .T. ) ;
#18537=ORIENTED_EDGE ( 'NONE', *, *, #14633, .T. ) ;
#18548=CIRCLE ( 'NONE', #9341, 11.99999999999999822 ) ;
#18550=AXIS2_PLACEMENT_3D ( 'NONE', #11541, #2915, #11652 ) ;
#18551=VECTOR ( 'NONE', #4373, 1000.000000000000000 ) ;
#18554=FACE_OUTER_BOUND ( 'NONE', #10628, .T. ) ;
#18556=EDGE_CURVE ( 'NONE', #17402, #1592, #14033, .T. ) ;
#18560=AXIS2_PLACEMENT_3D ( 'NONE', #21703, #16729, #5022 ) ;
#18566=ADVANCED_FACE ( 'NONE', ( #11858 ), #10200, .T. ) ;
#18587=ORIENTED_EDGE ( 'NONE', *, *, #9895, .T. ) ;
#18597=CYLINDRICAL_SURFACE ( 'NONE', #4527, 32.00000000000000000 ) ;
#18599=FACE_OUTER_BOUND ( 'NONE', #1658, .T. ) ;
#18601=DIRECTION ( 'NONE',  ( -1.000000000000000000, -0.000000000000000000, 0.000000000000000000 ) ) ;
#18603=AXIS2_PLACEMENT_3D ( 'NONE', #18253, #18463, #4760 ) ;
#18611=ORIENTED_EDGE ( 'NONE', *, *, #20801, .F. ) ;
#18615=ORIENTED_EDGE ( 'NONE', *, *, #11895, .T. ) ;
#18620=ORIENTED_EDGE ( 'NONE', *, *, #16764, .F. ) ;
#18621=AXIS2_PLACEMENT_3D ( 'NONE', #2524, #7729, #17350 ) ;
#18622=DIRECTION ( 'NONE',  ( -1.000000000000000000, 0.000000000000000000, 0.000000000000000000 ) ) ;
#18626=CARTESIAN_POINT ( 'NONE',  ( 10.00000000000000000, -27.48365448817207479, 0.9185515634840949462 ) ) ;
#18633=PLANE ( 'NONE',  #10438 ) ;
#18637=AXIS2_PLACEMENT_3D ( 'NONE', #6041, #5817, #19501 ) ;
#18639=DIRECTION ( 'NONE',  ( 0.000000000000000000, 0.000000000000000000, -1.000000000000000000 ) ) ;
#18640=ADVANCED_FACE ( 'NONE', ( #4321 ), #692, .T. ) ;
#18642=CIRCLE ( 'NONE', #20041, 27.49900000000000233 ) ;
#18643=DIRECTION ( 'NONE',  ( 1.000000000000000000, -0.000000000000000000, -0.000000000000000000 ) ) ;
#18644=ORIENTED_EDGE ( 'NONE', *, *, #3089, .T. ) ;
#18646=ADVANCED_FACE ( 'NONE', ( #20902 ), #14058, .T. ) ;
#18662=CIRCLE ( 'NONE', #9112, 11.99999999999999822 ) ;
#18683=DIRECTION ( 'NONE',  ( -1.000000000000000000, 0.000000000000000000, -0.000000000000000000 ) ) ;
#18686=CARTESIAN_POINT ( 'NONE',  ( 0.000000000000000000, -21.98203405400967014, 17.64965094506536403 ) ) ;
#18688=CARTESIAN_POINT ( 'NONE',  ( 0.000000000000000000, 0.000000000000000000, 0.000000000000000000 ) ) ;
#18692=CIRCLE ( 'NONE', #2106, 12.00000000000000000 ) ;
#18697=EDGE_CURVE ( 'NONE', #20540, #6613, #21125, .T. ) ;
#18703=ORIENTED_EDGE ( 'NONE', *, *, #21592, .F. ) ;
#18706=ORIENTED_EDGE ( 'NONE', *, *, #13009, .T. ) ;
#18711=FACE_OUTER_BOUND ( 'NONE', #14336, .T. ) ;
#18724=ORIENTED_EDGE ( 'NONE', *, *, #17010, .T. ) ;
#18725=EDGE_LOOP ( 'NONE', ( #10793, #15154, #20514, #7625 ) ) ;
#18726=FACE_OUTER_BOUND ( 'NONE', #5907, .T. ) ;
#18732=CARTESIAN_POINT ( 'NONE',  ( 0.000000000000000000, 9.366510754379232750, 25.85466064925429208 ) ) ;
#18733=AXIS2_PLACEMENT_3D ( 'NONE', #8152, #1183, #21190 ) ;
#18738=DIRECTION ( 'NONE',  ( 0.000000000000000000, 0.000000000000000000, 1.000000000000000000 ) ) ;
#18742=FACE_OUTER_BOUND ( 'NONE', #13689, .T. ) ;
#18743=VERTEX_POINT ( 'NONE', #19461 ) ;
#18744=CARTESIAN_POINT ( 'NONE',  ( 10.00000000000000000, -1.592605004252988898, 28.14575649959894221 ) ) ;
#18746=ORIENTED_EDGE ( 'NONE', *, *, #254, .T. ) ;
#18773=VERTEX_POINT ( 'NONE', #10258 ) ;
#18777=ORIENTED_EDGE ( 'NONE', *, *, #4464, .F. ) ;
#18779=DIRECTION ( 'NONE',  ( 1.000000000000000000, -0.000000000000000000, -0.000000000000000000 ) ) ;
#18786=CYLINDRICAL_SURFACE ( 'NONE', #18167, 32.00000000000000000 ) ;
#18800=EDGE_CURVE ( 'NONE', #13983, #9606, #12822, .T. ) ;
#18803=FACE_OUTER_BOUND ( 'NONE', #8174, .T. ) ;
#18814=EDGE_CURVE ( 'NONE', #12744, #5595, #17001, .T. ) ;
#18819=LINE ( 'NONE', #5558, #7069 ) ;
#18820=CIRCLE ( 'NONE', #9269, 11.99999999999999822 ) ;
#18827=CYLINDRICAL_SURFACE ( 'NONE', #13153, 27.49900000000000233 ) ;
#18830=EDGE_CURVE ( 'NONE', #1433, #1041, #4897, .T. ) ;
#18832=CYLINDRICAL_SURFACE ( 'NONE', #21257, 12.00000000000000000 ) ;
#18834=EDGE_CURVE ( 'NONE', #18743, #9215, #17249, .T. ) ;
#18838=DIRECTION ( 'NONE',  ( 1.000000000000000000, 0.000000000000000000, 0.000000000000000000 ) ) ;
#18841=LINE ( 'NONE', #10321, #12748 ) ;
#18842=AXIS2_PLACEMENT_3D ( 'NONE', #6836, #11907, #18866 ) ;
#18843=EDGE_LOOP ( 'NONE', ( #11979, #8990, #16858, #19640 ) ) ;
#18844=DIRECTION ( 'NONE',  ( -1.000000000000000000, 0.000000000000000000, -0.000000000000000000 ) ) ;
#18850=DIRECTION ( 'NONE',  ( -1.000000000000000000, 0.000000000000000000, 0.000000000000000000 ) ) ;
#18854=ORIENTED_EDGE ( 'NONE', *, *, #2464, .F. ) ;
#18855=ORIENTED_EDGE ( 'NONE', *, *, #21273, .F. ) ;
#18856=VERTEX_POINT ( 'NONE', #6080 ) ;
#18857=CYLINDRICAL_SURFACE ( 'NONE', #1538, 11.99999999999999822 ) ;
#18858=EDGE_LOOP ( 'NONE', ( #15068, #15226, #13900, #6362 ) ) ;
#18859=APPLICATION_CONTEXT ( 'automotive_design' ) ;
#18861=AXIS2_PLACEMENT_3D ( 'NONE', #9006, #12544, #15757 ) ;
#18866=DIRECTION ( 'NONE',  ( 0.000000000000000000, -0.7431448254773999063, 0.6691306063588519093 ) ) ;
#18869=FACE_OUTER_BOUND ( 'NONE', #5016, .T. ) ;
#18877=ORIENTED_EDGE ( 'NONE', *, *, #1373, .T. ) ;
#18883=ORIENTED_EDGE ( 'NONE', *, *, #14989, .T. ) ;
#18885=ORIENTED_EDGE ( 'NONE', *, *, #6637, .T. ) ;
#18888=CARTESIAN_POINT ( 'NONE',  ( 10.00000000000000000, -0.6021240089803571172, 31.99433460282944708 ) ) ;
#18893=VECTOR ( 'NONE', #1572, 1000.000000000000000 ) ;
#18903=ORIENTED_EDGE ( 'NONE', *, *, #9020, .F. ) ;
#18906=VERTEX_POINT ( 'NONE', #7070 ) ;
#18908=CARTESIAN_POINT ( 'NONE',  ( 10.00000000000000000, 27.26034713664097353, -7.182859710736244629 ) ) ;
#18914=CYLINDRICAL_SURFACE ( 'NONE', #6298, 32.00000000000000000 ) ;
#18915=EDGE_CURVE ( 'NONE', #20854, #6613, #6316, .T. ) ;
#18923=CARTESIAN_POINT ( 'NONE',  ( 10.00000000000000000, 0.000000000000000000, 0.000000000000000000 ) ) ;
#18926=AXIS2_PLACEMENT_3D ( 'NONE', #11345, #6616, #21411 ) ;
#18928=EDGE_CURVE ( 'NONE', #9285, #12792, #17944, .T. ) ;
#18929=CARTESIAN_POINT ( 'NONE',  ( 10.00000000000000000, -17.70753755129051754, 21.03896658273966480 ) ) ;
#18934=CARTESIAN_POINT ( 'NONE',  ( 10.00000000000000000, -23.57863763525731216, 15.45211464167656601 ) ) ;
#18937=CARTESIAN_POINT ( 'NONE',  ( -10.00000000000000000, 0.000000000000000000, 0.000000000000000000 ) ) ;
#18939=ORIENTED_EDGE ( 'NONE', *, *, #13560, .F. ) ;
#18941=DIRECTION ( 'NONE',  ( 1.000000000000000000, 0.000000000000000000, -0.000000000000000000 ) ) ;
#18947=CARTESIAN_POINT ( 'NONE',  ( 10.00000000000000000, -0.6021240089799252404, -31.99433460282945063 ) ) ;
#18955=CARTESIAN_POINT ( 'NONE',  ( 10.00000000000000000, -1.592605004252595213, -28.14575649959895998 ) ) ;
#18967=ADVANCED_FACE ( 'NONE', ( #19196 ), #13686, .T. ) ;
#18968=VERTEX_POINT ( 'NONE', #12353 ) ;
#18969=AXIS2_PLACEMENT_3D ( 'NONE', #9781, #4826, #11778 ) ;
#18970=ORIENTED_EDGE ( 'NONE', *, *, #3556, .T. ) ;
#18973=VERTEX_POINT ( 'NONE', #13894 ) ;
#18977=CYLINDRICAL_SURFACE ( 'NONE', #20259, 32.00000000000000000 ) ;
#18981=LINE ( 'NONE', #15765, #10573 ) ;
#18984=CIRCLE ( 'NONE', #8040, 12.00000000000000000 ) ;
#18987=CARTESIAN_POINT ( 'NONE',  ( 0.000000000000000000, -28.15804365424196121, -1.358152127006266197 ) ) ;
#18993=AXIS2_PLACEMENT_3D ( 'NONE', #13493, #3454, #15369 ) ;
#18995=ORIENTED_EDGE ( 'NONE', *, *, #14454, .T. ) ;
#19001=CIRCLE ( 'NONE', #2396, 11.99999999999999822 ) ;
#19004=DIRECTION ( 'NONE',  ( -1.000000000000000000, 0.000000000000000000, 0.000000000000000000 ) ) ;
#19007=CARTESIAN_POINT ( 'NONE',  ( 10.00000000000000000, -27.82509854686807671, -4.525913221811426190 ) ) ;
#19008=CARTESIAN_POINT ( 'NONE',  ( 10.00000000000000000, 4.294029059350239486, -27.86182539015961979 ) ) ;
#19012=DIRECTION ( 'NONE',  ( 0.000000000000000000, 0.000000000000000000, 1.000000000000000000 ) ) ;
#19018=EDGE_CURVE ( 'NONE', #17245, #9780, #12447, .T. ) ;
#19020=CARTESIAN_POINT ( 'NONE',  ( 0.000000000000000000, -25.17124263951000529, -12.69364185792245081 ) ) ;
#19022=VERTEX_POINT ( 'NONE', #10794 ) ;
#19031=CIRCLE ( 'NONE', #13031, 32.00000000000000000 ) ;
#19033=DIRECTION ( 'NONE',  ( -1.000000000000000000, 0.000000000000000000, 0.000000000000000000 ) ) ;
#19034=CARTESIAN_POINT ( 'NONE',  ( 10.00000000000000888, 0.000000000000000000, 0.000000000000000000 ) ) ;
#19039=VECTOR ( 'NONE', #11077, 1000.000000000000000 ) ;
#19045=ADVANCED_FACE ( 'NONE', ( #747 ), #14218, .T. ) ;
#19052=CARTESIAN_POINT ( 'NONE',  ( 10.00000000000000000, 28.15804365424197186, -1.358152127006073684 ) ) ;
#19059=EDGE_CURVE ( 'NONE', #9606, #14519, #18315, .T. ) ;
#19060=EDGE_CURVE ( 'NONE', #8420, #21583, #8788, .T. ) ;
#19061=ORIENTED_EDGE ( 'NONE', *, *, #9202, .T. ) ;
#19066=ORIENTED_EDGE ( 'NONE', *, *, #944, .T. ) ;
#19077=EDGE_LOOP ( 'NONE', ( #18855, #11365, #8693, #17884 ) ) ;
#19087=DIRECTION ( 'NONE',  ( -1.000000000000000000, -0.000000000000000000, 0.000000000000000000 ) ) ;
#19095=CARTESIAN_POINT ( 'NONE',  ( 5.000000000000000000, 31.88200538760793634, 2.745493118647104325 ) ) ;
#19097=EDGE_LOOP ( 'NONE', ( #126, #18316, #16518, #391 ) ) ;
#19106=DIRECTION ( 'NONE',  ( 0.000000000000000000, -0.5877852522924797984, 0.8090169943749425663 ) ) ;
#19116=ORIENTED_EDGE ( 'NONE', *, *, #9566, .T. ) ;
#19118=CARTESIAN_POINT ( 'NONE',  ( 0.000000000000000000, -27.26034713664092379, 4.817140289263571518 ) ) ;
#19122=CARTESIAN_POINT ( 'NONE',  ( 5.000000000000000000, 23.37352460145313771, -21.85585385440855788 ) ) ;
#19123=ORIENTED_EDGE ( 'NONE', *, *, #6788, .F. ) ;
#19125=DIRECTION ( 'NONE',  ( 0.000000000000000000, 0.000000000000000000, 1.000000000000000000 ) ) ;
#19131=DIRECTION ( 'NONE',  ( -1.000000000000000000, -0.000000000000000000, -0.000000000000000000 ) ) ;
#19132=VECTOR ( 'NONE', #7747, 1000.000000000000000 ) ;
#19140=DIRECTION ( 'NONE',  ( -1.000000000000000000, -0.000000000000000000, 0.000000000000000000 ) ) ;
#19143=AXIS2_PLACEMENT_3D ( 'NONE', #20340, #16678, #5201 ) ;
#19157=CARTESIAN_POINT ( 'NONE',  ( 10.00000000000000000, -27.07404830566974141, 4.815694066514342175 ) ) ;
#19166=DIRECTION ( 'NONE',  ( 0.000000000000000000, 0.000000000000000000, 1.000000000000000000 ) ) ;
#19167=ORIENTED_EDGE ( 'NONE', *, *, #12715, .T. ) ;
#19181=CARTESIAN_POINT ( 'NONE',  ( 10.00000000000000000, 0.000000000000000000, 0.000000000000000000 ) ) ;
#19190=ADVANCED_FACE ( 'NONE', ( #1731 ), #6723, .T. ) ;
#19196=FACE_OUTER_BOUND ( 'NONE', #5323, .T. ) ;
#19202=VECTOR ( 'NONE', #14611, 1000.000000000000000 ) ;
#19208=CARTESIAN_POINT ( 'NONE',  ( 0.000000000000000000, -26.27606311335944511, -10.21217444509438188 ) ) ;
#19210=CARTESIAN_POINT ( 'NONE',  ( -140.0000507999999968, 4.000000000000000000, 1.000000000000000000 ) ) ;
#19216=EDGE_CURVE ( 'NONE', #6772, #3550, #2799, .T. ) ;
#19218=EDGE_LOOP ( 'NONE', ( #16586, #14393, #20879, #11901 ) ) ;
#19219=EDGE_CURVE ( 'NONE', #20854, #15579, #17959, .T. ) ;
#19222=ORIENTED_EDGE ( 'NONE', *, *, #21727, .F. ) ;
#19223=ORIENTED_EDGE ( 'NONE', *, *, #17759, .F. ) ;
#19225=EDGE_CURVE ( 'NONE', #8085, #11265, #2429, .T. ) ;
#19227=AXIS2_PLACEMENT_3D ( 'NONE', #16330, #12786, #5856 ) ;
#19230=CIRCLE ( 'NONE', #8997, 12.00000000000000000 ) ;
#19232=AXIS2_PLACEMENT_3D ( 'NONE', #8105, #19808, #9407 ) ;
#19234=ORIENTED_EDGE ( 'NONE', *, *, #21635, .T. ) ;
#19240=LINE ( 'NONE', #5880, #12583 ) ;
#19250=CARTESIAN_POINT ( 'NONE',  ( 10.00000000000000000, 0.000000000000000000, 0.000000000000000000 ) ) ;
#19256=ORIENTED_EDGE ( 'NONE', *, *, #8776, .T. ) ;
#19263=CIRCLE ( 'NONE', #563, 11.99999999999999645 ) ;
#19269=CARTESIAN_POINT ( 'NONE',  ( 0.000000000000000000, -6.063030049134865429, -31.42037024962131397 ) ) ;
#19272=LINE ( 'NONE', #10436, #11144 ) ;
#19274=ORIENTED_EDGE ( 'NONE', *, *, #14760, .F. ) ;
#19275=AXIS2_PLACEMENT_3D ( 'NONE', #20230, #116, #14922 ) ;
#19279=CARTESIAN_POINT ( 'NONE',  ( -140.0000507999999968, 0.000000000000000000, 0.000000000000000000 ) ) ;
#19281=VERTEX_POINT ( 'NONE', #11570 ) ;
#19286=ORIENTED_EDGE ( 'NONE', *, *, #5833, .T. ) ;
#19290=AXIS2_PLACEMENT_3D ( 'NONE', #3368, #21503, #15185 ) ;
#19303=DIRECTION ( 'NONE',  ( -1.000000000000000000, 0.000000000000000000, 0.000000000000000000 ) ) ;
#19305=DIRECTION ( 'NONE',  ( 0.000000000000000000, -0.9510565162951565288, 0.3090169943749382919 ) ) ;
#19310=VERTEX_POINT ( 'NONE', #16749 ) ;
#19315=CARTESIAN_POINT ( 'NONE',  ( 5.000000000000000888, 31.75612719289746266, -3.943144139962234451 ) ) ;
#19317=FACE_OUTER_BOUND ( 'NONE', #830, .T. ) ;
#19324=DIRECTION ( 'NONE',  ( 0.000000000000000000, 0.000000000000000000, 1.000000000000000000 ) ) ;
#19331=VERTEX_POINT ( 'NONE', #13655 ) ;
#19333=ORIENTED_EDGE ( 'NONE', *, *, #4056, .T. ) ;
#19348=DIRECTION ( 'NONE',  ( -1.000000000000000000, 0.000000000000000000, -0.000000000000000000 ) ) ;
#19350=FACE_OUTER_BOUND ( 'NONE', #3199, .T. ) ;
#19351=LINE ( 'NONE', #14376, #4832 ) ;
#19362=ORIENTED_EDGE ( 'NONE', *, *, #2208, .T. ) ;
#19363=CARTESIAN_POINT ( 'NONE',  ( 0.000000000000000000, -28.15804365424197897, 1.358152127005888055 ) ) ;
#19368=DIRECTION ( 'NONE',  ( -1.000000000000000000, 0.000000000000000000, 0.000000000000000000 ) ) ;
#19372=CARTESIAN_POINT ( 'NONE',  ( 0.000000000000000000, 19.85071254963803611, -20.01672328094512565 ) ) ;
#19373=AXIS2_PLACEMENT_3D ( 'NONE', #17434, #14331, #19305 ) ;
#19374=VECTOR ( 'NONE', #3189, 1000.000000000000000 ) ;
#19399=DIRECTION ( 'NONE',  ( 0.000000000000000000, 0.000000000000000000, 1.000000000000000000 ) ) ;
#19400=VERTEX_POINT ( 'NONE', #16977 ) ;
#19403=CARTESIAN_POINT ( 'NONE',  ( 10.00000000000000000, 0.000000000000000000, 0.000000000000000000 ) ) ;
#19409=CARTESIAN_POINT ( 'NONE',  ( 10.00000000000000000, 30.24235385705252099, -10.45944707835077381 ) ) ;
#19412=VERTEX_POINT ( 'NONE', #7134 ) ;
#19418=VERTEX_POINT ( 'NONE', #7038 ) ;
#19426=LINE ( 'NONE', #21602, #819 ) ;
#19429=CIRCLE ( 'NONE', #6396, 12.00000000000000178 ) ;
#19430=ADVANCED_FACE ( 'NONE', ( #1835 ), #10447, .T. ) ;
#19431=CARTESIAN_POINT ( 'NONE',  ( 10.00000000000000000, 15.25521607131206459, 23.70650506194175478 ) ) ;
#19434=EDGE_CURVE ( 'NONE', #10449, #20563, #2447, .T. ) ;
#19435=ORIENTED_EDGE ( 'NONE', *, *, #20681, .F. ) ;
#19439=( GEOMETRIC_REPRESENTATION_CONTEXT ( 3 ) GLOBAL_UNCERTAINTY_ASSIGNED_CONTEXT ( ( #9893 ) ) GLOBAL_UNIT_ASSIGNED_CONTEXT ( ( #8797, #5807, #6144 ) ) REPRESENTATION_CONTEXT ( 'NONE', 'WORKASPACE' ) );
#19440=ORIENTED_EDGE ( 'NONE', *, *, #12813, .F. ) ;
#19446=ADVANCED_FACE ( 'NONE', ( #15748 ), #14093, .T. ) ;
#19448=LINE ( 'NONE', #4426, #19132 ) ;
#19452=CARTESIAN_POINT ( 'NONE',  ( 10.00000000000000000, -3.786343810537759147, 27.23708136986050832 ) ) ;
#19455=CARTESIAN_POINT ( 'NONE',  ( 10.00000000000000000, 0.000000000000000000, 0.000000000000000000 ) ) ;
#19458=CARTESIAN_POINT ( 'NONE',  ( 10.00000000000000000, 12.46320060045762013, -29.47318494484016327 ) ) ;
#19461=CARTESIAN_POINT ( 'NONE',  ( 0.000000000000000000, -24.73395913766455578, -12.01774797440602427 ) ) ;
#19472=CARTESIAN_POINT ( 'NONE',  ( 0.000000000000000000, 25.48117629651189375, 10.33947075754270095 ) ) ;
#19475=ADVANCED_FACE ( 'NONE', ( #16284 ), #14631, .T. ) ;
#19495=ADVANCED_FACE ( 'NONE', ( #723 ), #4358, .T. ) ;
#19501=DIRECTION ( 'NONE',  ( 0.000000000000000000, 0.9945218953682729568, 0.1045284632676570791 ) ) ;
#19502=CIRCLE ( 'NONE', #11375, 3.000000000000000444 ) ;
#19503=EDGE_LOOP ( 'NONE', ( #17356, #5004, #15989, #377 ) ) ;
#19504=CARTESIAN_POINT ( 'NONE',  ( 0.000000000000000000, -19.07277123396555041, 19.80970465344741882 ) ) ;
#19505=DIRECTION ( 'NONE',  ( -1.000000000000000000, 0.000000000000000000, -0.000000000000000000 ) ) ;
#19507=DIRECTION ( 'NONE',  ( -1.000000000000000000, -0.000000000000000000, -0.000000000000000000 ) ) ;
#19511=CARTESIAN_POINT ( 'NONE',  ( 0.000000000000000000, -7.619321854369744074, 26.42235673590688094 ) ) ;
#19512=CIRCLE ( 'NONE', #17045, 11.99999999999999822 ) ;
#19517=DIRECTION ( 'NONE',  ( 0.000000000000000000, 0.000000000000000000, -1.000000000000000000 ) ) ;
#19518=ORIENTED_EDGE ( 'NONE', *, *, #588, .T. ) ;
#19523=ORIENTED_EDGE ( 'NONE', *, *, #17662, .T. ) ;
#19528=AXIS2_PLACEMENT_3D ( 'NONE', #3049, #2931, #9891 ) ;
#19530=DIRECTION ( 'NONE',  ( 0.000000000000000000, 0.000000000000000000, 1.000000000000000000 ) ) ;
#19532=AXIS2_PLACEMENT_3D ( 'NONE', #13443, #8802, #402 ) ;
#19540=AXIS2_PLACEMENT_3D ( 'NONE', #16945, #6782, #1691 ) ;
#19553=DIRECTION ( 'NONE',  ( -1.000000000000000000, -0.000000000000000000, 0.000000000000000000 ) ) ;
#19555=AXIS2_PLACEMENT_3D ( 'NONE', #5057, #2069, #3399 ) ;
#19556=CARTESIAN_POINT ( 'NONE',  ( 0.000000000000000000, -14.53731623274912366, -23.34226719384920656 ) ) ;
#19559=CIRCLE ( 'NONE', #5108, 11.99999999999999822 ) ;
#19568=ADVANCED_FACE ( 'NONE', ( #9317 ), #12859, .T. ) ;
#19572=CARTESIAN_POINT ( 'NONE',  ( 5.000000000000000888, -7.240962358591787940, 31.16999300804312156 ) ) ;
#19573=AXIS2_PLACEMENT_3D ( 'NONE', #4129, #17619, #15941 ) ;
#19584=ORIENTED_EDGE ( 'NONE', *, *, #7582, .F. ) ;
#19585=VERTEX_POINT ( 'NONE', #17636 ) ;
#19590=DIRECTION ( 'NONE',  ( 0.000000000000000000, 0.000000000000000000, 1.000000000000000000 ) ) ;
#19592=AXIS2_PLACEMENT_3D ( 'NONE', #17429, #15766, #12664 ) ;
#19604=ORIENTED_EDGE ( 'NONE', *, *, #12063, .F. ) ;
#19608=CIRCLE ( 'NONE', #1269, 32.00000000000000000 ) ;
#19615=ORIENTED_EDGE ( 'NONE', *, *, #3520, .T. ) ;
#19620=FACE_OUTER_BOUND ( 'NONE', #7860, .T. ) ;
#19624=DIRECTION ( 'NONE',  ( -1.000000000000000000, 0.000000000000000000, 0.000000000000000000 ) ) ;
#19628=ORIENTED_EDGE ( 'NONE', *, *, #7582, .T. ) ;
#19630=EDGE_CURVE ( 'NONE', #2742, #5097, #5498, .T. ) ;
#19635=CARTESIAN_POINT ( 'NONE',  ( 0.000000000000000000, -1.959304526717615902, -27.42911093658677402 ) ) ;
#19637=EDGE_CURVE ( 'NONE', #15746, #20991, #5851, .T. ) ;
#19640=ORIENTED_EDGE ( 'NONE', *, *, #3110, .T. ) ;
#19642=ORIENTED_EDGE ( 'NONE', *, *, #10180, .F. ) ;
#19646=AXIS2_PLACEMENT_3D ( 'NONE', #14047, #14487, #16021 ) ;
#19648=CARTESIAN_POINT ( 'NONE',  ( 10.00000000000000000, 0.000000000000000000, 0.000000000000000000 ) ) ;
#19649=LINE ( 'NONE', #21531, #13219 ) ;
#19650=CARTESIAN_POINT ( 'NONE',  ( 10.00000000000000000, 0.000000000000000000, 0.000000000000000000 ) ) ;
#19652=FACE_OUTER_BOUND ( 'NONE', #8147, .T. ) ;
#19660=ORIENTED_EDGE ( 'NONE', *, *, #5342, .T. ) ;
#19661=ORIENTED_EDGE ( 'NONE', *, *, #6425, .F. ) ;
#19674=CARTESIAN_POINT ( 'NONE',  ( 0.000000000000000000, 0.000000000000000000, 0.000000000000000000 ) ) ;
#19689=ORIENTED_EDGE ( 'NONE', *, *, #9488, .F. ) ;
#19694=VERTEX_POINT ( 'NONE', #1588 ) ;
#19699=CARTESIAN_POINT ( 'NONE',  ( 10.00000000000000000, -7.240962358591358061, -31.16999300804321749 ) ) ;
#19700=DIRECTION ( 'NONE',  ( 0.000000000000000000, 0.7431448254773910245, 0.6691306063588617903 ) ) ;
#19701=EDGE_CURVE ( 'NONE', #9457, #18200, #3242, .T. ) ;
#19704=AXIS2_PLACEMENT_3D ( 'NONE', #4661, #16264, #1126 ) ;
#19705=FACE_OUTER_BOUND ( 'NONE', #959, .T. ) ;
#19706=AXIS2_PLACEMENT_3D ( 'NONE', #7642, #5768, #15923 ) ;
#19712=CARTESIAN_POINT ( 'NONE',  ( 10.00000000000000000, -6.063030049135288202, 31.42037024962122871 ) ) ;
#19715=DIRECTION ( 'NONE',  ( 0.000000000000000000, -0.4067366430757888285, -0.9135454576426059736 ) ) ;
#19722=ORIENTED_EDGE ( 'NONE', *, *, #2867, .F. ) ;
#19724=FACE_OUTER_BOUND ( 'NONE', #15084, .T. ) ;
#19729=CARTESIAN_POINT ( 'NONE',  ( 0.000000000000000000, 0.000000000000000000, 0.000000000000000000 ) ) ;
#19734=DIRECTION ( 'NONE',  ( 1.000000000000000000, 0.000000000000000000, 0.000000000000000000 ) ) ;
#19735=AXIS2_PLACEMENT_3D ( 'NONE', #10014, #1632, #21530 ) ;
#19737=AXIS2_PLACEMENT_3D ( 'NONE', #9423, #20935, #12749 ) ;
#19741=DIRECTION ( 'NONE',  ( 0.000000000000000000, -0.2079116908177664202, 0.9781476007338040235 ) ) ;
#19745=CARTESIAN_POINT ( 'NONE',  ( -10.00000000000000000, 0.000000000000000000, 0.000000000000000000 ) ) ;
#19747=EDGE_LOOP ( 'NONE', ( #9049, #19642 ) ) ;
#19753=VECTOR ( 'NONE', #7777, 1000.000000000000000 ) ;
#19758=EDGE_CURVE ( 'NONE', #4982, #17286, #11832, .T. ) ;
#19762=CARTESIAN_POINT ( 'NONE',  ( -10.00000000000000000, 0.000000000000000000, 0.000000000000000000 ) ) ;
#19763=DIRECTION ( 'NONE',  ( 0.000000000000000000, -0.7431448254773862505, -0.6691306063588668973 ) ) ;
#19765=FACE_OUTER_BOUND ( 'NONE', #16309, .T. ) ;
#19772=ORIENTED_EDGE ( 'NONE', *, *, #14887, .F. ) ;
#19779=EDGE_LOOP ( 'NONE', ( #17194, #7950, #5132, #15561 ) ) ;
#19784=DIRECTION ( 'NONE',  ( -1.000000000000000000, 0.000000000000000000, -0.000000000000000000 ) ) ;
#19786=DIRECTION ( 'NONE',  ( -1.000000000000000000, 0.000000000000000000, 0.000000000000000000 ) ) ;
#19795=ORIENTED_EDGE ( 'NONE', *, *, #6042, .F. ) ;
#19808=DIRECTION ( 'NONE',  ( -1.000000000000000000, 0.000000000000000000, 0.000000000000000000 ) ) ;
#19810=CARTESIAN_POINT ( 'NONE',  ( 0.000000000000000000, 30.61448696004464409, -9.314139153633924195 ) ) ;
#19821=ORIENTED_EDGE ( 'NONE', *, *, #3334, .F. ) ;
#19828=ORIENTED_EDGE ( 'NONE', *, *, #14309, .F. ) ;
#19830=FACE_OUTER_BOUND ( 'NONE', #12647, .T. ) ;
#19831=CARTESIAN_POINT ( 'NONE',  ( 5.000000000000000000, -23.37352460145298139, 21.85585385440871775 ) ) ;
#19841=DIRECTION ( 'NONE',  ( -1.000000000000000000, -0.000000000000000000, -0.000000000000000000 ) ) ;
#19842=EDGE_LOOP ( 'NONE', ( #18040, #9847, #15726, #4143 ) ) ;
#19843=AXIS2_PLACEMENT_3D ( 'NONE', #18241, #18683, #20219 ) ;
#19846=EDGE_CURVE ( 'NONE', #14785, #17245, #16068, .T. ) ;
#19849=VERTEX_POINT ( 'NONE', #7114 ) ;
#19850=CIRCLE ( 'NONE', #15253, 27.49900000000000233 ) ;
#19852=EDGE_CURVE ( 'NONE', #19022, #13874, #8320, .T. ) ;
#19860=LINE ( 'NONE', #11905, #17013 ) ;
#19871=FACE_OUTER_BOUND ( 'NONE', #3791, .T. ) ;
#19873=ORIENTED_EDGE ( 'NONE', *, *, #2990, .F. ) ;
#19875=ORIENTED_EDGE ( 'NONE', *, *, #6387, .T. ) ;
#19881=ORIENTED_EDGE ( 'NONE', *, *, #19846, .F. ) ;
#19890=DIRECTION ( 'NONE',  ( -1.000000000000000000, -0.000000000000000000, 0.000000000000000000 ) ) ;
#19893=LINE ( 'NONE', #8297, #10470 ) ;
#19896=EDGE_CURVE ( 'NONE', #8175, #3440, #14500, .T. ) ;
#19902=ORIENTED_EDGE ( 'NONE', *, *, #21203, .T. ) ;
#19906=ORIENTED_EDGE ( 'NONE', *, *, #19018, .T. ) ;
#19909=ORIENTED_EDGE ( 'NONE', *, *, #8354, .F. ) ;
#19911=CIRCLE ( 'NONE', #18861, 32.00000000000000000 ) ;
#19926=VECTOR ( 'NONE', #2142, 1000.000000000000000 ) ;
#19928=CYLINDRICAL_SURFACE ( 'NONE', #20407, 32.00000000000000000 ) ;
#19935=ORIENTED_EDGE ( 'NONE', *, *, #939, .T. ) ;
#19940=DIRECTION ( 'NONE',  ( 0.000000000000000000, 0.9945218953682736229, -0.1045284632676503761 ) ) ;
#19945=DIRECTION ( 'NONE',  ( 0.000000000000000000, 0.000000000000000000, 1.000000000000000000 ) ) ;
#19950=DIRECTION ( 'NONE',  ( 0.000000000000000000, 0.000000000000000000, 1.000000000000000000 ) ) ;
#19956=ORIENTED_EDGE ( 'NONE', *, *, #5692, .F. ) ;
#19961=CYLINDRICAL_SURFACE ( 'NONE', #18969, 11.99999999999999645 ) ;
#19973=DIRECTION ( 'NONE',  ( 0.000000000000000000, 0.000000000000000000, 1.000000000000000000 ) ) ;
#19977=CARTESIAN_POINT ( 'NONE',  ( 10.00000000000000000, 0.000000000000000000, 0.000000000000000000 ) ) ;
#19985=DIRECTION ( 'NONE',  ( -1.000000000000000000, 0.000000000000000000, 0.000000000000000000 ) ) ;
#19990=AXIS2_PLACEMENT_3D ( 'NONE', #21559, #4983, #16806 ) ;
#19994=AXIS2_PLACEMENT_3D ( 'NONE', #6325, #8077, #14813 ) ;
#20007=CARTESIAN_POINT ( 'NONE',  ( 10.00000000000000000, 0.000000000000000000, 0.000000000000000000 ) ) ;
#20011=EDGE_CURVE ( 'NONE', #4316, #14805, #15110, .T. ) ;
#20019=ORIENTED_EDGE ( 'NONE', *, *, #9707, .T. ) ;
#20020=EDGE_CURVE ( 'NONE', #9215, #18973, #4185, .T. ) ;
#20028=CYLINDRICAL_SURFACE ( 'NONE', #16861, 11.99999999999999822 ) ;
#20031=DIRECTION ( 'NONE',  ( 0.000000000000000000, 0.9945218953682736229, -0.1045284632676503622 ) ) ;
#20035=CARTESIAN_POINT ( 'NONE',  ( 0.000000000000000000, -31.75612719289738095, -3.943144139962873940 ) ) ;
#20036=CARTESIAN_POINT ( 'NONE',  ( 5.000000000000000888, 6.063030049135073263, 31.42037024962127134 ) ) ;
#20041=AXIS2_PLACEMENT_3D ( 'NONE', #19181, #7579, #14315 ) ;
#20045=LINE ( 'NONE', #13296, #21526 ) ;
#20059=ORIENTED_EDGE ( 'NONE', *, *, #20748, .F. ) ;
#20061=CARTESIAN_POINT ( 'NONE',  ( 0.000000000000000000, -3.786343810537388332, -27.23708136986056161 ) ) ;
#20066=CYLINDRICAL_SURFACE ( 'NONE', #14849, 32.00000000000000000 ) ;
#20071=CARTESIAN_POINT ( 'NONE',  ( 10.00000000000000000, -25.48117629651196125, 10.33947075754252332 ) ) ;
#20073=ORIENTED_EDGE ( 'NONE', *, *, #20416, .F. ) ;
#20077=CIRCLE ( 'NONE', #10535, 27.49900000000000233 ) ;
#20084=CARTESIAN_POINT ( 'NONE',  ( 0.000000000000000000, 24.17932380791719282, 20.96092317127012805 ) ) ;
#20089=CARTESIAN_POINT ( 'NONE',  ( 10.00000000000000000, -13.56333590713994575, -28.98337314858448366 ) ) ;
#20101=DIRECTION ( 'NONE',  ( 0.000000000000000000, 0.000000000000000000, 1.000000000000000000 ) ) ;
#20103=DIRECTION ( 'NONE',  ( 0.000000000000000000, -0.2079116908177469081, -0.9781476007338082423 ) ) ;
#20104=AXIS2_PLACEMENT_3D ( 'NONE', #5279, #17092, #80 ) ;
#20113=EDGE_CURVE ( 'NONE', #10715, #19331, #9819, .T. ) ;
#20118=CARTESIAN_POINT ( 'NONE',  ( 10.00000000000000000, 0.000000000000000000, 0.000000000000000000 ) ) ;
#20121=DIRECTION ( 'NONE',  ( -1.000000000000000000, -0.000000000000000000, 0.000000000000000000 ) ) ;
#20123=CARTESIAN_POINT ( 'NONE',  ( 0.000000000000000000, -7.619321854369379032, -26.42235673590698397 ) ) ;
#20124=EDGE_CURVE ( 'NONE', #5926, #10821, #16170, .T. ) ;
#20145=CARTESIAN_POINT ( 'NONE',  ( 10.00000000000000000, 17.83210509884640871, 21.83428559348767806 ) ) ;
#20154=LINE ( 'NONE', #9970, #16936 ) ;
#20163=ORIENTED_EDGE ( 'NONE', *, *, #4056, .F. ) ;
#20168=LINE ( 'NONE', #5027, #11879 ) ;
#20170=DIRECTION ( 'NONE',  ( -1.000000000000000000, 0.000000000000000000, 0.000000000000000000 ) ) ;
#20183=EDGE_LOOP ( 'NONE', ( #8607, #14013, #16505, #11513 ) ) ;
#20184=DIRECTION ( 'NONE',  ( -1.000000000000000000, -0.000000000000000000, -0.000000000000000000 ) ) ;
#20187=DIRECTION ( 'NONE',  ( 0.000000000000000000, 0.000000000000000000, 1.000000000000000000 ) ) ;
#20198=CARTESIAN_POINT ( 'NONE',  ( 0.000000000000000000, -15.25521607131222268, 23.70650506194164464 ) ) ;
#20204=FACE_OUTER_BOUND ( 'NONE', #10124, .T. ) ;
#20212=CIRCLE ( 'NONE', #13861, 11.99999999999999822 ) ;
#20213=VERTEX_POINT ( 'NONE', #10182 ) ;
#20219=DIRECTION ( 'NONE',  ( 0.000000000000000000, 0.8660254037844398178, -0.4999999999999978351 ) ) ;
#20221=VECTOR ( 'NONE', #21632, 1000.000000000000000 ) ;
#20222=CARTESIAN_POINT ( 'NONE',  ( 10.00000000000000000, 23.57863763525741874, -15.45211464167639548 ) ) ;
#20223=DIRECTION ( 'NONE',  ( 0.000000000000000000, 0.000000000000000000, 1.000000000000000000 ) ) ;
#20225=DIRECTION ( 'NONE',  ( -1.000000000000000000, -0.000000000000000000, 0.000000000000000000 ) ) ;
#20226=LINE ( 'NONE', #15574, #16172 ) ;
#20228=EDGE_CURVE ( 'NONE', #10261, #8175, #18662, .T. ) ;
#20230=CARTESIAN_POINT ( 'NONE',  ( 0.000000000000000000, -27.26034713664101972, 7.182859710736059888 ) ) ;
#20235=CIRCLE ( 'NONE', #9262, 32.00000000000000000 ) ;
#20237=DIRECTION ( 'NONE',  ( 0.000000000000000000, 0.4067366430758008744, -0.9135454576426006446 ) ) ;
#20254=DIRECTION ( 'NONE',  ( 0.000000000000000000, 0.000000000000000000, 1.000000000000000000 ) ) ;
#20255=ADVANCED_FACE ( 'NONE', ( #11954 ), #24, .T. ) ;
#20259=AXIS2_PLACEMENT_3D ( 'NONE', #3835, #10574, #17321 ) ;
#20261=CIRCLE ( 'NONE', #10724, 11.99999999999999822 ) ;
#20263=ORIENTED_EDGE ( 'NONE', *, *, #12600, .F. ) ;
#20279=DIRECTION ( 'NONE',  ( 0.000000000000000000, 0.4067366430757946572, 0.9135454576426033091 ) ) ;
#20292=VERTEX_POINT ( 'NONE', #4966 ) ;
#20305=CARTESIAN_POINT ( 'NONE',  ( -10.00000000000000000, 0.000000000000000000, 0.000000000000000000 ) ) ;
#20308=EDGE_LOOP ( 'NONE', ( #158, #10335, #12175, #8154 ) ) ;
#20312=CARTESIAN_POINT ( 'NONE',  ( 10.00000000000000000, 0.000000000000000000, 0.000000000000000000 ) ) ;
#20317=CIRCLE ( 'NONE', #2303, 12.00000000000000000 ) ;
#20321=EDGE_CURVE ( 'NONE', #18240, #17767, #10256, .T. ) ;
#20334=ORIENTED_EDGE ( 'NONE', *, *, #11842, .T. ) ;
#20340=CARTESIAN_POINT ( 'NONE',  ( 10.00000000000000000, 0.000000000000000000, 0.000000000000000000 ) ) ;
#20342=CYLINDRICAL_SURFACE ( 'NONE', #15612, 27.49900000000000233 ) ;
#20343=FACE_OUTER_BOUND ( 'NONE', #17640, .T. ) ;
#20347=AXIS2_PLACEMENT_3D ( 'NONE', #3973, #10708, #8735 ) ;
#20351=ORIENTED_EDGE ( 'NONE', *, *, #10867, .T. ) ;
#20353=CARTESIAN_POINT ( 'NONE',  ( 0.000000000000000000, -23.57863763525731216, 15.45211464167656601 ) ) ;
#20354=ORIENTED_EDGE ( 'NONE', *, *, #2741, .T. ) ;
#20356=ORIENTED_EDGE ( 'NONE', *, *, #5553, .F. ) ;
#20358=EDGE_CURVE ( 'NONE', #5649, #1433, #7033, .T. ) ;
#20371=VERTEX_POINT ( 'NONE', #5506 ) ;
#20375=FACE_OUTER_BOUND ( 'NONE', #9491, .T. ) ;
#20376=DIRECTION ( 'NONE',  ( -1.000000000000000000, -0.000000000000000000, -0.000000000000000000 ) ) ;
#20377=ORIENTED_EDGE ( 'NONE', *, *, #5792, .F. ) ;
#20389=AXIS2_PLACEMENT_3D ( 'NONE', #5479, #17079, #7131 ) ;
#20393=VECTOR ( 'NONE', #922, 1000.000000000000000 ) ;
#20400=CARTESIAN_POINT ( 'NONE',  ( 10.00000000000000000, -1.592605004252988898, 28.14575649959894221 ) ) ;
#20403=ORIENTED_EDGE ( 'NONE', *, *, #16100, .T. ) ;
#20407=AXIS2_PLACEMENT_3D ( 'NONE', #18174, #1151, #11419 ) ;
#20410=ORIENTED_EDGE ( 'NONE', *, *, #4064, .T. ) ;
#20416=EDGE_CURVE ( 'NONE', #7792, #17973, #20637, .T. ) ;
#20419=CARTESIAN_POINT ( 'NONE',  ( 10.00000000000000000, -19.07277123396555041, 19.80970465344741882 ) ) ;
#20422=CARTESIAN_POINT ( 'NONE',  ( -10.00000000000000000, 0.000000000000000000, 0.000000000000000000 ) ) ;
#20425=CARTESIAN_POINT ( 'NONE',  ( 5.000000000000000000, -27.40684453873955562, -16.51862198942037097 ) ) ;
#20428=DIRECTION ( 'NONE',  ( -1.000000000000000000, 0.000000000000000000, -0.000000000000000000 ) ) ;
#20433=EDGE_CURVE ( 'NONE', #12821, #13720, #7487, .T. ) ;
#20450=DIRECTION ( 'NONE',  ( 1.000000000000000000, 0.000000000000000000, 0.000000000000000000 ) ) ;
#20454=CARTESIAN_POINT ( 'NONE',  ( 10.00000000000000000, -3.786343810537388332, -27.23708136986056161 ) ) ;
#20457=AXIS2_PLACEMENT_3D ( 'NONE', #1050, #7463, #14189 ) ;
#20458=AXIS2_PLACEMENT_3D ( 'NONE', #4144, #15529, #14092 ) ;
#20459=ORIENTED_EDGE ( 'NONE', *, *, #12389, .F. ) ;
#20460=EDGE_CURVE ( 'NONE', #3440, #5218, #1031, .T. ) ;
#20470=DIRECTION ( 'NONE',  ( -1.000000000000000000, -0.000000000000000000, -0.000000000000000000 ) ) ;
#20474=CARTESIAN_POINT ( 'NONE',  ( 0.000000000000000000, -17.70753755129023332, -21.03896658273990639 ) ) ;
#20475=CARTESIAN_POINT ( 'NONE',  ( -140.0000507999999968, 0.000000000000000000, -5.000000000000000000 ) ) ;
#20477=CARTESIAN_POINT ( 'NONE',  ( 0.000000000000000000, -0.6021240089803554518, 31.99433460282944708 ) ) ;
#20482=DIRECTION ( 'NONE',  ( -1.000000000000000000, -0.000000000000000000, 0.000000000000000000 ) ) ;
#20483=CARTESIAN_POINT ( 'NONE',  ( 0.000000000000000000, 0.000000000000000000, 0.000000000000000000 ) ) ;
#20486=ORIENTED_EDGE ( 'NONE', *, *, #20662, .T. ) ;
#20490=ORIENTED_EDGE ( 'NONE', *, *, #13532, .F. ) ;
#20494=DIRECTION ( 'NONE',  ( -1.000000000000000000, -0.000000000000000000, -0.000000000000000000 ) ) ;
#20497=AXIS2_PLACEMENT_3D ( 'NONE', #20353, #2001, #17358 ) ;
#20503=DIRECTION ( 'NONE',  ( -1.000000000000000000, -0.000000000000000000, 0.000000000000000000 ) ) ;
#20505=ORIENTED_EDGE ( 'NONE', *, *, #16100, .F. ) ;
#20511=EDGE_CURVE ( 'NONE', #569, #9022, #13373, .T. ) ;
#20512=CARTESIAN_POINT ( 'NONE',  ( 0.000000000000000000, 19.07277123396541185, 19.80970465344755027 ) ) ;
#20514=ORIENTED_EDGE ( 'NONE', *, *, #10020, .T. ) ;
#20520=DIRECTION ( 'NONE',  ( -1.000000000000000000, 0.000000000000000000, 0.000000000000000000 ) ) ;
#20539=DIRECTION ( 'NONE',  ( 1.000000000000000000, 0.000000000000000000, 0.000000000000000000 ) ) ;
#20540=VERTEX_POINT ( 'NONE', #12890 ) ;
#20544=EDGE_CURVE ( 'NONE', #5051, #16474, #5977, .T. ) ;
#20546=DIRECTION ( 'NONE',  ( 0.000000000000000000, -0.9945218953682722907, -0.1045284632676636849 ) ) ;
#20557=DIRECTION ( 'NONE',  ( 0.000000000000000000, 0.000000000000000000, 1.000000000000000000 ) ) ;
#20559=VERTEX_POINT ( 'NONE', #12669 ) ;
#20563=VERTEX_POINT ( 'NONE', #1298 ) ;
#20570=VECTOR ( 'NONE', #652, 1000.000000000000000 ) ;
#20583=LINE ( 'NONE', #20903, #15168 ) ;
#20585=EDGE_LOOP ( 'NONE', ( #8422, #6062, #15858, #3116 ) ) ;
#20611=DIRECTION ( 'NONE',  ( 0.000000000000000000, 0.000000000000000000, 1.000000000000000000 ) ) ;
#20614=ORIENTED_EDGE ( 'NONE', *, *, #5461, .T. ) ;
#20623=CYLINDRICAL_SURFACE ( 'NONE', #8644, 12.00000000000000000 ) ;
#20625=CIRCLE ( 'NONE', #18520, 11.99999999999999467 ) ;
#20627=CARTESIAN_POINT ( 'NONE',  ( 0.000000000000000000, 0.000000000000000000, 0.000000000000000000 ) ) ;
#20631=CARTESIAN_POINT ( 'NONE',  ( 0.000000000000000000, 21.69483248597444813, -16.89761061231758177 ) ) ;
#20632=AXIS2_PLACEMENT_3D ( 'NONE', #11476, #16565, #6629 ) ;
#20633=VECTOR ( 'NONE', #13008, 1000.000000000000000 ) ;
#20637=LINE ( 'NONE', #10584, #4548 ) ;
#20652=PRODUCT_DEFINITION_CONTEXT ( 'detailed design', #18859, 'design' ) ;
#20658=DIRECTION ( 'NONE',  ( 0.000000000000000000, 0.8660254037844398178, -0.4999999999999978351 ) ) ;
#20661=CARTESIAN_POINT ( 'NONE',  ( -10.00000000000000000, 0.000000000000000000, 0.000000000000000000 ) ) ;
#20662=EDGE_CURVE ( 'NONE', #11788, #15688, #8686, .T. ) ;
#20668=ADVANCED_FACE ( 'NONE', ( #15306 ), #13545, .T. ) ;
#20674=EDGE_CURVE ( 'NONE', #2294, #3283, #5995, .T. ) ;
#20679=CARTESIAN_POINT ( 'NONE',  ( 10.00000000000000000, 0.000000000000000000, 1.000000000000000000 ) ) ;
#20680=VECTOR ( 'NONE', #4903, 1000.000000000000000 ) ;
#20681=EDGE_CURVE ( 'NONE', #771, #13033, #13740, .T. ) ;
#20683=DIRECTION ( 'NONE',  ( -1.000000000000000000, -0.000000000000000000, -0.000000000000000000 ) ) ;
#20691=EDGE_CURVE ( 'NONE', #11544, #17790, #19031, .T. ) ;
#20693=DIRECTION ( 'NONE',  ( 0.000000000000000000, 0.000000000000000000, 1.000000000000000000 ) ) ;
#20701=ADVANCED_FACE ( 'NONE', ( #18322 ), #3172, .T. ) ;
#20704=ORIENTED_EDGE ( 'NONE', *, *, #6784, .F. ) ;
#20709=CARTESIAN_POINT ( 'NONE',  ( 0.000000000000000000, 0.000000000000000000, 0.000000000000000000 ) ) ;
#20710=DIRECTION ( 'NONE',  ( 0.000000000000000000, 0.2079116908177599532, -0.9781476007338055778 ) ) ;
#20711=CARTESIAN_POINT ( 'NONE',  ( 10.00000000000000000, 0.000000000000000000, 0.000000000000000000 ) ) ;
#20713=ADVANCED_FACE ( 'NONE', ( #15416 ), #15863, .T. ) ;
#20729=CIRCLE ( 'NONE', #3092, 11.99999999999999822 ) ;
#20735=EDGE_LOOP ( 'NONE', ( #2433, #12646, #6600, #16009 ) ) ;
#20737=CARTESIAN_POINT ( 'NONE',  ( 10.00000000000000000, 27.26034713664087406, 7.182859710736605230 ) ) ;
#20739=CARTESIAN_POINT ( 'NONE',  ( 10.00000000000000000, 27.07404830566971299, 4.815694066514526028 ) ) ;
#20742=ORIENTED_EDGE ( 'NONE', *, *, #15080, .F. ) ;
#20746=AXIS2_PLACEMENT_3D ( 'NONE', #17318, #20520, #5603 ) ;
#20748=EDGE_CURVE ( 'NONE', #16515, #11372, #5284, .T. ) ;
#20753=DIRECTION ( 'NONE',  ( 0.000000000000000000, 0.000000000000000000, 1.000000000000000000 ) ) ;
#20757=ORIENTED_EDGE ( 'NONE', *, *, #17741, .F. ) ;
#20758=LINE ( 'NONE', #7716, #9723 ) ;
#20761=LINE ( 'NONE', #14125, #1934 ) ;
#20762=CARTESIAN_POINT ( 'NONE',  ( -140.0000507999999968, 0.000000000000000000, 0.000000000000000000 ) ) ;
#20770=CYLINDRICAL_SURFACE ( 'NONE', #10843, 3.000000000000000444 ) ;
#20775=EDGE_CURVE ( 'NONE', #18856, #5686, #7754, .T. ) ;
#20783=ADVANCED_FACE ( 'NONE', ( #10877 ), #10762, .T. ) ;
#20784=DIRECTION ( 'NONE',  ( 0.000000000000000000, 0.000000000000000000, 1.000000000000000000 ) ) ;
#20787=CARTESIAN_POINT ( 'NONE',  ( 10.00000000000000000, -17.83210509884626660, -21.83428559348779530 ) ) ;
#20790=DIRECTION ( 'NONE',  ( -1.000000000000000000, 0.000000000000000000, 0.000000000000000000 ) ) ;
#20800=EDGE_CURVE ( 'NONE', #3621, #17553, #14087, .T. ) ;
#20801=EDGE_CURVE ( 'NONE', #3708, #10821, #2056, .T. ) ;
#20803=DIRECTION ( 'NONE',  ( 0.000000000000000000, 0.000000000000000000, 1.000000000000000000 ) ) ;
#20806=DIRECTION ( 'NONE',  ( 1.000000000000000000, 0.000000000000000000, 0.000000000000000000 ) ) ;
#20807=ORIENTED_EDGE ( 'NONE', *, *, #2382, .T. ) ;
#20813=ORIENTED_EDGE ( 'NONE', *, *, #14739, .F. ) ;
#20814=ORIENTED_EDGE ( 'NONE', *, *, #9452, .T. ) ;
#20825=ORIENTED_EDGE ( 'NONE', *, *, #16804, .T. ) ;
#20828=CARTESIAN_POINT ( 'NONE',  ( 10.00000000000000000, 0.000000000000000000, 0.000000000000000000 ) ) ;
#20829=ORIENTED_EDGE ( 'NONE', *, *, #4189, .F. ) ;
#20831=DIRECTION ( 'NONE',  ( 0.000000000000000000, 0.000000000000000000, -1.000000000000000000 ) ) ;
#20840=VERTEX_POINT ( 'NONE', #9211 ) ;
#20842=DIRECTION ( 'NONE',  ( -1.000000000000000000, 0.000000000000000000, 0.000000000000000000 ) ) ;
#20847=DIRECTION ( 'NONE',  ( -1.000000000000000000, -0.000000000000000000, 0.000000000000000000 ) ) ;
#20853=DIRECTION ( 'NONE',  ( -1.000000000000000000, 0.000000000000000000, 0.000000000000000000 ) ) ;
#20854=VERTEX_POINT ( 'NONE', #17845 ) ;
#20858=ORIENTED_EDGE ( 'NONE', *, *, #6093, .T. ) ;
#20859=ORIENTED_EDGE ( 'NONE', *, *, #6648, .F. ) ;
#20871=CARTESIAN_POINT ( 'NONE',  ( 10.00000000000000000, -26.69209308833512395, 6.612652082459228531 ) ) ;
#20879=ORIENTED_EDGE ( 'NONE', *, *, #15564, .T. ) ;
#20880=VERTEX_POINT ( 'NONE', #2699 ) ;
#20885=EDGE_LOOP ( 'NONE', ( #21771, #21166, #12746, #18150 ) ) ;
#20887=DIRECTION ( 'NONE',  ( 0.000000000000000000, 0.000000000000000000, 1.000000000000000000 ) ) ;
#20890=EDGE_CURVE ( 'NONE', #9457, #14635, #358, .T. ) ;
#20902=FACE_OUTER_BOUND ( 'NONE', #7900, .T. ) ;
#20903=CARTESIAN_POINT ( 'NONE',  ( 5.000000000000000888, -28.00896854772002342, 15.47571261340914539 ) ) ;
#20906=ORIENTED_EDGE ( 'NONE', *, *, #10825, .F. ) ;
#20908=AXIS2_PLACEMENT_3D ( 'NONE', #20118, #9826, #16911 ) ;
#20912=CARTESIAN_POINT ( 'NONE',  ( 10.00000000000000000, 0.000000000000000000, 0.000000000000000000 ) ) ;
#20922=CARTESIAN_POINT ( 'NONE',  ( 0.000000000000000000, -1.592605004252988898, 28.14575649959894221 ) ) ;
#20934=DIRECTION ( 'NONE',  ( 0.000000000000000000, 0.000000000000000000, 1.000000000000000000 ) ) ;
#20935=DIRECTION ( 'NONE',  ( -1.000000000000000000, 0.000000000000000000, 0.000000000000000000 ) ) ;
#20936=VERTEX_POINT ( 'NONE', #4798 ) ;
#20937=CIRCLE ( 'NONE', #21646, 11.99999999999999822 ) ;
#20943=CARTESIAN_POINT ( 'NONE',  ( 10.00000000000000000, -27.82509854686814066, 4.525913221811051379 ) ) ;
#20944=CARTESIAN_POINT ( 'NONE',  ( 10.00000000000000000, -27.40684453873954851, -16.51862198942037097 ) ) ;
#20947=EDGE_CURVE ( 'NONE', #8227, #10261, #20154, .T. ) ;
#20957=DIRECTION ( 'NONE',  ( 0.000000000000000000, 0.000000000000000000, 1.000000000000000000 ) ) ;
#20958=DIRECTION ( 'NONE',  ( 0.000000000000000000, 0.000000000000000000, 1.000000000000000000 ) ) ;
#20962=CARTESIAN_POINT ( 'NONE',  ( 5.000000000000000000, -19.29292659244022445, 25.53004080487755800 ) ) ;
#20965=EDGE_CURVE ( 'NONE', #19585, #8691, #20045, .T. ) ;
#20966=ORIENTED_EDGE ( 'NONE', *, *, #5024, .F. ) ;
#20972=EDGE_CURVE ( 'NONE', #5686, #11788, #1063, .T. ) ;
#20979=FACE_OUTER_BOUND ( 'NONE', #2724, .T. ) ;
#20982=VECTOR ( 'NONE', #5761, 1000.000000000000000 ) ;
#20991=VERTEX_POINT ( 'NONE', #11650 ) ;
#21006=DIRECTION ( 'NONE',  ( 0.000000000000000000, 0.000000000000000000, 1.000000000000000000 ) ) ;
#21011=CARTESIAN_POINT ( 'NONE',  ( 10.00000000000000000, 22.77465461094694632, -15.41136296218063428 ) ) ;
#21018=LINE ( 'NONE', #12498, #3541 ) ;
#21025=CIRCLE ( 'NONE', #13611, 32.00000000000000000 ) ;
#21028=VECTOR ( 'NONE', #6030, 1000.000000000000000 ) ;
#21029=EDGE_CURVE ( 'NONE', #9001, #17402, #18495, .T. ) ;
#21033=CARTESIAN_POINT ( 'NONE',  ( 10.00000000000000000, 0.000000000000000000, 0.000000000000000000 ) ) ;
#21040=DIRECTION ( 'NONE',  ( -1.000000000000000000, 0.000000000000000000, 0.000000000000000000 ) ) ;
#21048=DIRECTION ( 'NONE',  ( -1.000000000000000000, 0.000000000000000000, 0.000000000000000000 ) ) ;
#21068=FACE_OUTER_BOUND ( 'NONE', #3438, .T. ) ;
#21072=EDGE_CURVE ( 'NONE', #19400, #11293, #5301, .T. ) ;
#21074=ADVANCED_FACE ( 'NONE', ( #5775 ), #13839, .T. ) ;
#21075=AXIS2_PLACEMENT_3D ( 'NONE', #19745, #19841, #21517 ) ;
#21076=EDGE_CURVE ( 'NONE', #10985, #8423, #18819, .T. ) ;
#21081=EDGE_CURVE ( 'NONE', #3591, #3827, #21175, .T. ) ;
#21082=ORIENTED_EDGE ( 'NONE', *, *, #8529, .F. ) ;
#21089=LINE ( 'NONE', #9149, #8936 ) ;
#21091=CIRCLE ( 'NONE', #2035, 32.00000000000000000 ) ;
#21092=CYLINDRICAL_SURFACE ( 'NONE', #14227, 11.99999999999999822 ) ;
#21102=ORIENTED_EDGE ( 'NONE', *, *, #21665, .T. ) ;
#21105=VECTOR ( 'NONE', #16697, 1000.000000000000000 ) ;
#21106=VECTOR ( 'NONE', #4341, 1000.000000000000000 ) ;
#21112=ORIENTED_EDGE ( 'NONE', *, *, #5428, .T. ) ;
#21115=DIRECTION ( 'NONE',  ( 0.000000000000000000, 0.000000000000000000, 1.000000000000000000 ) ) ;
#21123=CARTESIAN_POINT ( 'NONE',  ( 10.00000000000000000, 12.90282758292980247, 25.06465718894781247 ) ) ;
#21125=CIRCLE ( 'NONE', #10529, 32.00000000000000000 ) ;
#21142=CIRCLE ( 'NONE', #2780, 32.00000000000000000 ) ;
#21146=CYLINDRICAL_SURFACE ( 'NONE', #15320, 32.00000000000000000 ) ;
#21156=LINE ( 'NONE', #15948, #20393 ) ;
#21159=CIRCLE ( 'NONE', #5990, 11.99999999999999822 ) ;
#21166=ORIENTED_EDGE ( 'NONE', *, *, #21373, .F. ) ;
#21169=CARTESIAN_POINT ( 'NONE',  ( 0.000000000000000000, 27.82509854686811224, 4.525913221811229903 ) ) ;
#21172=CARTESIAN_POINT ( 'NONE',  ( 10.00000000000000888, 2.828427124746190291, 1.000000000000000000 ) ) ;
#21175=CIRCLE ( 'NONE', #4581, 11.99999999999999822 ) ;
#21176=CARTESIAN_POINT ( 'NONE',  ( 10.00000000000000000, -9.366510754379051562, -25.85466064925435603 ) ) ;
#21178=EDGE_CURVE ( 'NONE', #428, #11955, #20583, .T. ) ;
#21179=ORIENTED_EDGE ( 'NONE', *, *, #19216, .T. ) ;
#21180=DIRECTION ( 'NONE',  ( -1.000000000000000000, -0.000000000000000000, -0.000000000000000000 ) ) ;
#21186=ORIENTED_EDGE ( 'NONE', *, *, #1496, .T. ) ;
#21187=AXIS2_PLACEMENT_3D ( 'NONE', #6666, #5098, #13382 ) ;
#21189=VERTEX_POINT ( 'NONE', #12391 ) ;
#21190=DIRECTION ( 'NONE',  ( 0.000000000000000000, 0.4067366430757946572, 0.9135454576426033091 ) ) ;
#21195=CARTESIAN_POINT ( 'NONE',  ( 0.000000000000000000, 28.15804365424197186, 10.64184787299392454 ) ) ;
#21200=CYLINDRICAL_SURFACE ( 'NONE', #10142, 11.99999999999999645 ) ;
#21203=EDGE_CURVE ( 'NONE', #2294, #1686, #12006, .T. ) ;
#21215=ORIENTED_EDGE ( 'NONE', *, *, #20662, .F. ) ;
#21218=VERTEX_POINT ( 'NONE', #15931 ) ;
#21220=CARTESIAN_POINT ( 'NONE',  ( 0.000000000000000000, 0.000000000000000000, 0.000000000000000000 ) ) ;
#21222=CARTESIAN_POINT ( 'NONE',  ( 0.000000000000000000, 18.31866948046766552, 26.23788002993730828 ) ) ;
#21227=CYLINDRICAL_SURFACE ( 'NONE', #7485, 32.00000000000000000 ) ;
#21228=DIRECTION ( 'NONE',  ( -1.000000000000000000, -0.000000000000000000, -0.000000000000000000 ) ) ;
#21232=DIRECTION ( 'NONE',  ( 0.000000000000000000, 0.000000000000000000, 1.000000000000000000 ) ) ;
#21233=VERTEX_POINT ( 'NONE', #14384 ) ;
#21236=DIRECTION ( 'NONE',  ( -1.000000000000000000, 0.000000000000000000, 0.000000000000000000 ) ) ;
#21237=ORIENTED_EDGE ( 'NONE', *, *, #3956, .T. ) ;
#21239=ORIENTED_EDGE ( 'NONE', *, *, #21076, .T. ) ;
#21254=CARTESIAN_POINT ( 'NONE',  ( 10.00000000000000000, -15.25521607131190294, -23.70650506194185425 ) ) ;
#21257=AXIS2_PLACEMENT_3D ( 'NONE', #11871, #13961, #5249 ) ;
#21272=EDGE_LOOP ( 'NONE', ( #1241, #9844, #10152, #18370 ) ) ;
#21273=EDGE_CURVE ( 'NONE', #11293, #11232, #21018, .T. ) ;
#21282=AXIS2_PLACEMENT_3D ( 'NONE', #15077, #11987, #10105 ) ;
#21284=CARTESIAN_POINT ( 'NONE',  ( 0.000000000000000000, 1.592605004253184964, -28.14575649959892445 ) ) ;
#21289=ORIENTED_EDGE ( 'NONE', *, *, #10282, .F. ) ;
#21297=LINE ( 'NONE', #19315, #4910 ) ;
#21300=DIRECTION ( 'NONE',  ( 0.000000000000000000, 0.000000000000000000, 1.000000000000000000 ) ) ;
#21304=CYLINDRICAL_SURFACE ( 'NONE', #17190, 27.49900000000000233 ) ;
#21305=DIRECTION ( 'NONE',  ( 0.000000000000000000, 0.000000000000000000, 1.000000000000000000 ) ) ;
#21309=CARTESIAN_POINT ( 'NONE',  ( 10.00000000000000000, 0.000000000000000000, 0.000000000000000000 ) ) ;
#21326=CIRCLE ( 'NONE', #12488, 12.00000000000000000 ) ;
#21327=DIRECTION ( 'NONE',  ( -1.000000000000000000, 0.000000000000000000, 0.000000000000000000 ) ) ;
#21332=ADVANCED_FACE ( 'NONE', ( #11178 ), #16034, .T. ) ;
#21335=AXIS2_PLACEMENT_3D ( 'NONE', #10942, #2537, #10616 ) ;
#21337=AXIS2_PLACEMENT_3D ( 'NONE', #21738, #8162, #6622 ) ;
#21341=EDGE_CURVE ( 'NONE', #1024, #18295, #16593, .T. ) ;
#21350=DIRECTION ( 'NONE',  ( 0.000000000000000000, 0.000000000000000000, 1.000000000000000000 ) ) ;
#21351=EDGE_CURVE ( 'NONE', #15753, #3387, #21777, .T. ) ;
#21354=CARTESIAN_POINT ( 'NONE',  ( 10.00000000000000000, -22.77465461094663368, -15.41136296218110147 ) ) ;
#21355=CARTESIAN_POINT ( 'NONE',  ( 10.00000000000000000, -17.70753755129023332, -21.03896658273990639 ) ) ;
#21367=CIRCLE ( 'NONE', #7254, 12.00000000000000178 ) ;
#21369=EDGE_CURVE ( 'NONE', #10630, #18906, #2478, .T. ) ;
#21373=EDGE_CURVE ( 'NONE', #18906, #20563, #23, .T. ) ;
#21381=VECTOR ( 'NONE', #21504, 1000.000000000000000 ) ;
#21390=DIRECTION ( 'NONE',  ( 0.000000000000000000, 0.000000000000000000, 1.000000000000000000 ) ) ;
#21394=CARTESIAN_POINT ( 'NONE',  ( 0.000000000000000000, 28.15804365424195765, 1.358152127006451826 ) ) ;
#21395=VERTEX_POINT ( 'NONE', #13156 ) ;
#21396=EDGE_CURVE ( 'NONE', #16625, #18856, #6338, .T. ) ;
#21407=CARTESIAN_POINT ( 'NONE',  ( 10.00000000000000000, -4.294029059349679045, -27.86182539015970505 ) ) ;
#21411=DIRECTION ( 'NONE',  ( 0.000000000000000000, 0.000000000000000000, 1.000000000000000000 ) ) ;
#21413=CYLINDRICAL_SURFACE ( 'NONE', #8098, 11.99999999999999822 ) ;
#21415=CARTESIAN_POINT ( 'NONE',  ( -10.00000000000000000, 0.000000000000000000, 0.000000000000000000 ) ) ;
#21420=DIRECTION ( 'NONE',  ( -1.000000000000000000, -0.000000000000000000, -0.000000000000000000 ) ) ;
#21425=CARTESIAN_POINT ( 'NONE',  ( 10.00000000000000000, 4.294029059349855793, 27.86182539015968018 ) ) ;
#21435=AXIS2_PLACEMENT_3D ( 'NONE', #20828, #4252, #5690 ) ;
#21452=AXIS2_PLACEMENT_3D ( 'NONE', #468, #13732, #20254 ) ;
#21463=EDGE_CURVE ( 'NONE', #16306, #4799, #5315, .T. ) ;
#21472=AXIS2_PLACEMENT_3D ( 'NONE', #6221, #9609, #5075 ) ;
#21480=ADVANCED_FACE ( 'NONE', ( #16591 ), #3000, .T. ) ;
#21489=AXIS2_PLACEMENT_3D ( 'NONE', #18427, #6823, #16646 ) ;
#21497=ORIENTED_EDGE ( 'NONE', *, *, #5326, .F. ) ;
#21499=CARTESIAN_POINT ( 'NONE',  ( 10.00000000000000000, 0.000000000000000000, 0.000000000000000000 ) ) ;
#21503=DIRECTION ( 'NONE',  ( -1.000000000000000000, -0.000000000000000000, -0.000000000000000000 ) ) ;
#21504=DIRECTION ( 'NONE',  ( -1.000000000000000000, 0.000000000000000000, 0.000000000000000000 ) ) ;
#21506=DIRECTION ( 'NONE',  ( 0.000000000000000000, 0.000000000000000000, 1.000000000000000000 ) ) ;
#21512=AXIS2_PLACEMENT_3D ( 'NONE', #15882, #19087, #17756 ) ;
#21517=DIRECTION ( 'NONE',  ( 0.000000000000000000, 0.000000000000000000, 1.000000000000000000 ) ) ;
#21526=VECTOR ( 'NONE', #4911, 1000.000000000000000 ) ;
#21530=DIRECTION ( 'NONE',  ( 0.000000000000000000, 0.000000000000000000, 1.000000000000000000 ) ) ;
#21531=CARTESIAN_POINT ( 'NONE',  ( 10.00000000000000000, 12.94633825542301153, -24.26081875733320814 ) ) ;
#21537=DIRECTION ( 'NONE',  ( 0.000000000000000000, 0.000000000000000000, 1.000000000000000000 ) ) ;
#21539=LINE ( 'NONE', #3410, #3345 ) ;
#21541=DIRECTION ( 'NONE',  ( 0.000000000000000000, 0.000000000000000000, 1.000000000000000000 ) ) ;
#21542=ORIENTED_EDGE ( 'NONE', *, *, #2843, .T. ) ;
#21548=ORIENTED_EDGE ( 'NONE', *, *, #11598, .F. ) ;
#21550=CIRCLE ( 'NONE', #9542, 12.00000000000000000 ) ;
#21551=CARTESIAN_POINT ( 'NONE',  ( 10.00000000000000000, -27.26034713664092379, 4.817140289263571518 ) ) ;
#21552=CARTESIAN_POINT ( 'NONE',  ( 0.000000000000000000, -21.69483248597433089, 16.89761061231773454 ) ) ;
#21553=FACE_OUTER_BOUND ( 'NONE', #21756, .T. ) ;
#21559=CARTESIAN_POINT ( 'NONE',  ( -10.00000000000000000, 0.000000000000000000, 0.000000000000000000 ) ) ;
#21560=STYLED_ITEM ( 'NONE', ( #13079 ), #7762 ) ;
#21563=DIRECTION ( 'NONE',  ( -1.000000000000000000, 0.000000000000000000, -0.000000000000000000 ) ) ;
#21572=EDGE_CURVE ( 'NONE', #13306, #2453, #16611, .T. ) ;
#21575=CARTESIAN_POINT ( 'NONE',  ( 0.000000000000000000, 27.40684453873989668, -16.51862198941980608 ) ) ;
#21580=DIRECTION ( 'NONE',  ( -1.000000000000000000, -0.000000000000000000, -0.000000000000000000 ) ) ;
#21582=LINE ( 'NONE', #6459, #1698 ) ;
#21583=VERTEX_POINT ( 'NONE', #19118 ) ;
#21592=EDGE_CURVE ( 'NONE', #1543, #13950, #15198, .T. ) ;
#21598=LINE ( 'NONE', #14963, #15696 ) ;
#21599=CARTESIAN_POINT ( 'NONE',  ( 10.00000000000000000, 21.69483248597422076, 16.89761061231787309 ) ) ;
#21600=DIRECTION ( 'NONE',  ( 1.000000000000000000, -0.000000000000000000, -0.000000000000000000 ) ) ;
#21602=CARTESIAN_POINT ( 'NONE',  ( 10.00000000000000000, 3.786343810537573518, 27.23708136986054029 ) ) ;
#21606=EDGE_CURVE ( 'NONE', #7135, #874, #3551, .T. ) ;
#21611=FACE_OUTER_BOUND ( 'NONE', #4807, .T. ) ;
#21616=CARTESIAN_POINT ( 'NONE',  ( 0.000000000000000000, 15.25521607131237722, -23.70650506194154872 ) ) ;
#21617=ORIENTED_EDGE ( 'NONE', *, *, #20544, .F. ) ;
#21619=EDGE_CURVE ( 'NONE', #16625, #12763, #19429, .T. ) ;
#21624=CYLINDRICAL_SURFACE ( 'NONE', #8445, 3.000000000000000444 ) ;
#21632=DIRECTION ( 'NONE',  ( -1.000000000000000000, 0.000000000000000000, -0.000000000000000000 ) ) ;
#21635=EDGE_CURVE ( 'NONE', #16691, #2943, #8494, .T. ) ;
#21639=ORIENTED_EDGE ( 'NONE', *, *, #3334, .T. ) ;
#21646=AXIS2_PLACEMENT_3D ( 'NONE', #4664, #19368, #11072 ) ;
#21651=CARTESIAN_POINT ( 'NONE',  ( 10.00000000000000000, -28.00896854772001987, 15.47571261340913473 ) ) ;
#21652=LINE ( 'NONE', #21551, #17038 ) ;
#21656=DIRECTION ( 'NONE',  ( -1.000000000000000000, 0.000000000000000000, 0.000000000000000000 ) ) ;
#21665=EDGE_CURVE ( 'NONE', #5595, #11788, #21550, .T. ) ;
#21666=ORIENTED_EDGE ( 'NONE', *, *, #21619, .T. ) ;
#21668=VECTOR ( 'NONE', #1169, 1000.000000000000000 ) ;
#21679=DIRECTION ( 'NONE',  ( -1.000000000000000000, 0.000000000000000000, -0.000000000000000000 ) ) ;
#21689=AXIS2_PLACEMENT_3D ( 'NONE', #19052, #9195, #5466 ) ;
#21691=VECTOR ( 'NONE', #8724, 1000.000000000000000 ) ;
#21692=DIRECTION ( 'NONE',  ( 0.000000000000000000, -0.9510565162951504226, -0.3090169943749573322 ) ) ;
#21695=CARTESIAN_POINT ( 'NONE',  ( 10.00000000000000000, 25.48117629651203941, -10.33947075754235989 ) ) ;
#21703=CARTESIAN_POINT ( 'NONE',  ( 0.000000000000000000, 25.17124263951009411, -12.69364185792227495 ) ) ;
#21707=DIRECTION ( 'NONE',  ( -1.000000000000000000, -0.000000000000000000, -0.000000000000000000 ) ) ;
#21709=LINE ( 'NONE', #19831, #12905 ) ;
#21711=CIRCLE ( 'NONE', #3006, 11.99999999999999822 ) ;
#21715=CYLINDRICAL_SURFACE ( 'NONE', #12694, 11.99999999999999822 ) ;
#21719=AXIS2_PLACEMENT_3D ( 'NONE', #6334, #899, #7644 ) ;
#21727=EDGE_CURVE ( 'NONE', #10528, #7709, #1415, .T. ) ;
#21738=CARTESIAN_POINT ( 'NONE',  ( 0.000000000000000000, -15.25521607131190294, -23.70650506194185425 ) ) ;
#21750=VERTEX_POINT ( 'NONE', #11133 ) ;
#21753=CIRCLE ( 'NONE', #243, 32.00000000000000000 ) ;
#21754=ORIENTED_EDGE ( 'NONE', *, *, #16212, .T. ) ;
#21756=EDGE_LOOP ( 'NONE', ( #2163, #100, #19615, #19061 ) ) ;
#21757=VERTEX_POINT ( 'NONE', #20512 ) ;
#21758=VERTEX_POINT ( 'NONE', #20084 ) ;
#21761=VERTEX_POINT ( 'NONE', #4948 ) ;
#21771=ORIENTED_EDGE ( 'NONE', *, *, #2566, .F. ) ;
#21777=LINE ( 'NONE', #8092, #4598 ) ;
#21778=ORIENTED_EDGE ( 'NONE', *, *, #7577, .T. ) ;
#21779=AXIS2_PLACEMENT_3D ( 'NONE', #3921, #179, #3494 ) ;
#21784=ADVANCED_FACE ( 'NONE', ( #15202 ), #11783, .T. ) ;
#21787=DIRECTION ( 'NONE',  ( 0.000000000000000000, 0.7431448254773908024, 0.6691306063588620123 ) ) ;
#21795=CARTESIAN_POINT ( 'NONE',  ( 0.000000000000000000, -26.69209308833512395, 6.612652082459228531 ) ) ;
#21811=CARTESIAN_POINT ( 'NONE',  ( 0.000000000000000000, 4.294029059350239486, -27.86182539015961979 ) ) ;
#21820=CARTESIAN_POINT ( 'NONE',  ( 5.000000000000000000, -0.6021240089803554518, 31.99433460282944708 ) ) ;
#21821=DIRECTION ( 'NONE',  ( -1.000000000000000000, -0.000000000000000000, -0.000000000000000000 ) ) ;
#21824=CARTESIAN_POINT ( 'NONE',  ( 10.00000000000000000, 19.07277123396541185, 19.80970465344755027 ) ) ;
#21829=ORIENTED_EDGE ( 'NONE', *, *, #8949, .T. ) ;
#21831=AXIS2_PLACEMENT_3D ( 'NONE', #1091, #21420, #9575 ) ;
#21837=CARTESIAN_POINT ( 'NONE',  ( 0.000000000000000000, 0.000000000000000000, 0.000000000000000000 ) ) ;
#21845=DIRECTION ( 'NONE',  ( -1.000000000000000000, 0.000000000000000000, -0.000000000000000000 ) ) ;
#21847=EDGE_CURVE ( 'NONE', #15418, #13049, #10974, .T. ) ;
#21848=AXIS2_PLACEMENT_3D ( 'NONE', #14880, #1506, #18529 ) ;
#21850=AXIS2_PLACEMENT_3D ( 'NONE', #394, #7246, #17406 ) ;
#21857=EDGE_LOOP ( 'NONE', ( #18854, #10448, #16431, #3354 ) ) ;
ENDSEC;
END-ISO-10303-21;
